ISO-10303-21;
HEADER;
/* Generated by software containing ST-Developer
 * from STEP Tools, Inc. (www.steptools.com) 
 */

FILE_DESCRIPTION(
/* description */ ('STEP AP214'),
/* implementation_level */ '2;1');

FILE_NAME(
/* name */ 'Main Cartridge Housing.step',
/* time_stamp */ '2026-10-06T00:19:40-07:00',
/* author */ (''),
/* organization */ (''),
/* preprocessor_version */ 'ST-DEVELOPER v20.2',
/* originating_system */ 'Autodesk Translation Framework v15.15.0.0',
/* authorisation */ '');

FILE_SCHEMA (('AUTOMOTIVE_DESIGN { 1 0 10303 214 3 1 1 }'));
ENDSEC;

DATA;
#10=MECHANICAL_DESIGN_GEOMETRIC_PRESENTATION_REPRESENTATION('',(#2069),#98302);
#59=(
BOUNDED_SURFACE()
B_SPLINE_SURFACE(3,3,((#83282,#83283,#83284,#83285),(#83286,#83287,#83288,
#83289),(#83290,#83291,#83292,#83293),(#83294,#83295,#83296,#83297),(#83298,
#83299,#83300,#83301),(#83302,#83303,#83304,#83305),(#83306,#83307,#83308,
#83309)),.UNSPECIFIED.,.F.,.F.,.F.)
B_SPLINE_SURFACE_WITH_KNOTS((4,3,4),(4,4),(0.,1.,1.00725260737196),(0.,
1.),.UNSPECIFIED.)
GEOMETRIC_REPRESENTATION_ITEM()
RATIONAL_B_SPLINE_SURFACE(((1.,0.333333333333333,0.333333333333333,1.),
(1.,0.333333333333333,0.333333333333333,1.),(1.,0.333333333333333,0.333333333333333,
1.),(1.,0.333333333333333,0.333333333333333,1.),(1.,0.333333333333333,0.333333333333333,
1.),(1.,0.333333333333333,0.333333333333333,1.),(1.,0.333333333333333,0.333333333333333,
1.)))
REPRESENTATION_ITEM('')
SURFACE()
);
#60=(
BOUNDED_SURFACE()
B_SPLINE_SURFACE(2,2,((#83938,#83939,#83940,#83941,#83942),(#83943,#83944,
#83945,#83946,#83947),(#83948,#83949,#83950,#83951,#83952),(#83953,#83954,
#83955,#83956,#83957),(#83958,#83959,#83960,#83961,#83962)),
 .UNSPECIFIED.,.F.,.F.,.F.)
B_SPLINE_SURFACE_WITH_KNOTS((3,2,3),(3,2,3),(0.,0.785398163496265,1.57079632699253),
(-2.06718528792769,-1.03359264376751,3.92659169068388E-10),
 .UNSPECIFIED.)
GEOMETRIC_REPRESENTATION_ITEM()
RATIONAL_B_SPLINE_SURFACE(((1.,0.869406567431186,1.,0.869406567431186,1.),
(0.923879532492386,0.803226933064135,0.923879532492386,0.803226933064135,
0.923879532492386),(1.,0.869406567431186,1.,0.869406567431186,1.),(0.92387953249249,
0.803226933064225,0.92387953249249,0.803226933064225,0.92387953249249),
(1.,0.869406567431186,1.,0.869406567431186,1.)))
REPRESENTATION_ITEM('')
SURFACE()
);
#61=(
BOUNDED_SURFACE()
B_SPLINE_SURFACE(2,2,((#84445,#84446,#84447,#84448,#84449),(#84450,#84451,
#84452,#84453,#84454),(#84455,#84456,#84457,#84458,#84459),(#84460,#84461,
#84462,#84463,#84464),(#84465,#84466,#84467,#84468,#84469)),
 .UNSPECIFIED.,.F.,.F.,.F.)
B_SPLINE_SURFACE_WITH_KNOTS((3,2,3),(3,2,3),(0.,0.785398163496265,1.57079632699253),
(-3.92659169068388E-10,1.03359264376751,2.06718528792769),.UNSPECIFIED.)
GEOMETRIC_REPRESENTATION_ITEM()
RATIONAL_B_SPLINE_SURFACE(((1.,0.869406567431186,1.,0.869406567431186,1.),
(0.923879532492386,0.803226933064135,0.923879532492386,0.803226933064135,
0.923879532492386),(1.,0.869406567431186,1.,0.869406567431186,1.),(0.92387953249249,
0.803226933064225,0.92387953249249,0.803226933064225,0.92387953249249),
(1.,0.869406567431186,1.,0.869406567431186,1.)))
REPRESENTATION_ITEM('')
SURFACE()
);
#62=(
BOUNDED_SURFACE()
B_SPLINE_SURFACE(3,3,((#85159,#85160,#85161,#85162),(#85163,#85164,#85165,
#85166),(#85167,#85168,#85169,#85170),(#85171,#85172,#85173,#85174),(#85175,
#85176,#85177,#85178),(#85179,#85180,#85181,#85182),(#85183,#85184,#85185,
#85186)),.UNSPECIFIED.,.F.,.F.,.F.)
B_SPLINE_SURFACE_WITH_KNOTS((4,3,4),(4,4),(0.,1.,1.00725260737198),(0.,
1.),.UNSPECIFIED.)
GEOMETRIC_REPRESENTATION_ITEM()
RATIONAL_B_SPLINE_SURFACE(((1.,0.333333333333333,0.333333333333333,1.),
(1.,0.333333333333333,0.333333333333333,1.),(1.,0.333333333333333,0.333333333333333,
1.),(1.,0.333333333333333,0.333333333333333,1.),(1.,0.333333333333333,0.333333333333333,
1.),(1.,0.333333333333333,0.333333333333333,1.),(1.,0.333333333333333,0.333333333333333,
1.)))
REPRESENTATION_ITEM('')
SURFACE()
);
#214=TOROIDAL_SURFACE('',#36474,0.8,0.3);
#215=TOROIDAL_SURFACE('',#36514,11.3,0.3);
#216=TOROIDAL_SURFACE('',#36520,0.8,0.3);
#624=ELLIPSE('',#36463,0.633386697976725,0.600234218712226);
#625=ELLIPSE('',#36470,0.298848745481257,0.296905215937904);
#626=ELLIPSE('',#36481,0.298864249839058,0.2969781551131);
#627=ELLIPSE('',#36482,0.635896586711713,0.60270133395858);
#628=ELLIPSE('',#36483,0.298848747221063,0.29690521700943);
#629=ELLIPSE('',#36505,0.633386697976725,0.600234218712226);
#630=ELLIPSE('',#36515,0.361788189515145,0.300001798267345);
#631=ELLIPSE('',#36516,0.298848773865698,0.296905284176984);
#632=ELLIPSE('',#36519,12.0546709739503,2.90799426775398);
#633=ELLIPSE('',#36527,0.298864504195414,0.296977933551803);
#634=ELLIPSE('',#36528,0.298848775543376,0.296905285050702);
#635=ELLIPSE('',#36529,0.635896586711713,0.60270133395858);
#1182=B_SPLINE_SURFACE_WITH_KNOTS('',5,5,((#83999,#84000,#84001,#84002,
#84003,#84004),(#84005,#84006,#84007,#84008,#84009,#84010),(#84011,#84012,
#84013,#84014,#84015,#84016),(#84017,#84018,#84019,#84020,#84021,#84022),
(#84023,#84024,#84025,#84026,#84027,#84028),(#84029,#84030,#84031,#84032,
#84033,#84034),(#84035,#84036,#84037,#84038,#84039,#84040),(#84041,#84042,
#84043,#84044,#84045,#84046),(#84047,#84048,#84049,#84050,#84051,#84052)),
 .UNSPECIFIED.,.F.,.F.,.F.,(6,3,6),(6,6),(1.66473273091,2.15120270837,2.76480988669),
(0.,0.3),.UNSPECIFIED.);
#1183=B_SPLINE_SURFACE_WITH_KNOTS('',2,5,((#84112,#84113,#84114,#84115,
#84116,#84117),(#84118,#84119,#84120,#84121,#84122,#84123),(#84124,#84125,
#84126,#84127,#84128,#84129)),.UNSPECIFIED.,.F.,.F.,.F.,(3,3),(6,6),(0.,
0.253192357174),(0.,0.3),.UNSPECIFIED.);
#1184=B_SPLINE_SURFACE_WITH_KNOTS('',5,5,((#84188,#84189,#84190,#84191,
#84192,#84193),(#84194,#84195,#84196,#84197,#84198,#84199),(#84200,#84201,
#84202,#84203,#84204,#84205),(#84206,#84207,#84208,#84209,#84210,#84211),
(#84212,#84213,#84214,#84215,#84216,#84217),(#84218,#84219,#84220,#84221,
#84222,#84223),(#84224,#84225,#84226,#84227,#84228,#84229),(#84230,#84231,
#84232,#84233,#84234,#84235),(#84236,#84237,#84238,#84239,#84240,#84241)),
 .UNSPECIFIED.,.F.,.F.,.F.,(6,3,6),(6,6),(1.53218389395,1.91811675676,2.24943434875),
(0.,0.3),.UNSPECIFIED.);
#1185=B_SPLINE_SURFACE_WITH_KNOTS('',5,5,((#84279,#84280,#84281,#84282,
#84283,#84284),(#84285,#84286,#84287,#84288,#84289,#84290),(#84291,#84292,
#84293,#84294,#84295,#84296),(#84297,#84298,#84299,#84300,#84301,#84302),
(#84303,#84304,#84305,#84306,#84307,#84308),(#84309,#84310,#84311,#84312,
#84313,#84314),(#84315,#84316,#84317,#84318,#84319,#84320),(#84321,#84322,
#84323,#84324,#84325,#84326),(#84327,#84328,#84329,#84330,#84331,#84332)),
 .UNSPECIFIED.,.F.,.F.,.F.,(6,3,6),(6,6),(2.14863240656,2.81847755741,3.42099781868),
(0.,0.3),.UNSPECIFIED.);
#1186=B_SPLINE_SURFACE_WITH_KNOTS('',4,5,((#84384,#84385,#84386,#84387,
#84388,#84389),(#84390,#84391,#84392,#84393,#84394,#84395),(#84396,#84397,
#84398,#84399,#84400,#84401),(#84402,#84403,#84404,#84405,#84406,#84407),
(#84408,#84409,#84410,#84411,#84412,#84413)),.UNSPECIFIED.,.F.,.F.,.F.,
(5,5),(6,6),(1.5664121072,1.61647585835),(0.,0.3),.UNSPECIFIED.);
#1187=B_SPLINE_SURFACE_WITH_KNOTS('',5,5,((#84507,#84508,#84509,#84510,
#84511,#84512),(#84513,#84514,#84515,#84516,#84517,#84518),(#84519,#84520,
#84521,#84522,#84523,#84524),(#84525,#84526,#84527,#84528,#84529,#84530),
(#84531,#84532,#84533,#84534,#84535,#84536),(#84537,#84538,#84539,#84540,
#84541,#84542),(#84543,#84544,#84545,#84546,#84547,#84548),(#84549,#84550,
#84551,#84552,#84553,#84554),(#84555,#84556,#84557,#84558,#84559,#84560)),
 .UNSPECIFIED.,.F.,.F.,.F.,(6,3,6),(6,6),(1.66473273091,2.15120270837,2.76480988669),
(0.,0.3),.UNSPECIFIED.);
#1188=B_SPLINE_SURFACE_WITH_KNOTS('',2,5,((#84566,#84567,#84568,#84569,
#84570,#84571),(#84572,#84573,#84574,#84575,#84576,#84577),(#84578,#84579,
#84580,#84581,#84582,#84583)),.UNSPECIFIED.,.F.,.F.,.F.,(3,3),(6,6),(0.,
0.253192357174),(0.,0.3),.UNSPECIFIED.);
#1189=B_SPLINE_SURFACE_WITH_KNOTS('',5,5,((#84679,#84680,#84681,#84682,
#84683,#84684),(#84685,#84686,#84687,#84688,#84689,#84690),(#84691,#84692,
#84693,#84694,#84695,#84696),(#84697,#84698,#84699,#84700,#84701,#84702),
(#84703,#84704,#84705,#84706,#84707,#84708),(#84709,#84710,#84711,#84712,
#84713,#84714),(#84715,#84716,#84717,#84718,#84719,#84720),(#84721,#84722,
#84723,#84724,#84725,#84726),(#84727,#84728,#84729,#84730,#84731,#84732)),
 .UNSPECIFIED.,.F.,.F.,.F.,(6,3,6),(6,6),(1.53218389395,1.91811675676,2.24943434875),
(0.,0.3),.UNSPECIFIED.);
#1190=B_SPLINE_SURFACE_WITH_KNOTS('',5,5,((#84767,#84768,#84769,#84770,
#84771,#84772),(#84773,#84774,#84775,#84776,#84777,#84778),(#84779,#84780,
#84781,#84782,#84783,#84784),(#84785,#84786,#84787,#84788,#84789,#84790),
(#84791,#84792,#84793,#84794,#84795,#84796),(#84797,#84798,#84799,#84800,
#84801,#84802),(#84803,#84804,#84805,#84806,#84807,#84808),(#84809,#84810,
#84811,#84812,#84813,#84814),(#84815,#84816,#84817,#84818,#84819,#84820)),
 .UNSPECIFIED.,.F.,.F.,.F.,(6,3,6),(6,6),(2.14863240656,2.81847755741,3.42099781868),
(0.,0.3),.UNSPECIFIED.);
#1191=B_SPLINE_SURFACE_WITH_KNOTS('',4,5,((#84872,#84873,#84874,#84875,
#84876,#84877),(#84878,#84879,#84880,#84881,#84882,#84883),(#84884,#84885,
#84886,#84887,#84888,#84889),(#84890,#84891,#84892,#84893,#84894,#84895),
(#84896,#84897,#84898,#84899,#84900,#84901)),.UNSPECIFIED.,.F.,.F.,.F.,
(5,5),(6,6),(1.5664121072,1.61647585835),(0.,0.3),.UNSPECIFIED.);
#1301=FACE_BOUND('',#6609,.T.);
#1302=FACE_BOUND('',#6619,.T.);
#1303=FACE_BOUND('',#6620,.T.);
#1304=FACE_BOUND('',#6622,.T.);
#1305=FACE_BOUND('',#6623,.T.);
#1306=FACE_BOUND('',#6662,.T.);
#1307=FACE_BOUND('',#6715,.T.);
#1308=FACE_BOUND('',#6718,.T.);
#1830=B_SPLINE_CURVE_WITH_KNOTS('',3,(#83314,#83315,#83316,#83317),
 .UNSPECIFIED.,.F.,.F.,(4,4),(0.,1.),.UNSPECIFIED.);
#1831=B_SPLINE_CURVE_WITH_KNOTS('',3,(#83321,#83322,#83323,#83324),
 .UNSPECIFIED.,.F.,.F.,(4,4),(0.,1.),.UNSPECIFIED.);
#1832=B_SPLINE_CURVE_WITH_KNOTS('',3,(#83328,#83329,#83330,#83331,#83332,
#83333,#83334,#83335,#83336,#83337,#83338,#83339,#83340,#83341,#83342,#83343,
#83344,#83345,#83346,#83347,#83348,#83349,#83350,#83351,#83352,#83353,#83354,
#83355,#83356,#83357),.UNSPECIFIED.,.F.,.F.,(4,2,2,2,2,2,2,2,2,2,2,2,2,
2,4),(-0.833290959100427,-0.719731949150803,-0.654120822724273,-0.577438704646923,
-0.501338594516947,-0.461398420908702,-0.440530284809963,-0.42516956916302,
-0.409392849496736,-0.386618223744604,-0.341743775261219,-0.248906272057569,
-0.173189557116592,-0.104522264822832,0.),.UNSPECIFIED.);
#1833=B_SPLINE_CURVE_WITH_KNOTS('',3,(#83361,#83362,#83363,#83364,#83365,
#83366,#83367,#83368,#83369,#83370,#83371,#83372,#83373,#83374,#83375,#83376,
#83377,#83378,#83379,#83380,#83381,#83382,#83383,#83384,#83385,#83386,#83387,
#83388,#83389,#83390,#83391,#83392,#83393,#83394),.UNSPECIFIED.,.F.,.F.,
(4,2,2,2,2,2,2,2,2,2,2,2,2,2,2,2,4),(-1.07487450803108,-1.01285655971456,
-0.949156086804949,-0.887082494974661,-0.773145859214011,-0.648162202604292,
-0.588558809942147,-0.558533895802779,-0.537355412523811,-0.51622241952717,
-0.486414822988416,-0.427362602801514,-0.303708789768619,-0.188644968303673,
-0.126436798617497,-0.0628185639370024,0.),.UNSPECIFIED.);
#1834=B_SPLINE_CURVE_WITH_KNOTS('',3,(#83397,#83398,#83399,#83400,#83401,
#83402,#83403,#83404,#83405,#83406,#83407,#83408,#83409,#83410,#83411,#83412,
#83413,#83414,#83415,#83416,#83417,#83418,#83419,#83420,#83421,#83422,#83423,
#83424,#83425,#83426),.UNSPECIFIED.,.F.,.F.,(4,2,2,2,2,2,2,2,2,2,2,2,2,
2,4),(-0.852996228072085,-0.748747176415804,-0.679888185472483,-0.60345940835717,
-0.506988533121608,-0.460271817616593,-0.436590151478536,-0.420246786301877,
-0.404384441460722,-0.382912427188685,-0.341869354576151,-0.263694658937176,
-0.184053280783239,-0.1167820739734,0.),.UNSPECIFIED.);
#1835=B_SPLINE_CURVE_WITH_KNOTS('',3,(#83442,#83443,#83444,#83445,#83446,
#83447,#83448,#83449,#83450,#83451),.UNSPECIFIED.,.F.,.F.,(4,3,3,4),(-0.253192357174,
-0.139449012417409,-0.0270751805148477,0.),.UNSPECIFIED.);
#1836=B_SPLINE_CURVE_WITH_KNOTS('',3,(#83459,#83460,#83461,#83462,#83463,
#83464,#83465,#83466,#83467,#83468),.UNSPECIFIED.,.F.,.F.,(4,3,3,4),(-0.253192357174,
-0.138730841190324,-0.0343582758464,0.),.UNSPECIFIED.);
#1837=B_SPLINE_CURVE_WITH_KNOTS('',3,(#83549,#83550,#83551,#83552,#83553,
#83554,#83555,#83556,#83557,#83558),.UNSPECIFIED.,.F.,.F.,(4,2,2,2,4),(-0.144315123192822,
-0.131533764343683,-0.118752405494545,-0.107522188711281,-0.0962919719280169),
 .UNSPECIFIED.);
#1838=B_SPLINE_CURVE_WITH_KNOTS('',3,(#83562,#83563,#83564,#83565,#83566,
#83567,#83568,#83569,#83570,#83571),.UNSPECIFIED.,.F.,.F.,(4,2,2,2,4),(-0.196399203297034,
-0.185168424394202,-0.17393764549137,-0.16054110108432,-0.14714455667727),
 .UNSPECIFIED.);
#1839=B_SPLINE_CURVE_WITH_KNOTS('',3,(#83579,#83580,#83581,#83582,#83583,
#83584,#83585,#83586,#83587,#83588),.UNSPECIFIED.,.F.,.F.,(4,2,2,2,4),(-0.0467821086425278,
-0.0346600950145953,-0.0225380813866629,-0.0112690406933315,0.),
 .UNSPECIFIED.);
#1840=B_SPLINE_CURVE_WITH_KNOTS('',3,(#83592,#83593,#83594,#83595,#83596,
#83597,#83598,#83599,#83600,#83601),.UNSPECIFIED.,.F.,.F.,(4,2,2,2,4),(0.140042886502516,
0.152164900130449,0.164286913758381,0.175555954451712,0.186824995145044),
 .UNSPECIFIED.);
#1841=B_SPLINE_CURVE_WITH_KNOTS('',3,(#83609,#83610,#83611,#83612,#83613,
#83614,#83615,#83616,#83617,#83618),.UNSPECIFIED.,.F.,.F.,(4,2,2,2,4),(0.,
0.0112307789028322,0.0224615578056644,0.0358581022127147,0.049254646619765),
 .UNSPECIFIED.);
#1842=B_SPLINE_CURVE_WITH_KNOTS('',3,(#83622,#83623,#83624,#83625,#83626,
#83627,#83628,#83629,#83630,#83631),.UNSPECIFIED.,.F.,.F.,(4,2,2,2,4),(0.0482688206632123,
0.0610501795123504,0.0738315383614886,0.0850617551447528,0.0962919719280169),
 .UNSPECIFIED.);
#1843=B_SPLINE_CURVE_WITH_KNOTS('',3,(#83654,#83655,#83656,#83657,#83658,
#83659,#83660,#83661,#83662,#83663),.UNSPECIFIED.,.F.,.F.,(4,2,2,2,4),(0.155359683062337,
0.174129548699776,0.192899414337214,0.212868752049424,0.232838089761635),
 .UNSPECIFIED.);
#1844=B_SPLINE_CURVE_WITH_KNOTS('',3,(#83667,#83668,#83669,#83670,#83671,
#83672,#83673,#83674,#83675,#83676),.UNSPECIFIED.,.F.,.F.,(4,2,2,2,4),(0.,
0.0376480157709213,0.0752960315418425,0.114456223316623,0.153616415091404),
 .UNSPECIFIED.);
#1845=B_SPLINE_CURVE_WITH_KNOTS('',3,(#83680,#83681,#83682,#83683,#83684,
#83685,#83686,#83687,#83688,#83689),.UNSPECIFIED.,.F.,.F.,(4,2,2,2,4),(0.152551363664982,
0.191711555439763,0.230871747214544,0.268519762985465,0.306167778756386),
 .UNSPECIFIED.);
#1846=B_SPLINE_CURVE_WITH_KNOTS('',3,(#83693,#83694,#83695,#83696,#83697,
#83698,#83699,#83700,#83701,#83702),.UNSPECIFIED.,.F.,.F.,(4,2,2,2,4),(0.233240959425377,
0.253210297137588,0.273179634849798,0.291949500487237,0.310719366124675),
 .UNSPECIFIED.);
#1847=B_SPLINE_CURVE_WITH_KNOTS('',3,(#83706,#83707,#83708,#83709,#83710,
#83711,#83712,#83713,#83714,#83715),.UNSPECIFIED.,.F.,.F.,(4,2,2,2,4),(0.,
0.0187909725801054,0.0375819451602107,0.057142029435283,0.0767021137103553),
 .UNSPECIFIED.);
#1848=B_SPLINE_CURVE_WITH_KNOTS('',3,(#83719,#83720,#83721,#83722,#83723,
#83724,#83725,#83726,#83727,#83728),.UNSPECIFIED.,.F.,.F.,(4,2,2,2,4),(0.304035731537011,
0.341700659844232,0.379365588151452,0.417900205299532,0.456434822447611),
 .UNSPECIFIED.);
#1849=B_SPLINE_CURVE_WITH_KNOTS('',3,(#83732,#83733,#83734,#83735,#83736,
#83737,#83738,#83739,#83740,#83741),.UNSPECIFIED.,.F.,.F.,(4,2,2,2,4),(0.455672372163422,
0.494206989311501,0.53274160645958,0.570406534766801,0.608071463074022),
 .UNSPECIFIED.);
#1850=B_SPLINE_CURVE_WITH_KNOTS('',3,(#83744,#83745,#83746,#83747,#83748,
#83749,#83750,#83751,#83752,#83753),.UNSPECIFIED.,.F.,.F.,(4,2,2,2,4),(0.0770095720919635,
0.0965696563670357,0.116129740642108,0.134920713222213,0.153711685802319),
 .UNSPECIFIED.);
#1851=B_SPLINE_CURVE_WITH_KNOTS('',3,(#83760,#83761,#83762,#83763,#83764,
#83765,#83766,#83767,#83768,#83769),.UNSPECIFIED.,.F.,.F.,(4,2,2,2,4),(-0.153352484887989,
-0.134556531278179,-0.115760577668369,-0.0962856459910287,-0.0768107143136885),
 .UNSPECIFIED.);
#1852=B_SPLINE_CURVE_WITH_KNOTS('',3,(#83773,#83774,#83775,#83776,#83777,
#83778,#83779,#83780,#83781,#83782),.UNSPECIFIED.,.F.,.F.,(4,2,2,2,4),(-0.607454139351607,
-0.569789123310172,-0.532124107268736,-0.493689195876788,-0.45525428448484),
 .UNSPECIFIED.);
#1853=B_SPLINE_CURVE_WITH_KNOTS('',3,(#83786,#83787,#83788,#83789,#83790,
#83791,#83792,#83793,#83794,#83795),.UNSPECIFIED.,.F.,.F.,(4,2,2,2,4),(-0.455926924542571,
-0.417492013150623,-0.379057101758675,-0.341392085717239,-0.303727069675804),
 .UNSPECIFIED.);
#1854=B_SPLINE_CURVE_WITH_KNOTS('',3,(#83799,#83800,#83801,#83802,#83803,
#83804,#83805,#83806,#83807,#83808),.UNSPECIFIED.,.F.,.F.,(4,2,2,2,4),(-0.0765417705743012,
-0.0570668388969609,-0.0375919072196206,-0.0187959536098103,0.),
 .UNSPECIFIED.);
#1855=B_SPLINE_CURVE_WITH_KNOTS('',3,(#83812,#83813,#83814,#83815,#83816,
#83817,#83818,#83819,#83820,#83821),.UNSPECIFIED.,.F.,.F.,(4,2,2,2,4),(-0.309577812617237,
-0.29080046183718,-0.272023111057122,-0.252190592955192,-0.232358074853261),
 .UNSPECIFIED.);
#1856=B_SPLINE_CURVE_WITH_KNOTS('',3,(#83825,#83826,#83827,#83828,#83829,
#83830,#83831,#83832,#83833,#83834),.UNSPECIFIED.,.F.,.F.,(4,2,2,2,4),(-0.30560294875119,
-0.267953353992129,-0.230303759233068,-0.191318992716313,-0.152334226199558),
 .UNSPECIFIED.);
#1857=B_SPLINE_CURVE_WITH_KNOTS('',3,(#83838,#83839,#83840,#83841,#83842,
#83843,#83844,#83845,#83846,#83847),.UNSPECIFIED.,.F.,.F.,(4,2,2,2,4),(-0.153268722551632,
-0.114283956034877,-0.0752991895181218,-0.0376495947590609,-2.77555756156289E-17),
 .UNSPECIFIED.);
#1858=B_SPLINE_CURVE_WITH_KNOTS('',3,(#83851,#83852,#83853,#83854,#83855,
#83856,#83857,#83858,#83859,#83860),.UNSPECIFIED.,.F.,.F.,(4,2,2,2,4),(-0.232008644072594,
-0.212176125970663,-0.192343607868733,-0.173566257088676,-0.154788906308618),
 .UNSPECIFIED.);
#1859=B_SPLINE_CURVE_WITH_KNOTS('',5,(#83981,#83982,#83983,#83984,#83985,
#83986),.UNSPECIFIED.,.F.,.F.,(6,6),(0.,1.),.UNSPECIFIED.);
#1860=B_SPLINE_CURVE_WITH_KNOTS('',3,(#84055,#84056,#84057,#84058,#84059,
#84060,#84061,#84062,#84063,#84064,#84065,#84066,#84067,#84068,#84069,#84070,
#84071,#84072,#84073,#84074,#84075,#84076,#84077,#84078,#84079,#84080,#84081,
#84082,#84083,#84084,#84085,#84086,#84087,#84088,#84089,#84090,#84091,#84092,
#84093,#84094,#84095,#84096,#84097,#84098,#84099,#84100,#84101,#84102,#84103,
#84104,#84105,#84106,#84107,#84108,#84109),.UNSPECIFIED.,.F.,.F.,(4,3,3,
3,3,3,3,3,3,3,3,3,3,3,3,3,3,3,4),(0.,0.105101150010298,0.211780208222473,
0.250000000000078,0.350769437864941,0.375000000000119,0.43750000000015,
0.446703937993579,0.468750000000166,0.48437500000017,0.494150913539028,
0.500000000000174,0.587354816489945,0.669329229379294,0.750000000000087,
0.823686773495111,0.895618722555497,0.965577824896743,1.),.UNSPECIFIED.);
#1861=B_SPLINE_CURVE_WITH_KNOTS('',3,(#84137,#84138,#84139,#84140,#84141,
#84142,#84143,#84144,#84145,#84146,#84147,#84148,#84149,#84150,#84151,#84152,
#84153,#84154,#84155,#84156,#84157,#84158,#84159,#84160,#84161,#84162,#84163,
#84164,#84165,#84166,#84167),.UNSPECIFIED.,.F.,.F.,(4,3,3,3,3,3,3,3,3,3,
4),(1.53218401448002,1.66838947160658,1.72279580036,1.86752328695562,1.91811675676,
2.019356098765,2.09643752541409,2.12059544077,2.17333959204,2.22608374331,
2.24943434875),.UNSPECIFIED.);
#1862=B_SPLINE_CURVE_WITH_KNOTS('',5,(#84168,#84169,#84170,#84171,#84172,
#84173,#84174,#84175,#84176),.UNSPECIFIED.,.F.,.F.,(6,3,6),(0.,0.473543414125104,
1.),.UNSPECIFIED.);
#1863=B_SPLINE_CURVE_WITH_KNOTS('',5,(#84180,#84181,#84182,#84183,#84184,
#84185),.UNSPECIFIED.,.F.,.F.,(6,6),(-1.61647556848,-1.5664121072),
 .UNSPECIFIED.);
#1864=B_SPLINE_CURVE_WITH_KNOTS('',3,(#84243,#84244,#84245,#84246,#84247,
#84248,#84249,#84250,#84251,#84252,#84253,#84254,#84255,#84256,#84257,#84258,
#84259,#84260,#84261,#84262,#84263,#84264,#84265,#84266,#84267,#84268,#84269,
#84270,#84271,#84272,#84273),.UNSPECIFIED.,.F.,.F.,(4,3,3,3,3,3,3,3,3,3,
4),(5.40059579705348E-8,0.108408281448171,0.220095081705907,0.333600124442993,
0.450483280546452,0.466393453636723,0.5,0.618967115497545,0.74413257000632,
0.879599145160207,1.),.UNSPECIFIED.);
#1865=B_SPLINE_CURVE_WITH_KNOTS('',3,(#84334,#84335,#84336,#84337,#84338,
#84339,#84340,#84341,#84342,#84343,#84344,#84345,#84346,#84347,#84348,#84349,
#84350,#84351,#84352,#84353,#84354,#84355,#84356,#84357,#84358,#84359,#84360,
#84361,#84362,#84363,#84364,#84365,#84366,#84367,#84368,#84369,#84370,#84371,
#84372,#84373,#84374,#84375,#84376,#84377,#84378,#84379,#84380,#84381,#84382),
 .UNSPECIFIED.,.F.,.F.,(4,3,3,3,3,3,3,3,3,3,3,3,3,3,3,3,4),(-3.42099781868,
-3.33892724177637,-3.26381939413,-3.17772035749469,-3.10665277284,-3.01841374448793,
-2.96248504801,-2.88144261558925,-2.81847755741,-2.71554484205924,-2.67456504578,
-2.53067648094,-2.39385786562,-2.28537736936454,-2.25703034102,-2.17618742334,
-2.14863240656),.UNSPECIFIED.);
#1866=B_SPLINE_CURVE_WITH_KNOTS('',3,(#84590,#84591,#84592,#84593,#84594,
#84595,#84596,#84597,#84598,#84599,#84600,#84601,#84602,#84603,#84604,#84605,
#84606,#84607,#84608,#84609,#84610,#84611,#84612,#84613,#84614,#84615,#84616,
#84617,#84618,#84619,#84620,#84621,#84622,#84623,#84624,#84625,#84626,#84627,
#84628,#84629,#84630,#84631,#84632,#84633,#84634,#84635),.UNSPECIFIED.,
 .F.,.F.,(4,3,3,3,3,3,3,3,3,3,3,3,3,3,3,4),(0.,0.0675680446171937,0.124999999999998,
0.170177845044704,0.219746219115553,0.249999999999996,0.32140342215739,
0.397256102134981,0.473108782112573,0.499999999999997,0.613366660168327,
0.686326334594986,0.749999999999999,0.837332896579508,0.925213195395331,
0.999999999999777),.UNSPECIFIED.);
#1867=B_SPLINE_CURVE_WITH_KNOTS('',3,(#84636,#84637,#84638,#84639,#84640,
#84641,#84642,#84643,#84644,#84645,#84646,#84647,#84648,#84649,#84650,#84651,
#84652,#84653,#84654,#84655,#84656,#84657,#84658,#84659,#84660,#84661,#84662,
#84663,#84664,#84665,#84666),.UNSPECIFIED.,.F.,.F.,(4,3,3,3,3,3,3,3,3,3,
4),(1.53218401448,1.66838947160656,1.72279580036,1.86752328695562,1.91811675676,
2.019356098765,2.09643752541409,2.12059544077,2.17333959204,2.22608374331,
2.24943434875),.UNSPECIFIED.);
#1868=B_SPLINE_CURVE_WITH_KNOTS('',5,(#84670,#84671,#84672,#84673,#84674,
#84675),.UNSPECIFIED.,.F.,.F.,(6,6),(-1.61647556848,-1.5664121072),
 .UNSPECIFIED.);
#1869=B_SPLINE_CURVE_WITH_KNOTS('',3,(#84735,#84736,#84737,#84738,#84739,
#84740,#84741,#84742,#84743,#84744,#84745,#84746,#84747,#84748,#84749,#84750,
#84751,#84752,#84753,#84754,#84755,#84756,#84757,#84758,#84759,#84760,#84761,
#84762),.UNSPECIFIED.,.F.,.F.,(4,3,3,3,3,3,3,3,3,4),(6.97389952659368E-8,
0.156232405135153,0.315775975767977,0.47610392685238,0.538072664088518,
0.67492807522622,0.766738756539317,0.849071536484418,0.924535768242209,
1.),.UNSPECIFIED.);
#1870=B_SPLINE_CURVE_WITH_KNOTS('',3,(#84823,#84824,#84825,#84826,#84827,
#84828,#84829,#84830,#84831,#84832,#84833,#84834,#84835,#84836,#84837,#84838,
#84839,#84840,#84841,#84842,#84843,#84844,#84845,#84846,#84847,#84848,#84849,
#84850,#84851,#84852,#84853,#84854,#84855,#84856,#84857,#84858,#84859,#84860,
#84861,#84862,#84863,#84864,#84865,#84866,#84867,#84868,#84869,#84870,#84871),
 .UNSPECIFIED.,.F.,.F.,(4,3,3,3,3,3,3,3,3,3,3,3,3,3,3,3,4),(-3.42099781868,
-3.33892724177637,-3.26381939413,-3.17772035749469,-3.10665277284,-3.01841374448793,
-2.96248504801,-2.88144261558925,-2.81847755741,-2.71554484205924,-2.67456504578,
-2.53067648094,-2.39385786562,-2.28537736936454,-2.25703034102,-2.17618742334,
-2.14863240656),.UNSPECIFIED.);
#1871=B_SPLINE_CURVE_WITH_KNOTS('',3,(#85045,#85046,#85047,#85048,#85049,
#85050,#85051,#85052,#85053,#85054,#85055,#85056,#85057,#85058,#85059,#85060,
#85061,#85062,#85063,#85064,#85065,#85066,#85067,#85068,#85069,#85070,#85071,
#85072,#85073,#85074),.UNSPECIFIED.,.F.,.F.,(4,2,2,2,2,2,2,2,2,2,2,2,2,
2,4),(-0.833290959113763,-0.71973194916232,-0.654120822734474,-0.577438704655354,
-0.501338594523518,-0.4613984209143,-0.440530284815032,-0.425169569167644,
-0.409392849500976,-0.38661822374839,-0.341743775264109,-0.248906272058694,
-0.173189557116784,-0.104522264822944,0.),.UNSPECIFIED.);
#1872=B_SPLINE_CURVE_WITH_KNOTS('',3,(#85082,#85083,#85084,#85085,#85086,
#85087,#85088,#85089,#85090,#85091,#85092,#85093,#85094,#85095,#85096,#85097,
#85098,#85099,#85100,#85101,#85102,#85103,#85104,#85105,#85106,#85107,#85108,
#85109,#85110,#85111,#85112,#85113,#85114,#85115),.UNSPECIFIED.,.F.,.F.,
(4,2,2,2,2,2,2,2,2,2,2,2,2,2,2,2,4),(-1.07487450803614,-1.0128565597187,
-0.949156086808256,-0.887082494977377,-0.773145859215987,-0.648162202605535,
-0.588558809943016,-0.558533895803447,-0.537355412524404,-0.516222419527731,
-0.486414822988885,-0.427362602801782,-0.303708789768471,-0.188644968303642,
-0.126436798617536,-0.0628185639369926,0.),.UNSPECIFIED.);
#1873=B_SPLINE_CURVE_WITH_KNOTS('',3,(#85123,#85124,#85125,#85126,#85127,
#85128,#85129,#85130,#85131,#85132,#85133,#85134,#85135,#85136,#85137,#85138,
#85139,#85140,#85141,#85142,#85143,#85144,#85145,#85146,#85147,#85148,#85149,
#85150,#85151,#85152),.UNSPECIFIED.,.F.,.F.,(4,2,2,2,2,2,2,2,2,2,2,2,2,
2,4),(-0.852996228067092,-0.748747176411645,-0.679888185468851,-0.603459408354018,
-0.506988533119108,-0.4602718176145,-0.436590151476641,-0.420246786300089,
-0.404384441459014,-0.38291242718713,-0.341869354574893,-0.263694658936475,
-0.184053280783088,-0.116782073973477,0.),.UNSPECIFIED.);
#2049=SHAPE_REPRESENTATION_RELATIONSHIP('SRR','None',#98346,#2059);
#2059=ADVANCED_BREP_SHAPE_REPRESENTATION('',(#2078),#98298);
#2069=STYLED_ITEM('',(#98399),#2078);
#2078=MANIFOLD_SOLID_BREP('Body1',#34175);
#2323=PLANE('',#36382);
#2324=PLANE('',#36385);
#2325=PLANE('',#36388);
#2326=PLANE('',#36389);
#2327=PLANE('',#36390);
#2328=PLANE('',#36393);
#2329=PLANE('',#36396);
#2330=PLANE('',#36397);
#2331=PLANE('',#36398);
#2332=PLANE('',#36428);
#2333=PLANE('',#36429);
#2334=PLANE('',#36445);
#2335=PLANE('',#36449);
#2336=PLANE('',#36450);
#2337=PLANE('',#36454);
#2338=PLANE('',#36462);
#2339=PLANE('',#36466);
#2340=PLANE('',#36477);
#2341=PLANE('',#36485);
#2342=PLANE('',#36492);
#2343=PLANE('',#36499);
#2344=PLANE('',#36504);
#2345=PLANE('',#36509);
#2346=PLANE('',#36523);
#2347=PLANE('',#36531);
#2348=PLANE('',#36532);
#2349=PLANE('',#36533);
#2350=PLANE('',#36549);
#2351=PLANE('',#36553);
#2352=PLANE('',#36554);
#2353=PLANE('',#36555);
#2354=PLANE('',#36557);
#2355=PLANE('',#36559);
#2356=PLANE('',#36560);
#2357=PLANE('',#36562);
#2358=PLANE('',#36564);
#2359=PLANE('',#36567);
#2360=PLANE('',#36570);
#2361=PLANE('',#36573);
#2362=PLANE('',#36574);
#2363=PLANE('',#36575);
#2364=PLANE('',#36576);
#2365=PLANE('',#36577);
#2366=PLANE('',#36578);
#2367=PLANE('',#36579);
#2368=PLANE('',#36586);
#2369=PLANE('',#36588);
#2370=PLANE('',#36591);
#2371=PLANE('',#36594);
#2372=PLANE('',#36597);
#2373=PLANE('',#36600);
#2891=CYLINDRICAL_SURFACE('',#36379,11.);
#2892=CYLINDRICAL_SURFACE('',#36401,16.4);
#2893=CYLINDRICAL_SURFACE('',#36422,17.4);
#2894=CYLINDRICAL_SURFACE('',#36430,15.);
#2895=CYLINDRICAL_SURFACE('',#36433,2.);
#2896=CYLINDRICAL_SURFACE('',#36436,13.5);
#2897=CYLINDRICAL_SURFACE('',#36439,0.5);
#2898=CYLINDRICAL_SURFACE('',#36442,0.5);
#2899=CYLINDRICAL_SURFACE('',#36446,0.5);
#2900=CYLINDRICAL_SURFACE('',#36451,0.1);
#2901=CYLINDRICAL_SURFACE('',#36455,0.500000000000001);
#2902=CYLINDRICAL_SURFACE('',#36461,0.300000000000002);
#2903=CYLINDRICAL_SURFACE('',#36464,0.3);
#2904=CYLINDRICAL_SURFACE('',#36467,0.1);
#2905=CYLINDRICAL_SURFACE('',#36471,0.300000000000002);
#2906=CYLINDRICAL_SURFACE('',#36476,0.3);
#2907=CYLINDRICAL_SURFACE('',#36479,0.499999999999999);
#2908=CYLINDRICAL_SURFACE('',#36484,0.3);
#2909=CYLINDRICAL_SURFACE('',#36486,15.4);
#2910=CYLINDRICAL_SURFACE('',#36489,0.1);
#2911=CYLINDRICAL_SURFACE('',#36493,0.500000000000001);
#2912=CYLINDRICAL_SURFACE('',#36503,0.300000000000002);
#2913=CYLINDRICAL_SURFACE('',#36506,0.3);
#2914=CYLINDRICAL_SURFACE('',#36510,0.1);
#2915=CYLINDRICAL_SURFACE('',#36512,12.5);
#2916=CYLINDRICAL_SURFACE('',#36517,0.300000000000002);
#2917=CYLINDRICAL_SURFACE('',#36522,0.3);
#2918=CYLINDRICAL_SURFACE('',#36525,0.499999999999999);
#2919=CYLINDRICAL_SURFACE('',#36530,0.3);
#2920=CYLINDRICAL_SURFACE('',#36534,15.);
#2921=CYLINDRICAL_SURFACE('',#36537,2.);
#2922=CYLINDRICAL_SURFACE('',#36540,13.5);
#2923=CYLINDRICAL_SURFACE('',#36543,0.5);
#2924=CYLINDRICAL_SURFACE('',#36546,0.5);
#2925=CYLINDRICAL_SURFACE('',#36550,0.5);
#2926=CYLINDRICAL_SURFACE('',#36556,1.);
#2927=CYLINDRICAL_SURFACE('',#36558,1.);
#2928=CYLINDRICAL_SURFACE('',#36561,1.);
#2929=CYLINDRICAL_SURFACE('',#36563,1.);
#2930=CYLINDRICAL_SURFACE('',#36565,0.5);
#2931=CYLINDRICAL_SURFACE('',#36566,0.5);
#2932=CYLINDRICAL_SURFACE('',#36568,0.5);
#2933=CYLINDRICAL_SURFACE('',#36569,0.5);
#2934=CYLINDRICAL_SURFACE('',#36571,9.15);
#2935=CYLINDRICAL_SURFACE('',#36587,11.2571565141535);
#2936=CYLINDRICAL_SURFACE('',#36589,11.2571565141535);
#2937=CYLINDRICAL_SURFACE('',#36592,11.2571565141535);
#2938=CYLINDRICAL_SURFACE('',#36595,11.2571565141535);
#2939=CYLINDRICAL_SURFACE('',#36598,11.2571565141535);
#2940=CYLINDRICAL_SURFACE('',#36601,11.2571565141535);
#4418=FACE_OUTER_BOUND('',#6605,.T.);
#4419=FACE_OUTER_BOUND('',#6606,.T.);
#4420=FACE_OUTER_BOUND('',#6607,.T.);
#4421=FACE_OUTER_BOUND('',#6608,.T.);
#4422=FACE_OUTER_BOUND('',#6610,.T.);
#4423=FACE_OUTER_BOUND('',#6611,.T.);
#4424=FACE_OUTER_BOUND('',#6612,.T.);
#4425=FACE_OUTER_BOUND('',#6613,.T.);
#4426=FACE_OUTER_BOUND('',#6614,.T.);
#4427=FACE_OUTER_BOUND('',#6615,.T.);
#4428=FACE_OUTER_BOUND('',#6616,.T.);
#4429=FACE_OUTER_BOUND('',#6617,.T.);
#4430=FACE_OUTER_BOUND('',#6618,.T.);
#4431=FACE_OUTER_BOUND('',#6621,.T.);
#4432=FACE_OUTER_BOUND('',#6624,.T.);
#4433=FACE_OUTER_BOUND('',#6625,.T.);
#4434=FACE_OUTER_BOUND('',#6626,.T.);
#4435=FACE_OUTER_BOUND('',#6627,.T.);
#4436=FACE_OUTER_BOUND('',#6628,.T.);
#4437=FACE_OUTER_BOUND('',#6629,.T.);
#4438=FACE_OUTER_BOUND('',#6630,.T.);
#4439=FACE_OUTER_BOUND('',#6631,.T.);
#4440=FACE_OUTER_BOUND('',#6632,.T.);
#4441=FACE_OUTER_BOUND('',#6633,.T.);
#4442=FACE_OUTER_BOUND('',#6634,.T.);
#4443=FACE_OUTER_BOUND('',#6635,.T.);
#4444=FACE_OUTER_BOUND('',#6636,.T.);
#4445=FACE_OUTER_BOUND('',#6637,.T.);
#4446=FACE_OUTER_BOUND('',#6638,.T.);
#4447=FACE_OUTER_BOUND('',#6639,.T.);
#4448=FACE_OUTER_BOUND('',#6640,.T.);
#4449=FACE_OUTER_BOUND('',#6641,.T.);
#4450=FACE_OUTER_BOUND('',#6642,.T.);
#4451=FACE_OUTER_BOUND('',#6643,.T.);
#4452=FACE_OUTER_BOUND('',#6644,.T.);
#4453=FACE_OUTER_BOUND('',#6645,.T.);
#4454=FACE_OUTER_BOUND('',#6646,.T.);
#4455=FACE_OUTER_BOUND('',#6647,.T.);
#4456=FACE_OUTER_BOUND('',#6648,.T.);
#4457=FACE_OUTER_BOUND('',#6649,.T.);
#4458=FACE_OUTER_BOUND('',#6650,.T.);
#4459=FACE_OUTER_BOUND('',#6651,.T.);
#4460=FACE_OUTER_BOUND('',#6652,.T.);
#4461=FACE_OUTER_BOUND('',#6653,.T.);
#4462=FACE_OUTER_BOUND('',#6654,.T.);
#4463=FACE_OUTER_BOUND('',#6655,.T.);
#4464=FACE_OUTER_BOUND('',#6656,.T.);
#4465=FACE_OUTER_BOUND('',#6657,.T.);
#4466=FACE_OUTER_BOUND('',#6658,.T.);
#4467=FACE_OUTER_BOUND('',#6659,.T.);
#4468=FACE_OUTER_BOUND('',#6660,.T.);
#4469=FACE_OUTER_BOUND('',#6661,.T.);
#4470=FACE_OUTER_BOUND('',#6663,.T.);
#4471=FACE_OUTER_BOUND('',#6664,.T.);
#4472=FACE_OUTER_BOUND('',#6665,.T.);
#4473=FACE_OUTER_BOUND('',#6666,.T.);
#4474=FACE_OUTER_BOUND('',#6667,.T.);
#4475=FACE_OUTER_BOUND('',#6668,.T.);
#4476=FACE_OUTER_BOUND('',#6669,.T.);
#4477=FACE_OUTER_BOUND('',#6670,.T.);
#4478=FACE_OUTER_BOUND('',#6671,.T.);
#4479=FACE_OUTER_BOUND('',#6672,.T.);
#4480=FACE_OUTER_BOUND('',#6673,.T.);
#4481=FACE_OUTER_BOUND('',#6674,.T.);
#4482=FACE_OUTER_BOUND('',#6675,.T.);
#4483=FACE_OUTER_BOUND('',#6676,.T.);
#4484=FACE_OUTER_BOUND('',#6677,.T.);
#4485=FACE_OUTER_BOUND('',#6678,.T.);
#4486=FACE_OUTER_BOUND('',#6679,.T.);
#4487=FACE_OUTER_BOUND('',#6680,.T.);
#4488=FACE_OUTER_BOUND('',#6681,.T.);
#4489=FACE_OUTER_BOUND('',#6682,.T.);
#4490=FACE_OUTER_BOUND('',#6683,.T.);
#4491=FACE_OUTER_BOUND('',#6684,.T.);
#4492=FACE_OUTER_BOUND('',#6685,.T.);
#4493=FACE_OUTER_BOUND('',#6686,.T.);
#4494=FACE_OUTER_BOUND('',#6687,.T.);
#4495=FACE_OUTER_BOUND('',#6688,.T.);
#4496=FACE_OUTER_BOUND('',#6689,.T.);
#4497=FACE_OUTER_BOUND('',#6690,.T.);
#4498=FACE_OUTER_BOUND('',#6691,.T.);
#4499=FACE_OUTER_BOUND('',#6692,.T.);
#4500=FACE_OUTER_BOUND('',#6693,.T.);
#4501=FACE_OUTER_BOUND('',#6694,.T.);
#4502=FACE_OUTER_BOUND('',#6695,.T.);
#4503=FACE_OUTER_BOUND('',#6696,.T.);
#4504=FACE_OUTER_BOUND('',#6697,.T.);
#4505=FACE_OUTER_BOUND('',#6698,.T.);
#4506=FACE_OUTER_BOUND('',#6699,.T.);
#4507=FACE_OUTER_BOUND('',#6700,.T.);
#4508=FACE_OUTER_BOUND('',#6701,.T.);
#4509=FACE_OUTER_BOUND('',#6702,.T.);
#4510=FACE_OUTER_BOUND('',#6703,.T.);
#4511=FACE_OUTER_BOUND('',#6704,.T.);
#4512=FACE_OUTER_BOUND('',#6705,.T.);
#4513=FACE_OUTER_BOUND('',#6706,.T.);
#4514=FACE_OUTER_BOUND('',#6707,.T.);
#4515=FACE_OUTER_BOUND('',#6708,.T.);
#4516=FACE_OUTER_BOUND('',#6709,.T.);
#4517=FACE_OUTER_BOUND('',#6710,.T.);
#4518=FACE_OUTER_BOUND('',#6711,.T.);
#4519=FACE_OUTER_BOUND('',#6712,.T.);
#4520=FACE_OUTER_BOUND('',#6713,.T.);
#4521=FACE_OUTER_BOUND('',#6714,.T.);
#4522=FACE_OUTER_BOUND('',#6716,.T.);
#4523=FACE_OUTER_BOUND('',#6717,.T.);
#4524=FACE_OUTER_BOUND('',#6719,.T.);
#4525=FACE_OUTER_BOUND('',#6720,.T.);
#4526=FACE_OUTER_BOUND('',#6721,.T.);
#4527=FACE_OUTER_BOUND('',#6722,.T.);
#4528=FACE_OUTER_BOUND('',#6723,.T.);
#4529=FACE_OUTER_BOUND('',#6724,.T.);
#4530=FACE_OUTER_BOUND('',#6725,.T.);
#4531=FACE_OUTER_BOUND('',#6726,.T.);
#4532=FACE_OUTER_BOUND('',#6727,.T.);
#4533=FACE_OUTER_BOUND('',#6728,.T.);
#4534=FACE_OUTER_BOUND('',#6729,.T.);
#4535=FACE_OUTER_BOUND('',#6730,.T.);
#4536=FACE_OUTER_BOUND('',#6731,.T.);
#6605=EDGE_LOOP('',(#27343,#27344,#27345,#27346,#27347,#27348,#27349,#27350,
#27351,#27352));
#6606=EDGE_LOOP('',(#27353,#27354,#27355,#27356,#27357));
#6607=EDGE_LOOP('',(#27358,#27359,#27360,#27361,#27362,#27363,#27364,#27365));
#6608=EDGE_LOOP('',(#27366,#27367));
#6609=EDGE_LOOP('',(#27368));
#6610=EDGE_LOOP('',(#27369,#27370,#27371,#27372));
#6611=EDGE_LOOP('',(#27373,#27374,#27375,#27376));
#6612=EDGE_LOOP('',(#27377,#27378,#27379,#27380));
#6613=EDGE_LOOP('',(#27381,#27382,#27383,#27384));
#6614=EDGE_LOOP('',(#27385,#27386,#27387,#27388));
#6615=EDGE_LOOP('',(#27389,#27390,#27391,#27392));
#6616=EDGE_LOOP('',(#27393,#27394,#27395,#27396));
#6617=EDGE_LOOP('',(#27397,#27398,#27399,#27400));
#6618=EDGE_LOOP('',(#27401,#27402,#27403,#27404,#27405,#27406,#27407,#27408,
#27409,#27410,#27411,#27412,#27413,#27414,#27415,#27416,#27417,#27418,#27419,
#27420,#27421,#27422,#27423,#27424,#27425,#27426,#27427,#27428,#27429,#27430,
#27431,#27432,#27433,#27434,#27435,#27436,#27437,#27438,#27439,#27440,#27441,
#27442,#27443,#27444,#27445,#27446,#27447,#27448,#27449,#27450,#27451,#27452,
#27453,#27454));
#6619=EDGE_LOOP('',(#27455,#27456,#27457,#27458));
#6620=EDGE_LOOP('',(#27459,#27460,#27461,#27462));
#6621=EDGE_LOOP('',(#27463,#27464,#27465,#27466,#27467,#27468,#27469,#27470,
#27471,#27472,#27473,#27474,#27475,#27476,#27477,#27478,#27479,#27480,#27481,
#27482,#27483));
#6622=EDGE_LOOP('',(#27484,#27485,#27486,#27487));
#6623=EDGE_LOOP('',(#27488,#27489,#27490,#27491));
#6624=EDGE_LOOP('',(#27492,#27493,#27494,#27495));
#6625=EDGE_LOOP('',(#27496,#27497,#27498,#27499));
#6626=EDGE_LOOP('',(#27500,#27501,#27502,#27503));
#6627=EDGE_LOOP('',(#27504,#27505,#27506,#27507));
#6628=EDGE_LOOP('',(#27508,#27509,#27510,#27511));
#6629=EDGE_LOOP('',(#27512,#27513,#27514,#27515));
#6630=EDGE_LOOP('',(#27516,#27517,#27518,#27519));
#6631=EDGE_LOOP('',(#27520,#27521,#27522,#27523));
#6632=EDGE_LOOP('',(#27524,#27525,#27526,#27527));
#6633=EDGE_LOOP('',(#27528,#27529,#27530,#27531,#27532,#27533,#27534,#27535,
#27536,#27537,#27538,#27539));
#6634=EDGE_LOOP('',(#27540,#27541,#27542,#27543));
#6635=EDGE_LOOP('',(#27544,#27545,#27546,#27547));
#6636=EDGE_LOOP('',(#27548,#27549,#27550,#27551));
#6637=EDGE_LOOP('',(#27552,#27553,#27554,#27555));
#6638=EDGE_LOOP('',(#27556,#27557,#27558,#27559));
#6639=EDGE_LOOP('',(#27560,#27561,#27562,#27563));
#6640=EDGE_LOOP('',(#27564,#27565,#27566,#27567,#27568,#27569,#27570));
#6641=EDGE_LOOP('',(#27571,#27572,#27573,#27574));
#6642=EDGE_LOOP('',(#27575,#27576,#27577,#27578));
#6643=EDGE_LOOP('',(#27579,#27580,#27581,#27582));
#6644=EDGE_LOOP('',(#27583,#27584,#27585,#27586));
#6645=EDGE_LOOP('',(#27587,#27588,#27589,#27590));
#6646=EDGE_LOOP('',(#27591,#27592,#27593));
#6647=EDGE_LOOP('',(#27594,#27595,#27596,#27597,#27598));
#6648=EDGE_LOOP('',(#27599,#27600,#27601,#27602,#27603));
#6649=EDGE_LOOP('',(#27604,#27605,#27606,#27607));
#6650=EDGE_LOOP('',(#27608,#27609,#27610,#27611));
#6651=EDGE_LOOP('',(#27612,#27613,#27614,#27615));
#6652=EDGE_LOOP('',(#27616,#27617,#27618,#27619));
#6653=EDGE_LOOP('',(#27620,#27621,#27622,#27623));
#6654=EDGE_LOOP('',(#27624,#27625,#27626,#27627));
#6655=EDGE_LOOP('',(#27628,#27629,#27630,#27631,#27632,#27633));
#6656=EDGE_LOOP('',(#27634,#27635,#27636,#27637));
#6657=EDGE_LOOP('',(#27638,#27639,#27640,#27641));
#6658=EDGE_LOOP('',(#27642,#27643,#27644,#27645));
#6659=EDGE_LOOP('',(#27646,#27647,#27648,#27649));
#6660=EDGE_LOOP('',(#27650,#27651,#27652,#27653));
#6661=EDGE_LOOP('',(#27654,#27655,#27656,#27657,#27658,#27659));
#6662=EDGE_LOOP('',(#27660,#27661,#27662,#27663,#27664,#27665,#27666,#27667));
#6663=EDGE_LOOP('',(#27668,#27669,#27670,#27671));
#6664=EDGE_LOOP('',(#27672,#27673,#27674,#27675,#27676,#27677,#27678));
#6665=EDGE_LOOP('',(#27679,#27680,#27681,#27682));
#6666=EDGE_LOOP('',(#27683,#27684,#27685,#27686));
#6667=EDGE_LOOP('',(#27687,#27688,#27689,#27690));
#6668=EDGE_LOOP('',(#27691,#27692,#27693,#27694));
#6669=EDGE_LOOP('',(#27695,#27696,#27697,#27698));
#6670=EDGE_LOOP('',(#27699,#27700,#27701,#27702));
#6671=EDGE_LOOP('',(#27703,#27704,#27705,#27706));
#6672=EDGE_LOOP('',(#27707,#27708,#27709));
#6673=EDGE_LOOP('',(#27710,#27711,#27712,#27713,#27714));
#6674=EDGE_LOOP('',(#27715,#27716,#27717,#27718,#27719));
#6675=EDGE_LOOP('',(#27720,#27721,#27722,#27723));
#6676=EDGE_LOOP('',(#27724,#27725,#27726,#27727));
#6677=EDGE_LOOP('',(#27728,#27729,#27730,#27731));
#6678=EDGE_LOOP('',(#27732,#27733,#27734,#27735));
#6679=EDGE_LOOP('',(#27736,#27737,#27738,#27739));
#6680=EDGE_LOOP('',(#27740,#27741,#27742,#27743));
#6681=EDGE_LOOP('',(#27744,#27745,#27746,#27747,#27748,#27749));
#6682=EDGE_LOOP('',(#27750,#27751,#27752,#27753));
#6683=EDGE_LOOP('',(#27754,#27755,#27756,#27757));
#6684=EDGE_LOOP('',(#27758,#27759,#27760,#27761));
#6685=EDGE_LOOP('',(#27762,#27763,#27764,#27765));
#6686=EDGE_LOOP('',(#27766,#27767,#27768,#27769));
#6687=EDGE_LOOP('',(#27770,#27771,#27772,#27773));
#6688=EDGE_LOOP('',(#27774,#27775,#27776,#27777));
#6689=EDGE_LOOP('',(#27778,#27779,#27780,#27781));
#6690=EDGE_LOOP('',(#27782,#27783,#27784,#27785));
#6691=EDGE_LOOP('',(#27786,#27787,#27788,#27789,#27790,#27791,#27792,#27793,
#27794,#27795,#27796,#27797));
#6692=EDGE_LOOP('',(#27798,#27799,#27800,#27801));
#6693=EDGE_LOOP('',(#27802,#27803,#27804,#27805));
#6694=EDGE_LOOP('',(#27806,#27807,#27808,#27809));
#6695=EDGE_LOOP('',(#27810,#27811,#27812,#27813));
#6696=EDGE_LOOP('',(#27814,#27815,#27816,#27817));
#6697=EDGE_LOOP('',(#27818,#27819,#27820,#27821));
#6698=EDGE_LOOP('',(#27822,#27823,#27824,#27825));
#6699=EDGE_LOOP('',(#27826,#27827,#27828,#27829));
#6700=EDGE_LOOP('',(#27830,#27831,#27832,#27833));
#6701=EDGE_LOOP('',(#27834,#27835,#27836,#27837));
#6702=EDGE_LOOP('',(#27838,#27839,#27840,#27841));
#6703=EDGE_LOOP('',(#27842,#27843,#27844,#27845));
#6704=EDGE_LOOP('',(#27846,#27847,#27848,#27849));
#6705=EDGE_LOOP('',(#27850,#27851,#27852,#27853,#27854,#27855));
#6706=EDGE_LOOP('',(#27856,#27857,#27858,#27859));
#6707=EDGE_LOOP('',(#27860,#27861,#27862,#27863));
#6708=EDGE_LOOP('',(#27864,#27865,#27866,#27867));
#6709=EDGE_LOOP('',(#27868,#27869,#27870,#27871));
#6710=EDGE_LOOP('',(#27872,#27873,#27874,#27875));
#6711=EDGE_LOOP('',(#27876,#27877,#27878,#27879,#27880,#27881,#27882,#27883));
#6712=EDGE_LOOP('',(#27884,#27885,#27886,#27887));
#6713=EDGE_LOOP('',(#27888,#27889,#27890,#27891,#27892));
#6714=EDGE_LOOP('',(#27893,#27894,#27895,#27896,#27897,#27898,#27899,#27900,
#27901,#27902,#27903,#27904,#27905,#27906,#27907,#27908,#27909,#27910,#27911,
#27912,#27913));
#6715=EDGE_LOOP('',(#27914));
#6716=EDGE_LOOP('',(#27915,#27916,#27917,#27918,#27919));
#6717=EDGE_LOOP('',(#27920));
#6718=EDGE_LOOP('',(#27921,#27922,#27923,#27924,#27925,#27926,#27927,#27928,
#27929,#27930,#27931,#27932));
#6719=EDGE_LOOP('',(#27933,#27934,#27935,#27936));
#6720=EDGE_LOOP('',(#27937,#27938,#27939,#27940));
#6721=EDGE_LOOP('',(#27941,#27942,#27943,#27944));
#6722=EDGE_LOOP('',(#27945,#27946,#27947,#27948,#27949));
#6723=EDGE_LOOP('',(#27950,#27951,#27952,#27953));
#6724=EDGE_LOOP('',(#27954,#27955,#27956,#27957));
#6725=EDGE_LOOP('',(#27958,#27959,#27960,#27961));
#6726=EDGE_LOOP('',(#27962,#27963,#27964,#27965));
#6727=EDGE_LOOP('',(#27966,#27967,#27968,#27969));
#6728=EDGE_LOOP('',(#27970,#27971,#27972,#27973,#27974));
#6729=EDGE_LOOP('',(#27975,#27976,#27977,#27978));
#6730=EDGE_LOOP('',(#27979,#27980,#27981,#27982));
#6731=EDGE_LOOP('',(#27983,#27984,#27985,#27986,#27987,#27988,#27989,#27990,
#27991,#27992));
#8658=LINE('',#83433,#10498);
#8659=LINE('',#83440,#10499);
#8660=LINE('',#83453,#10500);
#8661=LINE('',#83457,#10501);
#8662=LINE('',#83469,#10502);
#8663=LINE('',#83477,#10503);
#8664=LINE('',#83481,#10504);
#8665=LINE('',#83485,#10505);
#8666=LINE('',#83487,#10506);
#8667=LINE('',#83488,#10507);
#8668=LINE('',#83492,#10508);
#8669=LINE('',#83493,#10509);
#8670=LINE('',#83494,#10510);
#8671=LINE('',#83501,#10511);
#8672=LINE('',#83505,#10512);
#8673=LINE('',#83509,#10513);
#8674=LINE('',#83511,#10514);
#8675=LINE('',#83512,#10515);
#8676=LINE('',#83515,#10516);
#8677=LINE('',#83517,#10517);
#8678=LINE('',#83518,#10518);
#8679=LINE('',#83527,#10519);
#8680=LINE('',#83531,#10520);
#8681=LINE('',#83535,#10521);
#8682=LINE('',#83539,#10522);
#8683=LINE('',#83543,#10523);
#8684=LINE('',#83547,#10524);
#8685=LINE('',#83573,#10525);
#8686=LINE('',#83577,#10526);
#8687=LINE('',#83603,#10527);
#8688=LINE('',#83607,#10528);
#8689=LINE('',#83633,#10529);
#8690=LINE('',#83637,#10530);
#8691=LINE('',#83641,#10531);
#8692=LINE('',#83645,#10532);
#8693=LINE('',#83649,#10533);
#8694=LINE('',#83665,#10534);
#8695=LINE('',#83691,#10535);
#8696=LINE('',#83717,#10536);
#8697=LINE('',#83743,#10537);
#8698=LINE('',#83756,#10538);
#8699=LINE('',#83771,#10539);
#8700=LINE('',#83797,#10540);
#8701=LINE('',#83823,#10541);
#8702=LINE('',#83849,#10542);
#8703=LINE('',#83864,#10543);
#8704=LINE('',#83866,#10544);
#8705=LINE('',#83867,#10545);
#8706=LINE('',#83870,#10546);
#8707=LINE('',#83872,#10547);
#8708=LINE('',#83873,#10548);
#8709=LINE('',#83879,#10549);
#8710=LINE('',#83886,#10550);
#8711=LINE('',#83890,#10551);
#8712=LINE('',#83895,#10552);
#8713=LINE('',#83902,#10553);
#8714=LINE('',#83905,#10554);
#8715=LINE('',#83906,#10555);
#8716=LINE('',#83912,#10556);
#8717=LINE('',#83914,#10557);
#8718=LINE('',#83916,#10558);
#8719=LINE('',#83922,#10559);
#8720=LINE('',#83925,#10560);
#8721=LINE('',#83928,#10561);
#8722=LINE('',#83930,#10562);
#8723=LINE('',#83931,#10563);
#8724=LINE('',#83937,#10564);
#8725=LINE('',#83969,#10565);
#8726=LINE('',#83970,#10566);
#8727=LINE('',#83973,#10567);
#8728=LINE('',#83977,#10568);
#8729=LINE('',#83978,#10569);
#8730=LINE('',#83988,#10570);
#8731=LINE('',#83991,#10571);
#8732=LINE('',#83992,#10572);
#8733=LINE('',#83997,#10573);
#8734=LINE('',#84111,#10574);
#8735=LINE('',#84179,#10575);
#8736=LINE('',#84187,#10576);
#8737=LINE('',#84278,#10577);
#8738=LINE('',#84418,#10578);
#8739=LINE('',#84420,#10579);
#8740=LINE('',#84424,#10580);
#8741=LINE('',#84431,#10581);
#8742=LINE('',#84435,#10582);
#8743=LINE('',#84437,#10583);
#8744=LINE('',#84438,#10584);
#8745=LINE('',#84442,#10585);
#8746=LINE('',#84476,#10586);
#8747=LINE('',#84482,#10587);
#8748=LINE('',#84485,#10588);
#8749=LINE('',#84487,#10589);
#8750=LINE('',#84490,#10590);
#8751=LINE('',#84495,#10591);
#8752=LINE('',#84498,#10592);
#8753=LINE('',#84499,#10593);
#8754=LINE('',#84502,#10594);
#8755=LINE('',#84565,#10595);
#8756=LINE('',#84676,#10596);
#8757=LINE('',#84678,#10597);
#8758=LINE('',#84765,#10598);
#8759=LINE('',#84906,#10599);
#8760=LINE('',#84908,#10600);
#8761=LINE('',#84911,#10601);
#8762=LINE('',#84913,#10602);
#8763=LINE('',#84914,#10603);
#8764=LINE('',#84917,#10604);
#8765=LINE('',#84919,#10605);
#8766=LINE('',#84920,#10606);
#8767=LINE('',#84926,#10607);
#8768=LINE('',#84933,#10608);
#8769=LINE('',#84937,#10609);
#8770=LINE('',#84942,#10610);
#8771=LINE('',#84949,#10611);
#8772=LINE('',#84952,#10612);
#8773=LINE('',#84953,#10613);
#8774=LINE('',#84959,#10614);
#8775=LINE('',#84961,#10615);
#8776=LINE('',#84963,#10616);
#8777=LINE('',#84965,#10617);
#8778=LINE('',#84966,#10618);
#8779=LINE('',#84968,#10619);
#8780=LINE('',#84970,#10620);
#8781=LINE('',#84972,#10621);
#8782=LINE('',#84974,#10622);
#8783=LINE('',#84976,#10623);
#8784=LINE('',#84977,#10624);
#8785=LINE('',#84979,#10625);
#8786=LINE('',#84981,#10626);
#8787=LINE('',#84983,#10627);
#8788=LINE('',#84985,#10628);
#8789=LINE('',#84987,#10629);
#8790=LINE('',#84989,#10630);
#8791=LINE('',#84992,#10631);
#8792=LINE('',#84994,#10632);
#8793=LINE('',#84999,#10633);
#8794=LINE('',#85011,#10634);
#8795=LINE('',#85015,#10635);
#8796=LINE('',#85019,#10636);
#8797=LINE('',#85023,#10637);
#8798=LINE('',#85027,#10638);
#8799=LINE('',#85030,#10639);
#8800=LINE('',#85032,#10640);
#8801=LINE('',#85033,#10641);
#8802=LINE('',#85035,#10642);
#8803=LINE('',#85037,#10643);
#8804=LINE('',#85040,#10644);
#8805=LINE('',#85044,#10645);
#8806=LINE('',#85077,#10646);
#8807=LINE('',#85081,#10647);
#8808=LINE('',#85118,#10648);
#8809=LINE('',#85122,#10649);
#8810=LINE('',#85154,#10650);
#8811=LINE('',#85157,#10651);
#10498=VECTOR('',#43813,16.4);
#10499=VECTOR('',#43820,1000.);
#10500=VECTOR('',#43821,1000.);
#10501=VECTOR('',#43824,1000.);
#10502=VECTOR('',#43825,1000.);
#10503=VECTOR('',#43834,1000.);
#10504=VECTOR('',#43837,1000.);
#10505=VECTOR('',#43842,1000.);
#10506=VECTOR('',#43843,1000.);
#10507=VECTOR('',#43844,1000.);
#10508=VECTOR('',#43847,1000.);
#10509=VECTOR('',#43848,1000.);
#10510=VECTOR('',#43849,1000.);
#10511=VECTOR('',#43858,1000.);
#10512=VECTOR('',#43861,1000.);
#10513=VECTOR('',#43866,1000.);
#10514=VECTOR('',#43867,1000.);
#10515=VECTOR('',#43868,1000.);
#10516=VECTOR('',#43871,1000.);
#10517=VECTOR('',#43872,1000.);
#10518=VECTOR('',#43873,1000.);
#10519=VECTOR('',#43884,16.4);
#10520=VECTOR('',#43887,1000.);
#10521=VECTOR('',#43890,1000.);
#10522=VECTOR('',#43893,1000.);
#10523=VECTOR('',#43896,1000.);
#10524=VECTOR('',#43899,1000.);
#10525=VECTOR('',#43902,1000.);
#10526=VECTOR('',#43905,1000.);
#10527=VECTOR('',#43908,1000.);
#10528=VECTOR('',#43911,1000.);
#10529=VECTOR('',#43914,1000.);
#10530=VECTOR('',#43917,1000.);
#10531=VECTOR('',#43920,1000.);
#10532=VECTOR('',#43923,1000.);
#10533=VECTOR('',#43926,1000.);
#10534=VECTOR('',#43931,1000.);
#10535=VECTOR('',#43934,1000.);
#10536=VECTOR('',#43937,1000.);
#10537=VECTOR('',#43940,1000.);
#10538=VECTOR('',#43943,17.4);
#10539=VECTOR('',#43946,1000.);
#10540=VECTOR('',#43949,1000.);
#10541=VECTOR('',#43952,1000.);
#10542=VECTOR('',#43955,1000.);
#10543=VECTOR('',#43960,10.);
#10544=VECTOR('',#43961,1000.);
#10545=VECTOR('',#43962,1000.);
#10546=VECTOR('',#43965,1000.);
#10547=VECTOR('',#43966,1000.);
#10548=VECTOR('',#43967,10.);
#10549=VECTOR('',#43974,1000.);
#10550=VECTOR('',#43983,1000.);
#10551=VECTOR('',#43986,1000.);
#10552=VECTOR('',#43991,1000.);
#10553=VECTOR('',#44000,1000.);
#10554=VECTOR('',#44005,1000.);
#10555=VECTOR('',#44006,10.);
#10556=VECTOR('',#44013,1000.);
#10557=VECTOR('',#44016,1000.);
#10558=VECTOR('',#44019,10.);
#10559=VECTOR('',#44024,1000.);
#10560=VECTOR('',#44027,1000.);
#10561=VECTOR('',#44030,10.);
#10562=VECTOR('',#44031,1000.);
#10563=VECTOR('',#44032,1000.);
#10564=VECTOR('',#44039,1000.);
#10565=VECTOR('',#44048,1000.);
#10566=VECTOR('',#44049,1000.);
#10567=VECTOR('',#44052,1000.);
#10568=VECTOR('',#44055,1000.);
#10569=VECTOR('',#44056,10.);
#10570=VECTOR('',#44059,1000.);
#10571=VECTOR('',#44064,1000.);
#10572=VECTOR('',#44065,10.);
#10573=VECTOR('',#44070,1000.);
#10574=VECTOR('',#44077,1000.);
#10575=VECTOR('',#44088,1000.);
#10576=VECTOR('',#44091,1000.);
#10577=VECTOR('',#44098,1000.);
#10578=VECTOR('',#44107,1000.);
#10579=VECTOR('',#44110,10.);
#10580=VECTOR('',#44113,1000.);
#10581=VECTOR('',#44122,1000.);
#10582=VECTOR('',#44127,1000.);
#10583=VECTOR('',#44128,1000.);
#10584=VECTOR('',#44129,10.);
#10585=VECTOR('',#44132,1000.);
#10586=VECTOR('',#44145,1000.);
#10587=VECTOR('',#44154,1000.);
#10588=VECTOR('',#44157,10.);
#10589=VECTOR('',#44158,1000.);
#10590=VECTOR('',#44161,1000.);
#10591=VECTOR('',#44166,1000.);
#10592=VECTOR('',#44171,10.);
#10593=VECTOR('',#44172,1000.);
#10594=VECTOR('',#44175,1000.);
#10595=VECTOR('',#44190,1000.);
#10596=VECTOR('',#44201,1000.);
#10597=VECTOR('',#44204,1000.);
#10598=VECTOR('',#44209,1000.);
#10599=VECTOR('',#44220,1000.);
#10600=VECTOR('',#44223,10.);
#10601=VECTOR('',#44226,10.);
#10602=VECTOR('',#44227,1000.);
#10603=VECTOR('',#44228,1000.);
#10604=VECTOR('',#44231,1000.);
#10605=VECTOR('',#44232,1000.);
#10606=VECTOR('',#44233,10.);
#10607=VECTOR('',#44240,1000.);
#10608=VECTOR('',#44249,1000.);
#10609=VECTOR('',#44252,1000.);
#10610=VECTOR('',#44257,1000.);
#10611=VECTOR('',#44266,1000.);
#10612=VECTOR('',#44271,1000.);
#10613=VECTOR('',#44272,10.);
#10614=VECTOR('',#44279,1000.);
#10615=VECTOR('',#44282,1000.);
#10616=VECTOR('',#44285,10.);
#10617=VECTOR('',#44288,1000.);
#10618=VECTOR('',#44289,1000.);
#10619=VECTOR('',#44292,1000.);
#10620=VECTOR('',#44295,1000.);
#10621=VECTOR('',#44298,1000.);
#10622=VECTOR('',#44301,1000.);
#10623=VECTOR('',#44304,1000.);
#10624=VECTOR('',#44305,1000.);
#10625=VECTOR('',#44308,1000.);
#10626=VECTOR('',#44311,1000.);
#10627=VECTOR('',#44314,1000.);
#10628=VECTOR('',#44317,1000.);
#10629=VECTOR('',#44320,1000.);
#10630=VECTOR('',#44323,1000.);
#10631=VECTOR('',#44328,1000.);
#10632=VECTOR('',#44331,1000.);
#10633=VECTOR('',#44338,9.15);
#10634=VECTOR('',#44355,1000.);
#10635=VECTOR('',#44358,1000.);
#10636=VECTOR('',#44361,1000.);
#10637=VECTOR('',#44364,1000.);
#10638=VECTOR('',#44367,1000.);
#10639=VECTOR('',#44370,1000.);
#10640=VECTOR('',#44373,1000.);
#10641=VECTOR('',#44374,1000.);
#10642=VECTOR('',#44377,1000.);
#10643=VECTOR('',#44380,1000.);
#10644=VECTOR('',#44383,1000.);
#10645=VECTOR('',#44388,1000.);
#10646=VECTOR('',#44391,1000.);
#10647=VECTOR('',#44396,1000.);
#10648=VECTOR('',#44399,1000.);
#10649=VECTOR('',#44404,1000.);
#10650=VECTOR('',#44407,1000.);
#10651=VECTOR('',#44412,1000.);
#12403=CIRCLE('',#36370,11.2571565141535);
#12404=CIRCLE('',#36371,10.527435261753);
#12405=CIRCLE('',#36372,11.2571565141535);
#12406=CIRCLE('',#36373,11.2571565141535);
#12407=CIRCLE('',#36374,11.2571565141535);
#12408=CIRCLE('',#36376,17.4);
#12409=CIRCLE('',#36377,17.4);
#12410=CIRCLE('',#36378,16.4);
#12411=CIRCLE('',#36380,11.);
#12412=CIRCLE('',#36381,11.);
#12413=CIRCLE('',#36383,10.527435261753);
#12414=CIRCLE('',#36384,9.15);
#12415=CIRCLE('',#36386,17.4);
#12416=CIRCLE('',#36387,16.4);
#12417=CIRCLE('',#36391,17.4);
#12418=CIRCLE('',#36392,16.4);
#12419=CIRCLE('',#36394,17.4);
#12420=CIRCLE('',#36395,16.4);
#12421=CIRCLE('',#36399,17.4);
#12422=CIRCLE('',#36400,16.4);
#12423=CIRCLE('',#36402,16.4);
#12424=CIRCLE('',#36403,16.4);
#12425=CIRCLE('',#36404,16.4);
#12426=CIRCLE('',#36405,16.4);
#12427=CIRCLE('',#36406,16.4);
#12428=CIRCLE('',#36407,16.4);
#12429=CIRCLE('',#36408,16.4);
#12430=CIRCLE('',#36409,16.4);
#12431=CIRCLE('',#36410,16.4);
#12432=CIRCLE('',#36411,16.4000000000001);
#12433=CIRCLE('',#36412,16.4);
#12434=CIRCLE('',#36413,16.3999999999877);
#12435=CIRCLE('',#36414,16.4);
#12436=CIRCLE('',#36415,16.3999999999998);
#12437=CIRCLE('',#36416,16.4);
#12438=CIRCLE('',#36417,16.4);
#12439=CIRCLE('',#36418,16.4);
#12440=CIRCLE('',#36419,16.4);
#12441=CIRCLE('',#36420,16.4);
#12442=CIRCLE('',#36421,16.4);
#12443=CIRCLE('',#36423,17.4);
#12444=CIRCLE('',#36424,17.4);
#12445=CIRCLE('',#36425,17.4);
#12446=CIRCLE('',#36426,17.4);
#12447=CIRCLE('',#36427,17.4);
#12448=CIRCLE('',#36431,15.);
#12449=CIRCLE('',#36432,15.0000000000004);
#12450=CIRCLE('',#36434,2.);
#12451=CIRCLE('',#36435,2.);
#12452=CIRCLE('',#36437,13.4999999999999);
#12453=CIRCLE('',#36438,13.5);
#12454=CIRCLE('',#36440,0.500000000000003);
#12455=CIRCLE('',#36441,0.5);
#12456=CIRCLE('',#36443,0.5);
#12457=CIRCLE('',#36444,0.5);
#12458=CIRCLE('',#36447,0.5);
#12459=CIRCLE('',#36448,0.499999999999994);
#12460=CIRCLE('',#36452,0.100000000000004);
#12461=CIRCLE('',#36453,0.1);
#12462=CIRCLE('',#36456,0.5);
#12463=CIRCLE('',#36457,0.5);
#12464=CIRCLE('',#36458,0.2);
#12465=CIRCLE('',#36459,0.299999999999999);
#12466=CIRCLE('',#36460,0.3);
#12467=CIRCLE('',#36465,0.3);
#12468=CIRCLE('',#36468,0.0999999999999997);
#12469=CIRCLE('',#36469,0.1);
#12470=CIRCLE('',#36472,0.71602073105324);
#12471=CIRCLE('',#36473,0.30000057515613);
#12472=CIRCLE('',#36475,0.3);
#12473=CIRCLE('',#36478,0.300001459552508);
#12474=CIRCLE('',#36480,0.500000000000001);
#12475=CIRCLE('',#36487,15.4);
#12476=CIRCLE('',#36488,15.4);
#12477=CIRCLE('',#36490,0.1);
#12478=CIRCLE('',#36491,0.100000000000002);
#12479=CIRCLE('',#36494,0.5);
#12480=CIRCLE('',#36495,0.5);
#12481=CIRCLE('',#36496,0.3);
#12482=CIRCLE('',#36497,0.299999999999999);
#12483=CIRCLE('',#36498,0.2);
#12484=CIRCLE('',#36500,11.3);
#12485=CIRCLE('',#36501,12.5);
#12486=CIRCLE('',#36502,0.1);
#12487=CIRCLE('',#36507,0.3);
#12488=CIRCLE('',#36508,0.30000000000001);
#12489=CIRCLE('',#36511,0.0999999999999998);
#12490=CIRCLE('',#36513,12.5000000000001);
#12491=CIRCLE('',#36518,0.30000057515613);
#12492=CIRCLE('',#36521,0.3);
#12493=CIRCLE('',#36524,0.300001459552676);
#12494=CIRCLE('',#36526,0.499999999999989);
#12495=CIRCLE('',#36535,15.);
#12496=CIRCLE('',#36536,15.0000000000004);
#12497=CIRCLE('',#36538,2.);
#12498=CIRCLE('',#36539,2.);
#12499=CIRCLE('',#36541,13.4999999999999);
#12500=CIRCLE('',#36542,13.5);
#12501=CIRCLE('',#36544,0.500000000000003);
#12502=CIRCLE('',#36545,0.5);
#12503=CIRCLE('',#36547,0.5);
#12504=CIRCLE('',#36548,0.5);
#12505=CIRCLE('',#36551,0.5);
#12506=CIRCLE('',#36552,0.499999999999994);
#12507=CIRCLE('',#36572,9.15);
#12508=CIRCLE('',#36580,11.2571565141535);
#12509=CIRCLE('',#36581,11.2571565141535);
#12510=CIRCLE('',#36582,11.2571565141535);
#12511=CIRCLE('',#36583,11.2571565141535);
#12512=CIRCLE('',#36584,11.2571565141535);
#12513=CIRCLE('',#36585,11.2571565141535);
#12514=CIRCLE('',#36590,11.2571565141535);
#12515=CIRCLE('',#36593,11.2571565141535);
#12516=CIRCLE('',#36596,11.2571565141535);
#12517=CIRCLE('',#36599,11.2571565141535);
#15303=VERTEX_POINT('',#83310);
#15304=VERTEX_POINT('',#83311);
#15305=VERTEX_POINT('',#83313);
#15306=VERTEX_POINT('',#83318);
#15307=VERTEX_POINT('',#83320);
#15308=VERTEX_POINT('',#83325);
#15309=VERTEX_POINT('',#83327);
#15310=VERTEX_POINT('',#83358);
#15311=VERTEX_POINT('',#83360);
#15312=VERTEX_POINT('',#83395);
#15313=VERTEX_POINT('',#83428);
#15314=VERTEX_POINT('',#83429);
#15315=VERTEX_POINT('',#83432);
#15316=VERTEX_POINT('',#83436);
#15317=VERTEX_POINT('',#83437);
#15318=VERTEX_POINT('',#83439);
#15319=VERTEX_POINT('',#83441);
#15320=VERTEX_POINT('',#83452);
#15321=VERTEX_POINT('',#83454);
#15322=VERTEX_POINT('',#83456);
#15323=VERTEX_POINT('',#83458);
#15324=VERTEX_POINT('',#83472);
#15325=VERTEX_POINT('',#83475);
#15326=VERTEX_POINT('',#83476);
#15327=VERTEX_POINT('',#83478);
#15328=VERTEX_POINT('',#83480);
#15329=VERTEX_POINT('',#83484);
#15330=VERTEX_POINT('',#83486);
#15331=VERTEX_POINT('',#83490);
#15332=VERTEX_POINT('',#83491);
#15333=VERTEX_POINT('',#83499);
#15334=VERTEX_POINT('',#83500);
#15335=VERTEX_POINT('',#83502);
#15336=VERTEX_POINT('',#83504);
#15337=VERTEX_POINT('',#83508);
#15338=VERTEX_POINT('',#83510);
#15339=VERTEX_POINT('',#83514);
#15340=VERTEX_POINT('',#83516);
#15341=VERTEX_POINT('',#83523);
#15342=VERTEX_POINT('',#83524);
#15343=VERTEX_POINT('',#83526);
#15344=VERTEX_POINT('',#83528);
#15345=VERTEX_POINT('',#83530);
#15346=VERTEX_POINT('',#83532);
#15347=VERTEX_POINT('',#83534);
#15348=VERTEX_POINT('',#83536);
#15349=VERTEX_POINT('',#83538);
#15350=VERTEX_POINT('',#83540);
#15351=VERTEX_POINT('',#83542);
#15352=VERTEX_POINT('',#83544);
#15353=VERTEX_POINT('',#83546);
#15354=VERTEX_POINT('',#83548);
#15355=VERTEX_POINT('',#83559);
#15356=VERTEX_POINT('',#83561);
#15357=VERTEX_POINT('',#83572);
#15358=VERTEX_POINT('',#83574);
#15359=VERTEX_POINT('',#83576);
#15360=VERTEX_POINT('',#83578);
#15361=VERTEX_POINT('',#83589);
#15362=VERTEX_POINT('',#83591);
#15363=VERTEX_POINT('',#83602);
#15364=VERTEX_POINT('',#83604);
#15365=VERTEX_POINT('',#83606);
#15366=VERTEX_POINT('',#83608);
#15367=VERTEX_POINT('',#83619);
#15368=VERTEX_POINT('',#83621);
#15369=VERTEX_POINT('',#83632);
#15370=VERTEX_POINT('',#83634);
#15371=VERTEX_POINT('',#83636);
#15372=VERTEX_POINT('',#83638);
#15373=VERTEX_POINT('',#83640);
#15374=VERTEX_POINT('',#83642);
#15375=VERTEX_POINT('',#83644);
#15376=VERTEX_POINT('',#83646);
#15377=VERTEX_POINT('',#83648);
#15378=VERTEX_POINT('',#83651);
#15379=VERTEX_POINT('',#83653);
#15380=VERTEX_POINT('',#83664);
#15381=VERTEX_POINT('',#83666);
#15382=VERTEX_POINT('',#83677);
#15383=VERTEX_POINT('',#83679);
#15384=VERTEX_POINT('',#83690);
#15385=VERTEX_POINT('',#83692);
#15386=VERTEX_POINT('',#83703);
#15387=VERTEX_POINT('',#83705);
#15388=VERTEX_POINT('',#83716);
#15389=VERTEX_POINT('',#83718);
#15390=VERTEX_POINT('',#83729);
#15391=VERTEX_POINT('',#83731);
#15392=VERTEX_POINT('',#83742);
#15393=VERTEX_POINT('',#83755);
#15394=VERTEX_POINT('',#83757);
#15395=VERTEX_POINT('',#83759);
#15396=VERTEX_POINT('',#83770);
#15397=VERTEX_POINT('',#83772);
#15398=VERTEX_POINT('',#83783);
#15399=VERTEX_POINT('',#83785);
#15400=VERTEX_POINT('',#83796);
#15401=VERTEX_POINT('',#83798);
#15402=VERTEX_POINT('',#83809);
#15403=VERTEX_POINT('',#83811);
#15404=VERTEX_POINT('',#83822);
#15405=VERTEX_POINT('',#83824);
#15406=VERTEX_POINT('',#83835);
#15407=VERTEX_POINT('',#83837);
#15408=VERTEX_POINT('',#83848);
#15409=VERTEX_POINT('',#83850);
#15410=VERTEX_POINT('',#83863);
#15411=VERTEX_POINT('',#83865);
#15412=VERTEX_POINT('',#83869);
#15413=VERTEX_POINT('',#83871);
#15414=VERTEX_POINT('',#83875);
#15415=VERTEX_POINT('',#83877);
#15416=VERTEX_POINT('',#83884);
#15417=VERTEX_POINT('',#83885);
#15418=VERTEX_POINT('',#83887);
#15419=VERTEX_POINT('',#83889);
#15420=VERTEX_POINT('',#83893);
#15421=VERTEX_POINT('',#83894);
#15422=VERTEX_POINT('',#83899);
#15423=VERTEX_POINT('',#83901);
#15424=VERTEX_POINT('',#83908);
#15425=VERTEX_POINT('',#83910);
#15426=VERTEX_POINT('',#83918);
#15427=VERTEX_POINT('',#83919);
#15428=VERTEX_POINT('',#83921);
#15429=VERTEX_POINT('',#83923);
#15430=VERTEX_POINT('',#83927);
#15431=VERTEX_POINT('',#83929);
#15432=VERTEX_POINT('',#83933);
#15433=VERTEX_POINT('',#83935);
#15434=VERTEX_POINT('',#83963);
#15435=VERTEX_POINT('',#83964);
#15436=VERTEX_POINT('',#83972);
#15437=VERTEX_POINT('',#83974);
#15438=VERTEX_POINT('',#83976);
#15439=VERTEX_POINT('',#83980);
#15440=VERTEX_POINT('',#83987);
#15441=VERTEX_POINT('',#83994);
#15442=VERTEX_POINT('',#83996);
#15443=VERTEX_POINT('',#84053);
#15444=VERTEX_POINT('',#84130);
#15445=VERTEX_POINT('',#84134);
#15446=VERTEX_POINT('',#84136);
#15447=VERTEX_POINT('',#84178);
#15448=VERTEX_POINT('',#84242);
#15449=VERTEX_POINT('',#84276);
#15450=VERTEX_POINT('',#84333);
#15451=VERTEX_POINT('',#84414);
#15452=VERTEX_POINT('',#84422);
#15453=VERTEX_POINT('',#84423);
#15454=VERTEX_POINT('',#84428);
#15455=VERTEX_POINT('',#84430);
#15456=VERTEX_POINT('',#84434);
#15457=VERTEX_POINT('',#84436);
#15458=VERTEX_POINT('',#84440);
#15459=VERTEX_POINT('',#84441);
#15460=VERTEX_POINT('',#84470);
#15461=VERTEX_POINT('',#84472);
#15462=VERTEX_POINT('',#84478);
#15463=VERTEX_POINT('',#84484);
#15464=VERTEX_POINT('',#84486);
#15465=VERTEX_POINT('',#84488);
#15466=VERTEX_POINT('',#84492);
#15467=VERTEX_POINT('',#84494);
#15468=VERTEX_POINT('',#84501);
#15469=VERTEX_POINT('',#84561);
#15470=VERTEX_POINT('',#84584);
#15471=VERTEX_POINT('',#84588);
#15472=VERTEX_POINT('',#84589);
#15473=VERTEX_POINT('',#84669);
#15474=VERTEX_POINT('',#84733);
#15475=VERTEX_POINT('',#84764);
#15476=VERTEX_POINT('',#84821);
#15477=VERTEX_POINT('',#84902);
#15478=VERTEX_POINT('',#84910);
#15479=VERTEX_POINT('',#84912);
#15480=VERTEX_POINT('',#84916);
#15481=VERTEX_POINT('',#84918);
#15482=VERTEX_POINT('',#84922);
#15483=VERTEX_POINT('',#84924);
#15484=VERTEX_POINT('',#84931);
#15485=VERTEX_POINT('',#84932);
#15486=VERTEX_POINT('',#84934);
#15487=VERTEX_POINT('',#84936);
#15488=VERTEX_POINT('',#84940);
#15489=VERTEX_POINT('',#84941);
#15490=VERTEX_POINT('',#84946);
#15491=VERTEX_POINT('',#84948);
#15492=VERTEX_POINT('',#84955);
#15493=VERTEX_POINT('',#84957);
#15494=VERTEX_POINT('',#84997);
#15495=VERTEX_POINT('',#85007);
#15496=VERTEX_POINT('',#85008);
#15497=VERTEX_POINT('',#85010);
#15498=VERTEX_POINT('',#85012);
#15499=VERTEX_POINT('',#85014);
#15500=VERTEX_POINT('',#85016);
#15501=VERTEX_POINT('',#85018);
#15502=VERTEX_POINT('',#85020);
#15503=VERTEX_POINT('',#85022);
#15504=VERTEX_POINT('',#85024);
#15505=VERTEX_POINT('',#85026);
#15506=VERTEX_POINT('',#85028);
#15507=VERTEX_POINT('',#85039);
#15508=VERTEX_POINT('',#85043);
#15509=VERTEX_POINT('',#85076);
#15510=VERTEX_POINT('',#85080);
#15511=VERTEX_POINT('',#85117);
#15512=VERTEX_POINT('',#85121);
#19443=EDGE_CURVE('',#15303,#15304,#12403,.T.);
#19444=EDGE_CURVE('',#15304,#15305,#1830,.T.);
#19445=EDGE_CURVE('',#15306,#15305,#12404,.T.);
#19446=EDGE_CURVE('',#15307,#15306,#1831,.T.);
#19447=EDGE_CURVE('',#15307,#15308,#12405,.T.);
#19448=EDGE_CURVE('',#15309,#15308,#1832,.T.);
#19449=EDGE_CURVE('',#15310,#15309,#12406,.T.);
#19450=EDGE_CURVE('',#15311,#15310,#1833,.T.);
#19451=EDGE_CURVE('',#15311,#15312,#12407,.T.);
#19452=EDGE_CURVE('',#15303,#15312,#1834,.T.);
#19453=EDGE_CURVE('',#15313,#15314,#12408,.T.);
#19454=EDGE_CURVE('',#15314,#15313,#12409,.T.);
#19455=EDGE_CURVE('',#15314,#15315,#8658,.T.);
#19456=EDGE_CURVE('',#15315,#15315,#12410,.T.);
#19457=EDGE_CURVE('',#15316,#15317,#12411,.T.);
#19458=EDGE_CURVE('',#15317,#15318,#8659,.T.);
#19459=EDGE_CURVE('',#15318,#15319,#1835,.T.);
#19460=EDGE_CURVE('',#15319,#15320,#8660,.T.);
#19461=EDGE_CURVE('',#15320,#15321,#12412,.T.);
#19462=EDGE_CURVE('',#15322,#15321,#8661,.T.);
#19463=EDGE_CURVE('',#15323,#15322,#1836,.T.);
#19464=EDGE_CURVE('',#15316,#15323,#8662,.T.);
#19465=EDGE_CURVE('',#15305,#15306,#12413,.T.);
#19466=EDGE_CURVE('',#15324,#15324,#12414,.T.);
#19467=EDGE_CURVE('',#15325,#15326,#8663,.T.);
#19468=EDGE_CURVE('',#15327,#15326,#12415,.T.);
#19469=EDGE_CURVE('',#15328,#15327,#8664,.T.);
#19470=EDGE_CURVE('',#15328,#15325,#12416,.T.);
#19471=EDGE_CURVE('',#15329,#15328,#8665,.T.);
#19472=EDGE_CURVE('',#15330,#15327,#8666,.T.);
#19473=EDGE_CURVE('',#15329,#15330,#8667,.T.);
#19474=EDGE_CURVE('',#15331,#15332,#8668,.T.);
#19475=EDGE_CURVE('',#15332,#15326,#8669,.T.);
#19476=EDGE_CURVE('',#15331,#15325,#8670,.T.);
#19477=EDGE_CURVE('',#15332,#15330,#12417,.T.);
#19478=EDGE_CURVE('',#15331,#15329,#12418,.T.);
#19479=EDGE_CURVE('',#15333,#15334,#8671,.T.);
#19480=EDGE_CURVE('',#15335,#15333,#12419,.T.);
#19481=EDGE_CURVE('',#15335,#15336,#8672,.T.);
#19482=EDGE_CURVE('',#15336,#15334,#12420,.T.);
#19483=EDGE_CURVE('',#15337,#15335,#8673,.T.);
#19484=EDGE_CURVE('',#15337,#15338,#8674,.T.);
#19485=EDGE_CURVE('',#15338,#15336,#8675,.T.);
#19486=EDGE_CURVE('',#15339,#15334,#8676,.T.);
#19487=EDGE_CURVE('',#15340,#15339,#8677,.T.);
#19488=EDGE_CURVE('',#15340,#15333,#8678,.T.);
#19489=EDGE_CURVE('',#15340,#15337,#12421,.T.);
#19490=EDGE_CURVE('',#15339,#15338,#12422,.T.);
#19491=EDGE_CURVE('',#15341,#15342,#12423,.T.);
#19492=EDGE_CURVE('',#15342,#15343,#8679,.T.);
#19493=EDGE_CURVE('',#15343,#15344,#12424,.T.);
#19494=EDGE_CURVE('',#15344,#15345,#8680,.T.);
#19495=EDGE_CURVE('',#15346,#15345,#12425,.T.);
#19496=EDGE_CURVE('',#15347,#15346,#8681,.T.);
#19497=EDGE_CURVE('',#15347,#15348,#12426,.T.);
#19498=EDGE_CURVE('',#15348,#15349,#8682,.T.);
#19499=EDGE_CURVE('',#15350,#15349,#12427,.T.);
#19500=EDGE_CURVE('',#15351,#15350,#8683,.T.);
#19501=EDGE_CURVE('',#15351,#15352,#12428,.T.);
#19502=EDGE_CURVE('',#15352,#15353,#8684,.T.);
#19503=EDGE_CURVE('',#15354,#15353,#1837,.T.);
#19504=EDGE_CURVE('',#15355,#15354,#12429,.T.);
#19505=EDGE_CURVE('',#15356,#15355,#1838,.T.);
#19506=EDGE_CURVE('',#15357,#15356,#8685,.T.);
#19507=EDGE_CURVE('',#15357,#15358,#12430,.T.);
#19508=EDGE_CURVE('',#15358,#15359,#8686,.T.);
#19509=EDGE_CURVE('',#15360,#15359,#1839,.T.);
#19510=EDGE_CURVE('',#15360,#15361,#12431,.T.);
#19511=EDGE_CURVE('',#15361,#15362,#1840,.T.);
#19512=EDGE_CURVE('',#15363,#15362,#8687,.T.);
#19513=EDGE_CURVE('',#15363,#15364,#12432,.T.);
#19514=EDGE_CURVE('',#15364,#15365,#8688,.T.);
#19515=EDGE_CURVE('',#15365,#15366,#1841,.T.);
#19516=EDGE_CURVE('',#15366,#15367,#12433,.T.);
#19517=EDGE_CURVE('',#15367,#15368,#1842,.T.);
#19518=EDGE_CURVE('',#15369,#15368,#8689,.T.);
#19519=EDGE_CURVE('',#15369,#15370,#12434,.T.);
#19520=EDGE_CURVE('',#15370,#15371,#8690,.T.);
#19521=EDGE_CURVE('',#15372,#15371,#12435,.T.);
#19522=EDGE_CURVE('',#15373,#15372,#8691,.T.);
#19523=EDGE_CURVE('',#15373,#15374,#12436,.T.);
#19524=EDGE_CURVE('',#15374,#15375,#8692,.T.);
#19525=EDGE_CURVE('',#15376,#15375,#12437,.T.);
#19526=EDGE_CURVE('',#15377,#15376,#8693,.T.);
#19527=EDGE_CURVE('',#15377,#15343,#12438,.T.);
#19528=EDGE_CURVE('',#15342,#15378,#12439,.T.);
#19529=EDGE_CURVE('',#15379,#15378,#1843,.T.);
#19530=EDGE_CURVE('',#15379,#15380,#8694,.T.);
#19531=EDGE_CURVE('',#15380,#15381,#1844,.T.);
#19532=EDGE_CURVE('',#15381,#15382,#12440,.T.);
#19533=EDGE_CURVE('',#15382,#15383,#1845,.T.);
#19534=EDGE_CURVE('',#15384,#15383,#8695,.T.);
#19535=EDGE_CURVE('',#15385,#15384,#1846,.T.);
#19536=EDGE_CURVE('',#15385,#15386,#12441,.T.);
#19537=EDGE_CURVE('',#15387,#15386,#1847,.T.);
#19538=EDGE_CURVE('',#15387,#15388,#8696,.T.);
#19539=EDGE_CURVE('',#15388,#15389,#1848,.T.);
#19540=EDGE_CURVE('',#15390,#15389,#12442,.T.);
#19541=EDGE_CURVE('',#15390,#15391,#1849,.T.);
#19542=EDGE_CURVE('',#15392,#15391,#8697,.T.);
#19543=EDGE_CURVE('',#15341,#15392,#1850,.T.);
#19544=EDGE_CURVE('',#15313,#15393,#8698,.T.);
#19545=EDGE_CURVE('',#15394,#15393,#12443,.T.);
#19546=EDGE_CURVE('',#15395,#15394,#1851,.T.);
#19547=EDGE_CURVE('',#15395,#15396,#8699,.T.);
#19548=EDGE_CURVE('',#15396,#15397,#1852,.T.);
#19549=EDGE_CURVE('',#15397,#15398,#12444,.T.);
#19550=EDGE_CURVE('',#15398,#15399,#1853,.T.);
#19551=EDGE_CURVE('',#15400,#15399,#8700,.T.);
#19552=EDGE_CURVE('',#15401,#15400,#1854,.T.);
#19553=EDGE_CURVE('',#15401,#15402,#12445,.T.);
#19554=EDGE_CURVE('',#15403,#15402,#1855,.T.);
#19555=EDGE_CURVE('',#15403,#15404,#8701,.T.);
#19556=EDGE_CURVE('',#15404,#15405,#1856,.T.);
#19557=EDGE_CURVE('',#15406,#15405,#12446,.T.);
#19558=EDGE_CURVE('',#15406,#15407,#1857,.T.);
#19559=EDGE_CURVE('',#15408,#15407,#8702,.T.);
#19560=EDGE_CURVE('',#15409,#15408,#1858,.T.);
#19561=EDGE_CURVE('',#15393,#15409,#12447,.T.);
#19562=EDGE_CURVE('',#15410,#15374,#8703,.T.);
#19563=EDGE_CURVE('',#15410,#15411,#8704,.T.);
#19564=EDGE_CURVE('',#15411,#15375,#8705,.T.);
#19565=EDGE_CURVE('',#15412,#15372,#8706,.T.);
#19566=EDGE_CURVE('',#15412,#15413,#8707,.T.);
#19567=EDGE_CURVE('',#15413,#15373,#8708,.T.);
#19568=EDGE_CURVE('',#15411,#15414,#12448,.T.);
#19569=EDGE_CURVE('',#15410,#15415,#12449,.T.);
#19570=EDGE_CURVE('',#15414,#15415,#8709,.T.);
#19571=EDGE_CURVE('',#15415,#15413,#12450,.T.);
#19572=EDGE_CURVE('',#15414,#15412,#12451,.T.);
#19573=EDGE_CURVE('',#15416,#15417,#8710,.T.);
#19574=EDGE_CURVE('',#15417,#15418,#12452,.T.);
#19575=EDGE_CURVE('',#15418,#15419,#8711,.T.);
#19576=EDGE_CURVE('',#15416,#15419,#12453,.T.);
#19577=EDGE_CURVE('',#15420,#15421,#8712,.T.);
#19578=EDGE_CURVE('',#15417,#15420,#12454,.T.);
#19579=EDGE_CURVE('',#15421,#15416,#12455,.T.);
#19580=EDGE_CURVE('',#15421,#15422,#12456,.T.);
#19581=EDGE_CURVE('',#15423,#15422,#8713,.T.);
#19582=EDGE_CURVE('',#15423,#15420,#12457,.T.);
#19583=EDGE_CURVE('',#15371,#15422,#8714,.T.);
#19584=EDGE_CURVE('',#15370,#15423,#8715,.T.);
#19585=EDGE_CURVE('',#15424,#15419,#12458,.T.);
#19586=EDGE_CURVE('',#15418,#15425,#12459,.T.);
#19587=EDGE_CURVE('',#15425,#15424,#8716,.T.);
#19588=EDGE_CURVE('',#15424,#15376,#8717,.T.);
#19589=EDGE_CURVE('',#15425,#15377,#8718,.T.);
#19590=EDGE_CURVE('',#15426,#15427,#12460,.T.);
#19591=EDGE_CURVE('',#15428,#15427,#8719,.T.);
#19592=EDGE_CURVE('',#15428,#15429,#12461,.T.);
#19593=EDGE_CURVE('',#15429,#15426,#8720,.T.);
#19594=EDGE_CURVE('',#15427,#15430,#8721,.T.);
#19595=EDGE_CURVE('',#15431,#15430,#8722,.T.);
#19596=EDGE_CURVE('',#15431,#15428,#8723,.T.);
#19597=EDGE_CURVE('',#15432,#15320,#12462,.T.);
#19598=EDGE_CURVE('',#15433,#15319,#12463,.T.);
#19599=EDGE_CURVE('',#15433,#15432,#8724,.T.);
#19600=EDGE_CURVE('',#15434,#15435,#12464,.T.);
#19601=EDGE_CURVE('',#15435,#15320,#12465,.T.);
#19602=EDGE_CURVE('',#15434,#15432,#12466,.T.);
#19603=EDGE_CURVE('',#15361,#15434,#8725,.T.);
#19604=EDGE_CURVE('',#15362,#15432,#8726,.T.);
#19605=EDGE_CURVE('',#15436,#15433,#8727,.T.);
#19606=EDGE_CURVE('',#15437,#15436,#624,.T.);
#19607=EDGE_CURVE('',#15438,#15437,#8728,.T.);
#19608=EDGE_CURVE('',#15363,#15438,#8729,.T.);
#19609=EDGE_CURVE('',#15439,#15437,#1859,.T.);
#19610=EDGE_CURVE('',#15440,#15439,#8730,.T.);
#19611=EDGE_CURVE('',#15440,#15438,#12467,.T.);
#19612=EDGE_CURVE('',#15439,#15365,#8731,.T.);
#19613=EDGE_CURVE('',#15440,#15364,#8732,.T.);
#19614=EDGE_CURVE('',#15430,#15441,#12468,.T.);
#19615=EDGE_CURVE('',#15442,#15441,#8733,.T.);
#19616=EDGE_CURVE('',#15442,#15431,#12469,.T.);
#19617=EDGE_CURVE('',#15443,#15436,#625,.T.);
#19618=EDGE_CURVE('',#15439,#15443,#1860,.T.);
#19619=EDGE_CURVE('',#15443,#15366,#8734,.T.);
#19620=EDGE_CURVE('',#15444,#15319,#12470,.T.);
#19621=EDGE_CURVE('',#15444,#15318,#12471,.T.);
#19622=EDGE_CURVE('',#15445,#15433,#12472,.T.);
#19623=EDGE_CURVE('',#15446,#15444,#1861,.T.);
#19624=EDGE_CURVE('',#15445,#15446,#1862,.T.);
#19625=EDGE_CURVE('',#15443,#15447,#8735,.T.);
#19626=EDGE_CURVE('',#15447,#15445,#1863,.T.);
#19627=EDGE_CURVE('',#15367,#15447,#8736,.T.);
#19628=EDGE_CURVE('',#15448,#15318,#1864,.T.);
#19629=EDGE_CURVE('',#15446,#15448,#12473,.T.);
#19630=EDGE_CURVE('',#15449,#15317,#12474,.T.);
#19631=EDGE_CURVE('',#15448,#15449,#8737,.T.);
#19632=EDGE_CURVE('',#15450,#15448,#1865,.T.);
#19633=EDGE_CURVE('',#15445,#15450,#626,.T.);
#19634=EDGE_CURVE('',#15451,#15450,#627,.T.);
#19635=EDGE_CURVE('',#15447,#15451,#628,.T.);
#19636=EDGE_CURVE('',#15368,#15451,#8738,.T.);
#19637=EDGE_CURVE('',#15369,#15449,#8739,.T.);
#19638=EDGE_CURVE('',#15452,#15453,#8740,.T.);
#19639=EDGE_CURVE('',#15426,#15453,#12475,.F.);
#19640=EDGE_CURVE('',#15429,#15452,#12476,.T.);
#19641=EDGE_CURVE('',#15454,#15452,#12477,.T.);
#19642=EDGE_CURVE('',#15454,#15455,#8741,.T.);
#19643=EDGE_CURVE('',#15453,#15455,#12478,.T.);
#19644=EDGE_CURVE('',#15456,#15454,#8742,.T.);
#19645=EDGE_CURVE('',#15456,#15457,#8743,.T.);
#19646=EDGE_CURVE('',#15455,#15457,#8744,.T.);
#19647=EDGE_CURVE('',#15458,#15459,#8745,.T.);
#19648=EDGE_CURVE('',#15458,#15322,#12479,.T.);
#19649=EDGE_CURVE('',#15459,#15321,#12480,.T.);
#19650=EDGE_CURVE('',#15460,#15459,#12481,.T.);
#19651=EDGE_CURVE('',#15461,#15321,#12482,.T.);
#19652=EDGE_CURVE('',#15460,#15461,#12483,.T.);
#19653=EDGE_CURVE('',#15360,#15460,#8746,.T.);
#19654=EDGE_CURVE('',#15461,#15435,#12484,.T.);
#19655=EDGE_CURVE('',#15442,#15462,#12485,.T.);
#19656=EDGE_CURVE('',#15462,#15456,#12486,.T.);
#19657=EDGE_CURVE('',#15359,#15459,#8747,.T.);
#19658=EDGE_CURVE('',#15358,#15463,#8748,.T.);
#19659=EDGE_CURVE('',#15463,#15464,#8749,.T.);
#19660=EDGE_CURVE('',#15464,#15465,#629,.T.);
#19661=EDGE_CURVE('',#15465,#15458,#8750,.T.);
#19662=EDGE_CURVE('',#15466,#15463,#12487,.T.);
#19663=EDGE_CURVE('',#15466,#15467,#8751,.T.);
#19664=EDGE_CURVE('',#15467,#15464,#12488,.T.);
#19665=EDGE_CURVE('',#15466,#15357,#8752,.T.);
#19666=EDGE_CURVE('',#15467,#15356,#8753,.T.);
#19667=EDGE_CURVE('',#15462,#15468,#8754,.T.);
#19668=EDGE_CURVE('',#15457,#15468,#12489,.T.);
#19669=EDGE_CURVE('',#15468,#15441,#12490,.T.);
#19670=EDGE_CURVE('',#15467,#15469,#630,.T.);
#19671=EDGE_CURVE('',#15469,#15465,#631,.T.);
#19672=EDGE_CURVE('',#15469,#15355,#8755,.T.);
#19673=EDGE_CURVE('',#15470,#15323,#12491,.T.);
#19674=EDGE_CURVE('',#15470,#15322,#632,.T.);
#19675=EDGE_CURVE('',#15471,#15472,#1866,.T.);
#19676=EDGE_CURVE('',#15472,#15470,#1867,.T.);
#19677=EDGE_CURVE('',#15471,#15458,#12492,.T.);
#19678=EDGE_CURVE('',#15473,#15471,#1868,.T.);
#19679=EDGE_CURVE('',#15469,#15473,#8756,.T.);
#19680=EDGE_CURVE('',#15354,#15473,#8757,.T.);
#19681=EDGE_CURVE('',#15472,#15474,#12493,.T.);
#19682=EDGE_CURVE('',#15474,#15323,#1869,.T.);
#19683=EDGE_CURVE('',#15474,#15475,#8758,.T.);
#19684=EDGE_CURVE('',#15475,#15316,#12494,.T.);
#19685=EDGE_CURVE('',#15471,#15476,#633,.T.);
#19686=EDGE_CURVE('',#15476,#15474,#1870,.T.);
#19687=EDGE_CURVE('',#15473,#15477,#634,.T.);
#19688=EDGE_CURVE('',#15477,#15476,#635,.T.);
#19689=EDGE_CURVE('',#15353,#15477,#8759,.T.);
#19690=EDGE_CURVE('',#15352,#15475,#8760,.T.);
#19691=EDGE_CURVE('',#15478,#15348,#8761,.T.);
#19692=EDGE_CURVE('',#15478,#15479,#8762,.T.);
#19693=EDGE_CURVE('',#15479,#15349,#8763,.T.);
#19694=EDGE_CURVE('',#15480,#15346,#8764,.T.);
#19695=EDGE_CURVE('',#15480,#15481,#8765,.T.);
#19696=EDGE_CURVE('',#15481,#15347,#8766,.T.);
#19697=EDGE_CURVE('',#15479,#15482,#12495,.T.);
#19698=EDGE_CURVE('',#15478,#15483,#12496,.T.);
#19699=EDGE_CURVE('',#15482,#15483,#8767,.T.);
#19700=EDGE_CURVE('',#15483,#15481,#12497,.T.);
#19701=EDGE_CURVE('',#15482,#15480,#12498,.T.);
#19702=EDGE_CURVE('',#15484,#15485,#8768,.T.);
#19703=EDGE_CURVE('',#15485,#15486,#12499,.T.);
#19704=EDGE_CURVE('',#15486,#15487,#8769,.T.);
#19705=EDGE_CURVE('',#15484,#15487,#12500,.T.);
#19706=EDGE_CURVE('',#15488,#15489,#8770,.T.);
#19707=EDGE_CURVE('',#15485,#15488,#12501,.T.);
#19708=EDGE_CURVE('',#15489,#15484,#12502,.T.);
#19709=EDGE_CURVE('',#15489,#15490,#12503,.T.);
#19710=EDGE_CURVE('',#15491,#15490,#8771,.T.);
#19711=EDGE_CURVE('',#15491,#15488,#12504,.T.);
#19712=EDGE_CURVE('',#15345,#15490,#8772,.T.);
#19713=EDGE_CURVE('',#15344,#15491,#8773,.T.);
#19714=EDGE_CURVE('',#15492,#15487,#12505,.T.);
#19715=EDGE_CURVE('',#15486,#15493,#12506,.T.);
#19716=EDGE_CURVE('',#15493,#15492,#8774,.T.);
#19717=EDGE_CURVE('',#15492,#15350,#8775,.T.);
#19718=EDGE_CURVE('',#15493,#15351,#8776,.T.);
#19719=EDGE_CURVE('',#15404,#15383,#8777,.T.);
#19720=EDGE_CURVE('',#15384,#15403,#8778,.T.);
#19721=EDGE_CURVE('',#15405,#15382,#8779,.T.);
#19722=EDGE_CURVE('',#15406,#15381,#8780,.T.);
#19723=EDGE_CURVE('',#15407,#15380,#8781,.T.);
#19724=EDGE_CURVE('',#15379,#15408,#8782,.T.);
#19725=EDGE_CURVE('',#15388,#15399,#8783,.T.);
#19726=EDGE_CURVE('',#15400,#15387,#8784,.T.);
#19727=EDGE_CURVE('',#15389,#15398,#8785,.T.);
#19728=EDGE_CURVE('',#15390,#15397,#8786,.T.);
#19729=EDGE_CURVE('',#15391,#15396,#8787,.T.);
#19730=EDGE_CURVE('',#15395,#15392,#8788,.T.);
#19731=EDGE_CURVE('',#15378,#15409,#8789,.T.);
#19732=EDGE_CURVE('',#15394,#15341,#8790,.T.);
#19733=EDGE_CURVE('',#15385,#15402,#8791,.T.);
#19734=EDGE_CURVE('',#15401,#15386,#8792,.T.);
#19735=EDGE_CURVE('',#15494,#15494,#12507,.T.);
#19736=EDGE_CURVE('',#15494,#15324,#8793,.T.);
#19737=EDGE_CURVE('',#15495,#15496,#12508,.T.);
#19738=EDGE_CURVE('',#15497,#15495,#8794,.T.);
#19739=EDGE_CURVE('',#15498,#15497,#12509,.T.);
#19740=EDGE_CURVE('',#15499,#15498,#8795,.T.);
#19741=EDGE_CURVE('',#15500,#15499,#12510,.T.);
#19742=EDGE_CURVE('',#15501,#15500,#8796,.T.);
#19743=EDGE_CURVE('',#15502,#15501,#12511,.T.);
#19744=EDGE_CURVE('',#15503,#15502,#8797,.T.);
#19745=EDGE_CURVE('',#15504,#15503,#12512,.T.);
#19746=EDGE_CURVE('',#15505,#15504,#8798,.T.);
#19747=EDGE_CURVE('',#15506,#15505,#12513,.T.);
#19748=EDGE_CURVE('',#15496,#15506,#8799,.T.);
#19749=EDGE_CURVE('',#15311,#15495,#8800,.T.);
#19750=EDGE_CURVE('',#15310,#15497,#8801,.T.);
#19751=EDGE_CURVE('',#15312,#15496,#8802,.T.);
#19752=EDGE_CURVE('',#15303,#15506,#8803,.T.);
#19753=EDGE_CURVE('',#15507,#15505,#8804,.T.);
#19754=EDGE_CURVE('',#15304,#15507,#12514,.T.);
#19755=EDGE_CURVE('',#15508,#15504,#8805,.T.);
#19756=EDGE_CURVE('',#15508,#15507,#1871,.T.);
#19757=EDGE_CURVE('',#15509,#15503,#8806,.T.);
#19758=EDGE_CURVE('',#15508,#15509,#12515,.T.);
#19759=EDGE_CURVE('',#15510,#15502,#8807,.T.);
#19760=EDGE_CURVE('',#15510,#15509,#1872,.T.);
#19761=EDGE_CURVE('',#15511,#15501,#8808,.T.);
#19762=EDGE_CURVE('',#15510,#15511,#12516,.T.);
#19763=EDGE_CURVE('',#15512,#15500,#8809,.T.);
#19764=EDGE_CURVE('',#15512,#15511,#1873,.T.);
#19765=EDGE_CURVE('',#15308,#15499,#8810,.T.);
#19766=EDGE_CURVE('',#15512,#15307,#12517,.T.);
#19767=EDGE_CURVE('',#15309,#15498,#8811,.T.);
#27343=ORIENTED_EDGE('',*,*,#19443,.T.);
#27344=ORIENTED_EDGE('',*,*,#19444,.T.);
#27345=ORIENTED_EDGE('',*,*,#19445,.F.);
#27346=ORIENTED_EDGE('',*,*,#19446,.F.);
#27347=ORIENTED_EDGE('',*,*,#19447,.T.);
#27348=ORIENTED_EDGE('',*,*,#19448,.F.);
#27349=ORIENTED_EDGE('',*,*,#19449,.F.);
#27350=ORIENTED_EDGE('',*,*,#19450,.F.);
#27351=ORIENTED_EDGE('',*,*,#19451,.T.);
#27352=ORIENTED_EDGE('',*,*,#19452,.F.);
#27353=ORIENTED_EDGE('',*,*,#19453,.F.);
#27354=ORIENTED_EDGE('',*,*,#19454,.F.);
#27355=ORIENTED_EDGE('',*,*,#19455,.T.);
#27356=ORIENTED_EDGE('',*,*,#19456,.F.);
#27357=ORIENTED_EDGE('',*,*,#19455,.F.);
#27358=ORIENTED_EDGE('',*,*,#19457,.T.);
#27359=ORIENTED_EDGE('',*,*,#19458,.T.);
#27360=ORIENTED_EDGE('',*,*,#19459,.T.);
#27361=ORIENTED_EDGE('',*,*,#19460,.T.);
#27362=ORIENTED_EDGE('',*,*,#19461,.T.);
#27363=ORIENTED_EDGE('',*,*,#19462,.F.);
#27364=ORIENTED_EDGE('',*,*,#19463,.F.);
#27365=ORIENTED_EDGE('',*,*,#19464,.F.);
#27366=ORIENTED_EDGE('',*,*,#19445,.T.);
#27367=ORIENTED_EDGE('',*,*,#19465,.T.);
#27368=ORIENTED_EDGE('',*,*,#19466,.T.);
#27369=ORIENTED_EDGE('',*,*,#19467,.T.);
#27370=ORIENTED_EDGE('',*,*,#19468,.F.);
#27371=ORIENTED_EDGE('',*,*,#19469,.F.);
#27372=ORIENTED_EDGE('',*,*,#19470,.T.);
#27373=ORIENTED_EDGE('',*,*,#19471,.T.);
#27374=ORIENTED_EDGE('',*,*,#19469,.T.);
#27375=ORIENTED_EDGE('',*,*,#19472,.F.);
#27376=ORIENTED_EDGE('',*,*,#19473,.F.);
#27377=ORIENTED_EDGE('',*,*,#19474,.T.);
#27378=ORIENTED_EDGE('',*,*,#19475,.T.);
#27379=ORIENTED_EDGE('',*,*,#19467,.F.);
#27380=ORIENTED_EDGE('',*,*,#19476,.F.);
#27381=ORIENTED_EDGE('',*,*,#19473,.T.);
#27382=ORIENTED_EDGE('',*,*,#19477,.F.);
#27383=ORIENTED_EDGE('',*,*,#19474,.F.);
#27384=ORIENTED_EDGE('',*,*,#19478,.T.);
#27385=ORIENTED_EDGE('',*,*,#19479,.F.);
#27386=ORIENTED_EDGE('',*,*,#19480,.F.);
#27387=ORIENTED_EDGE('',*,*,#19481,.T.);
#27388=ORIENTED_EDGE('',*,*,#19482,.T.);
#27389=ORIENTED_EDGE('',*,*,#19481,.F.);
#27390=ORIENTED_EDGE('',*,*,#19483,.F.);
#27391=ORIENTED_EDGE('',*,*,#19484,.T.);
#27392=ORIENTED_EDGE('',*,*,#19485,.T.);
#27393=ORIENTED_EDGE('',*,*,#19486,.F.);
#27394=ORIENTED_EDGE('',*,*,#19487,.F.);
#27395=ORIENTED_EDGE('',*,*,#19488,.T.);
#27396=ORIENTED_EDGE('',*,*,#19479,.T.);
#27397=ORIENTED_EDGE('',*,*,#19484,.F.);
#27398=ORIENTED_EDGE('',*,*,#19489,.F.);
#27399=ORIENTED_EDGE('',*,*,#19487,.T.);
#27400=ORIENTED_EDGE('',*,*,#19490,.T.);
#27401=ORIENTED_EDGE('',*,*,#19491,.T.);
#27402=ORIENTED_EDGE('',*,*,#19492,.T.);
#27403=ORIENTED_EDGE('',*,*,#19493,.T.);
#27404=ORIENTED_EDGE('',*,*,#19494,.T.);
#27405=ORIENTED_EDGE('',*,*,#19495,.F.);
#27406=ORIENTED_EDGE('',*,*,#19496,.F.);
#27407=ORIENTED_EDGE('',*,*,#19497,.T.);
#27408=ORIENTED_EDGE('',*,*,#19498,.T.);
#27409=ORIENTED_EDGE('',*,*,#19499,.F.);
#27410=ORIENTED_EDGE('',*,*,#19500,.F.);
#27411=ORIENTED_EDGE('',*,*,#19501,.T.);
#27412=ORIENTED_EDGE('',*,*,#19502,.T.);
#27413=ORIENTED_EDGE('',*,*,#19503,.F.);
#27414=ORIENTED_EDGE('',*,*,#19504,.F.);
#27415=ORIENTED_EDGE('',*,*,#19505,.F.);
#27416=ORIENTED_EDGE('',*,*,#19506,.F.);
#27417=ORIENTED_EDGE('',*,*,#19507,.T.);
#27418=ORIENTED_EDGE('',*,*,#19508,.T.);
#27419=ORIENTED_EDGE('',*,*,#19509,.F.);
#27420=ORIENTED_EDGE('',*,*,#19510,.T.);
#27421=ORIENTED_EDGE('',*,*,#19511,.T.);
#27422=ORIENTED_EDGE('',*,*,#19512,.F.);
#27423=ORIENTED_EDGE('',*,*,#19513,.T.);
#27424=ORIENTED_EDGE('',*,*,#19514,.T.);
#27425=ORIENTED_EDGE('',*,*,#19515,.T.);
#27426=ORIENTED_EDGE('',*,*,#19516,.T.);
#27427=ORIENTED_EDGE('',*,*,#19517,.T.);
#27428=ORIENTED_EDGE('',*,*,#19518,.F.);
#27429=ORIENTED_EDGE('',*,*,#19519,.T.);
#27430=ORIENTED_EDGE('',*,*,#19520,.T.);
#27431=ORIENTED_EDGE('',*,*,#19521,.F.);
#27432=ORIENTED_EDGE('',*,*,#19522,.F.);
#27433=ORIENTED_EDGE('',*,*,#19523,.T.);
#27434=ORIENTED_EDGE('',*,*,#19524,.T.);
#27435=ORIENTED_EDGE('',*,*,#19525,.F.);
#27436=ORIENTED_EDGE('',*,*,#19526,.F.);
#27437=ORIENTED_EDGE('',*,*,#19527,.T.);
#27438=ORIENTED_EDGE('',*,*,#19492,.F.);
#27439=ORIENTED_EDGE('',*,*,#19528,.T.);
#27440=ORIENTED_EDGE('',*,*,#19529,.F.);
#27441=ORIENTED_EDGE('',*,*,#19530,.T.);
#27442=ORIENTED_EDGE('',*,*,#19531,.T.);
#27443=ORIENTED_EDGE('',*,*,#19532,.T.);
#27444=ORIENTED_EDGE('',*,*,#19533,.T.);
#27445=ORIENTED_EDGE('',*,*,#19534,.F.);
#27446=ORIENTED_EDGE('',*,*,#19535,.F.);
#27447=ORIENTED_EDGE('',*,*,#19536,.T.);
#27448=ORIENTED_EDGE('',*,*,#19537,.F.);
#27449=ORIENTED_EDGE('',*,*,#19538,.T.);
#27450=ORIENTED_EDGE('',*,*,#19539,.T.);
#27451=ORIENTED_EDGE('',*,*,#19540,.F.);
#27452=ORIENTED_EDGE('',*,*,#19541,.T.);
#27453=ORIENTED_EDGE('',*,*,#19542,.F.);
#27454=ORIENTED_EDGE('',*,*,#19543,.F.);
#27455=ORIENTED_EDGE('',*,*,#19490,.F.);
#27456=ORIENTED_EDGE('',*,*,#19486,.T.);
#27457=ORIENTED_EDGE('',*,*,#19482,.F.);
#27458=ORIENTED_EDGE('',*,*,#19485,.F.);
#27459=ORIENTED_EDGE('',*,*,#19476,.T.);
#27460=ORIENTED_EDGE('',*,*,#19470,.F.);
#27461=ORIENTED_EDGE('',*,*,#19471,.F.);
#27462=ORIENTED_EDGE('',*,*,#19478,.F.);
#27463=ORIENTED_EDGE('',*,*,#19453,.T.);
#27464=ORIENTED_EDGE('',*,*,#19454,.T.);
#27465=ORIENTED_EDGE('',*,*,#19544,.T.);
#27466=ORIENTED_EDGE('',*,*,#19545,.F.);
#27467=ORIENTED_EDGE('',*,*,#19546,.F.);
#27468=ORIENTED_EDGE('',*,*,#19547,.T.);
#27469=ORIENTED_EDGE('',*,*,#19548,.T.);
#27470=ORIENTED_EDGE('',*,*,#19549,.T.);
#27471=ORIENTED_EDGE('',*,*,#19550,.T.);
#27472=ORIENTED_EDGE('',*,*,#19551,.F.);
#27473=ORIENTED_EDGE('',*,*,#19552,.F.);
#27474=ORIENTED_EDGE('',*,*,#19553,.T.);
#27475=ORIENTED_EDGE('',*,*,#19554,.F.);
#27476=ORIENTED_EDGE('',*,*,#19555,.T.);
#27477=ORIENTED_EDGE('',*,*,#19556,.T.);
#27478=ORIENTED_EDGE('',*,*,#19557,.F.);
#27479=ORIENTED_EDGE('',*,*,#19558,.T.);
#27480=ORIENTED_EDGE('',*,*,#19559,.F.);
#27481=ORIENTED_EDGE('',*,*,#19560,.F.);
#27482=ORIENTED_EDGE('',*,*,#19561,.F.);
#27483=ORIENTED_EDGE('',*,*,#19544,.F.);
#27484=ORIENTED_EDGE('',*,*,#19477,.T.);
#27485=ORIENTED_EDGE('',*,*,#19472,.T.);
#27486=ORIENTED_EDGE('',*,*,#19468,.T.);
#27487=ORIENTED_EDGE('',*,*,#19475,.F.);
#27488=ORIENTED_EDGE('',*,*,#19483,.T.);
#27489=ORIENTED_EDGE('',*,*,#19480,.T.);
#27490=ORIENTED_EDGE('',*,*,#19488,.F.);
#27491=ORIENTED_EDGE('',*,*,#19489,.T.);
#27492=ORIENTED_EDGE('',*,*,#19524,.F.);
#27493=ORIENTED_EDGE('',*,*,#19562,.F.);
#27494=ORIENTED_EDGE('',*,*,#19563,.T.);
#27495=ORIENTED_EDGE('',*,*,#19564,.T.);
#27496=ORIENTED_EDGE('',*,*,#19565,.F.);
#27497=ORIENTED_EDGE('',*,*,#19566,.T.);
#27498=ORIENTED_EDGE('',*,*,#19567,.T.);
#27499=ORIENTED_EDGE('',*,*,#19522,.T.);
#27500=ORIENTED_EDGE('',*,*,#19568,.F.);
#27501=ORIENTED_EDGE('',*,*,#19563,.F.);
#27502=ORIENTED_EDGE('',*,*,#19569,.T.);
#27503=ORIENTED_EDGE('',*,*,#19570,.F.);
#27504=ORIENTED_EDGE('',*,*,#19570,.T.);
#27505=ORIENTED_EDGE('',*,*,#19571,.T.);
#27506=ORIENTED_EDGE('',*,*,#19566,.F.);
#27507=ORIENTED_EDGE('',*,*,#19572,.F.);
#27508=ORIENTED_EDGE('',*,*,#19573,.T.);
#27509=ORIENTED_EDGE('',*,*,#19574,.T.);
#27510=ORIENTED_EDGE('',*,*,#19575,.T.);
#27511=ORIENTED_EDGE('',*,*,#19576,.F.);
#27512=ORIENTED_EDGE('',*,*,#19577,.F.);
#27513=ORIENTED_EDGE('',*,*,#19578,.F.);
#27514=ORIENTED_EDGE('',*,*,#19573,.F.);
#27515=ORIENTED_EDGE('',*,*,#19579,.F.);
#27516=ORIENTED_EDGE('',*,*,#19580,.T.);
#27517=ORIENTED_EDGE('',*,*,#19581,.F.);
#27518=ORIENTED_EDGE('',*,*,#19582,.T.);
#27519=ORIENTED_EDGE('',*,*,#19577,.T.);
#27520=ORIENTED_EDGE('',*,*,#19581,.T.);
#27521=ORIENTED_EDGE('',*,*,#19583,.F.);
#27522=ORIENTED_EDGE('',*,*,#19520,.F.);
#27523=ORIENTED_EDGE('',*,*,#19584,.T.);
#27524=ORIENTED_EDGE('',*,*,#19585,.T.);
#27525=ORIENTED_EDGE('',*,*,#19575,.F.);
#27526=ORIENTED_EDGE('',*,*,#19586,.T.);
#27527=ORIENTED_EDGE('',*,*,#19587,.T.);
#27528=ORIENTED_EDGE('',*,*,#19521,.T.);
#27529=ORIENTED_EDGE('',*,*,#19583,.T.);
#27530=ORIENTED_EDGE('',*,*,#19580,.F.);
#27531=ORIENTED_EDGE('',*,*,#19579,.T.);
#27532=ORIENTED_EDGE('',*,*,#19576,.T.);
#27533=ORIENTED_EDGE('',*,*,#19585,.F.);
#27534=ORIENTED_EDGE('',*,*,#19588,.T.);
#27535=ORIENTED_EDGE('',*,*,#19525,.T.);
#27536=ORIENTED_EDGE('',*,*,#19564,.F.);
#27537=ORIENTED_EDGE('',*,*,#19568,.T.);
#27538=ORIENTED_EDGE('',*,*,#19572,.T.);
#27539=ORIENTED_EDGE('',*,*,#19565,.T.);
#27540=ORIENTED_EDGE('',*,*,#19589,.T.);
#27541=ORIENTED_EDGE('',*,*,#19526,.T.);
#27542=ORIENTED_EDGE('',*,*,#19588,.F.);
#27543=ORIENTED_EDGE('',*,*,#19587,.F.);
#27544=ORIENTED_EDGE('',*,*,#19590,.T.);
#27545=ORIENTED_EDGE('',*,*,#19591,.F.);
#27546=ORIENTED_EDGE('',*,*,#19592,.T.);
#27547=ORIENTED_EDGE('',*,*,#19593,.T.);
#27548=ORIENTED_EDGE('',*,*,#19591,.T.);
#27549=ORIENTED_EDGE('',*,*,#19594,.T.);
#27550=ORIENTED_EDGE('',*,*,#19595,.F.);
#27551=ORIENTED_EDGE('',*,*,#19596,.T.);
#27552=ORIENTED_EDGE('',*,*,#19597,.T.);
#27553=ORIENTED_EDGE('',*,*,#19460,.F.);
#27554=ORIENTED_EDGE('',*,*,#19598,.F.);
#27555=ORIENTED_EDGE('',*,*,#19599,.T.);
#27556=ORIENTED_EDGE('',*,*,#19600,.T.);
#27557=ORIENTED_EDGE('',*,*,#19601,.T.);
#27558=ORIENTED_EDGE('',*,*,#19597,.F.);
#27559=ORIENTED_EDGE('',*,*,#19602,.F.);
#27560=ORIENTED_EDGE('',*,*,#19511,.F.);
#27561=ORIENTED_EDGE('',*,*,#19603,.T.);
#27562=ORIENTED_EDGE('',*,*,#19602,.T.);
#27563=ORIENTED_EDGE('',*,*,#19604,.F.);
#27564=ORIENTED_EDGE('',*,*,#19599,.F.);
#27565=ORIENTED_EDGE('',*,*,#19605,.F.);
#27566=ORIENTED_EDGE('',*,*,#19606,.F.);
#27567=ORIENTED_EDGE('',*,*,#19607,.F.);
#27568=ORIENTED_EDGE('',*,*,#19608,.F.);
#27569=ORIENTED_EDGE('',*,*,#19512,.T.);
#27570=ORIENTED_EDGE('',*,*,#19604,.T.);
#27571=ORIENTED_EDGE('',*,*,#19607,.T.);
#27572=ORIENTED_EDGE('',*,*,#19609,.F.);
#27573=ORIENTED_EDGE('',*,*,#19610,.F.);
#27574=ORIENTED_EDGE('',*,*,#19611,.T.);
#27575=ORIENTED_EDGE('',*,*,#19610,.T.);
#27576=ORIENTED_EDGE('',*,*,#19612,.T.);
#27577=ORIENTED_EDGE('',*,*,#19514,.F.);
#27578=ORIENTED_EDGE('',*,*,#19613,.F.);
#27579=ORIENTED_EDGE('',*,*,#19614,.T.);
#27580=ORIENTED_EDGE('',*,*,#19615,.F.);
#27581=ORIENTED_EDGE('',*,*,#19616,.T.);
#27582=ORIENTED_EDGE('',*,*,#19595,.T.);
#27583=ORIENTED_EDGE('',*,*,#19609,.T.);
#27584=ORIENTED_EDGE('',*,*,#19606,.T.);
#27585=ORIENTED_EDGE('',*,*,#19617,.F.);
#27586=ORIENTED_EDGE('',*,*,#19618,.F.);
#27587=ORIENTED_EDGE('',*,*,#19618,.T.);
#27588=ORIENTED_EDGE('',*,*,#19619,.T.);
#27589=ORIENTED_EDGE('',*,*,#19515,.F.);
#27590=ORIENTED_EDGE('',*,*,#19612,.F.);
#27591=ORIENTED_EDGE('',*,*,#19620,.T.);
#27592=ORIENTED_EDGE('',*,*,#19459,.F.);
#27593=ORIENTED_EDGE('',*,*,#19621,.F.);
#27594=ORIENTED_EDGE('',*,*,#19622,.T.);
#27595=ORIENTED_EDGE('',*,*,#19598,.T.);
#27596=ORIENTED_EDGE('',*,*,#19620,.F.);
#27597=ORIENTED_EDGE('',*,*,#19623,.F.);
#27598=ORIENTED_EDGE('',*,*,#19624,.F.);
#27599=ORIENTED_EDGE('',*,*,#19625,.F.);
#27600=ORIENTED_EDGE('',*,*,#19617,.T.);
#27601=ORIENTED_EDGE('',*,*,#19605,.T.);
#27602=ORIENTED_EDGE('',*,*,#19622,.F.);
#27603=ORIENTED_EDGE('',*,*,#19626,.F.);
#27604=ORIENTED_EDGE('',*,*,#19627,.F.);
#27605=ORIENTED_EDGE('',*,*,#19516,.F.);
#27606=ORIENTED_EDGE('',*,*,#19619,.F.);
#27607=ORIENTED_EDGE('',*,*,#19625,.T.);
#27608=ORIENTED_EDGE('',*,*,#19623,.T.);
#27609=ORIENTED_EDGE('',*,*,#19621,.T.);
#27610=ORIENTED_EDGE('',*,*,#19628,.F.);
#27611=ORIENTED_EDGE('',*,*,#19629,.F.);
#27612=ORIENTED_EDGE('',*,*,#19628,.T.);
#27613=ORIENTED_EDGE('',*,*,#19458,.F.);
#27614=ORIENTED_EDGE('',*,*,#19630,.F.);
#27615=ORIENTED_EDGE('',*,*,#19631,.F.);
#27616=ORIENTED_EDGE('',*,*,#19624,.T.);
#27617=ORIENTED_EDGE('',*,*,#19629,.T.);
#27618=ORIENTED_EDGE('',*,*,#19632,.F.);
#27619=ORIENTED_EDGE('',*,*,#19633,.F.);
#27620=ORIENTED_EDGE('',*,*,#19626,.T.);
#27621=ORIENTED_EDGE('',*,*,#19633,.T.);
#27622=ORIENTED_EDGE('',*,*,#19634,.F.);
#27623=ORIENTED_EDGE('',*,*,#19635,.F.);
#27624=ORIENTED_EDGE('',*,*,#19517,.F.);
#27625=ORIENTED_EDGE('',*,*,#19627,.T.);
#27626=ORIENTED_EDGE('',*,*,#19635,.T.);
#27627=ORIENTED_EDGE('',*,*,#19636,.F.);
#27628=ORIENTED_EDGE('',*,*,#19631,.T.);
#27629=ORIENTED_EDGE('',*,*,#19637,.F.);
#27630=ORIENTED_EDGE('',*,*,#19518,.T.);
#27631=ORIENTED_EDGE('',*,*,#19636,.T.);
#27632=ORIENTED_EDGE('',*,*,#19634,.T.);
#27633=ORIENTED_EDGE('',*,*,#19632,.T.);
#27634=ORIENTED_EDGE('',*,*,#19638,.T.);
#27635=ORIENTED_EDGE('',*,*,#19639,.F.);
#27636=ORIENTED_EDGE('',*,*,#19593,.F.);
#27637=ORIENTED_EDGE('',*,*,#19640,.T.);
#27638=ORIENTED_EDGE('',*,*,#19638,.F.);
#27639=ORIENTED_EDGE('',*,*,#19641,.F.);
#27640=ORIENTED_EDGE('',*,*,#19642,.T.);
#27641=ORIENTED_EDGE('',*,*,#19643,.F.);
#27642=ORIENTED_EDGE('',*,*,#19644,.F.);
#27643=ORIENTED_EDGE('',*,*,#19645,.T.);
#27644=ORIENTED_EDGE('',*,*,#19646,.F.);
#27645=ORIENTED_EDGE('',*,*,#19642,.F.);
#27646=ORIENTED_EDGE('',*,*,#19647,.F.);
#27647=ORIENTED_EDGE('',*,*,#19648,.T.);
#27648=ORIENTED_EDGE('',*,*,#19462,.T.);
#27649=ORIENTED_EDGE('',*,*,#19649,.F.);
#27650=ORIENTED_EDGE('',*,*,#19650,.T.);
#27651=ORIENTED_EDGE('',*,*,#19649,.T.);
#27652=ORIENTED_EDGE('',*,*,#19651,.F.);
#27653=ORIENTED_EDGE('',*,*,#19652,.F.);
#27654=ORIENTED_EDGE('',*,*,#19603,.F.);
#27655=ORIENTED_EDGE('',*,*,#19510,.F.);
#27656=ORIENTED_EDGE('',*,*,#19653,.T.);
#27657=ORIENTED_EDGE('',*,*,#19652,.T.);
#27658=ORIENTED_EDGE('',*,*,#19654,.T.);
#27659=ORIENTED_EDGE('',*,*,#19600,.F.);
#27660=ORIENTED_EDGE('',*,*,#19641,.T.);
#27661=ORIENTED_EDGE('',*,*,#19640,.F.);
#27662=ORIENTED_EDGE('',*,*,#19592,.F.);
#27663=ORIENTED_EDGE('',*,*,#19596,.F.);
#27664=ORIENTED_EDGE('',*,*,#19616,.F.);
#27665=ORIENTED_EDGE('',*,*,#19655,.T.);
#27666=ORIENTED_EDGE('',*,*,#19656,.T.);
#27667=ORIENTED_EDGE('',*,*,#19644,.T.);
#27668=ORIENTED_EDGE('',*,*,#19657,.T.);
#27669=ORIENTED_EDGE('',*,*,#19650,.F.);
#27670=ORIENTED_EDGE('',*,*,#19653,.F.);
#27671=ORIENTED_EDGE('',*,*,#19509,.T.);
#27672=ORIENTED_EDGE('',*,*,#19657,.F.);
#27673=ORIENTED_EDGE('',*,*,#19508,.F.);
#27674=ORIENTED_EDGE('',*,*,#19658,.T.);
#27675=ORIENTED_EDGE('',*,*,#19659,.T.);
#27676=ORIENTED_EDGE('',*,*,#19660,.T.);
#27677=ORIENTED_EDGE('',*,*,#19661,.T.);
#27678=ORIENTED_EDGE('',*,*,#19647,.T.);
#27679=ORIENTED_EDGE('',*,*,#19662,.F.);
#27680=ORIENTED_EDGE('',*,*,#19663,.T.);
#27681=ORIENTED_EDGE('',*,*,#19664,.T.);
#27682=ORIENTED_EDGE('',*,*,#19659,.F.);
#27683=ORIENTED_EDGE('',*,*,#19665,.T.);
#27684=ORIENTED_EDGE('',*,*,#19506,.T.);
#27685=ORIENTED_EDGE('',*,*,#19666,.F.);
#27686=ORIENTED_EDGE('',*,*,#19663,.F.);
#27687=ORIENTED_EDGE('',*,*,#19645,.F.);
#27688=ORIENTED_EDGE('',*,*,#19656,.F.);
#27689=ORIENTED_EDGE('',*,*,#19667,.T.);
#27690=ORIENTED_EDGE('',*,*,#19668,.F.);
#27691=ORIENTED_EDGE('',*,*,#19655,.F.);
#27692=ORIENTED_EDGE('',*,*,#19615,.T.);
#27693=ORIENTED_EDGE('',*,*,#19669,.F.);
#27694=ORIENTED_EDGE('',*,*,#19667,.F.);
#27695=ORIENTED_EDGE('',*,*,#19654,.F.);
#27696=ORIENTED_EDGE('',*,*,#19651,.T.);
#27697=ORIENTED_EDGE('',*,*,#19461,.F.);
#27698=ORIENTED_EDGE('',*,*,#19601,.F.);
#27699=ORIENTED_EDGE('',*,*,#19670,.T.);
#27700=ORIENTED_EDGE('',*,*,#19671,.T.);
#27701=ORIENTED_EDGE('',*,*,#19660,.F.);
#27702=ORIENTED_EDGE('',*,*,#19664,.F.);
#27703=ORIENTED_EDGE('',*,*,#19666,.T.);
#27704=ORIENTED_EDGE('',*,*,#19505,.T.);
#27705=ORIENTED_EDGE('',*,*,#19672,.F.);
#27706=ORIENTED_EDGE('',*,*,#19670,.F.);
#27707=ORIENTED_EDGE('',*,*,#19673,.T.);
#27708=ORIENTED_EDGE('',*,*,#19463,.T.);
#27709=ORIENTED_EDGE('',*,*,#19674,.F.);
#27710=ORIENTED_EDGE('',*,*,#19675,.T.);
#27711=ORIENTED_EDGE('',*,*,#19676,.T.);
#27712=ORIENTED_EDGE('',*,*,#19674,.T.);
#27713=ORIENTED_EDGE('',*,*,#19648,.F.);
#27714=ORIENTED_EDGE('',*,*,#19677,.F.);
#27715=ORIENTED_EDGE('',*,*,#19678,.T.);
#27716=ORIENTED_EDGE('',*,*,#19677,.T.);
#27717=ORIENTED_EDGE('',*,*,#19661,.F.);
#27718=ORIENTED_EDGE('',*,*,#19671,.F.);
#27719=ORIENTED_EDGE('',*,*,#19679,.T.);
#27720=ORIENTED_EDGE('',*,*,#19679,.F.);
#27721=ORIENTED_EDGE('',*,*,#19672,.T.);
#27722=ORIENTED_EDGE('',*,*,#19504,.T.);
#27723=ORIENTED_EDGE('',*,*,#19680,.T.);
#27724=ORIENTED_EDGE('',*,*,#19681,.T.);
#27725=ORIENTED_EDGE('',*,*,#19682,.T.);
#27726=ORIENTED_EDGE('',*,*,#19673,.F.);
#27727=ORIENTED_EDGE('',*,*,#19676,.F.);
#27728=ORIENTED_EDGE('',*,*,#19683,.T.);
#27729=ORIENTED_EDGE('',*,*,#19684,.T.);
#27730=ORIENTED_EDGE('',*,*,#19464,.T.);
#27731=ORIENTED_EDGE('',*,*,#19682,.F.);
#27732=ORIENTED_EDGE('',*,*,#19685,.T.);
#27733=ORIENTED_EDGE('',*,*,#19686,.T.);
#27734=ORIENTED_EDGE('',*,*,#19681,.F.);
#27735=ORIENTED_EDGE('',*,*,#19675,.F.);
#27736=ORIENTED_EDGE('',*,*,#19687,.T.);
#27737=ORIENTED_EDGE('',*,*,#19688,.T.);
#27738=ORIENTED_EDGE('',*,*,#19685,.F.);
#27739=ORIENTED_EDGE('',*,*,#19678,.F.);
#27740=ORIENTED_EDGE('',*,*,#19689,.T.);
#27741=ORIENTED_EDGE('',*,*,#19687,.F.);
#27742=ORIENTED_EDGE('',*,*,#19680,.F.);
#27743=ORIENTED_EDGE('',*,*,#19503,.T.);
#27744=ORIENTED_EDGE('',*,*,#19686,.F.);
#27745=ORIENTED_EDGE('',*,*,#19688,.F.);
#27746=ORIENTED_EDGE('',*,*,#19689,.F.);
#27747=ORIENTED_EDGE('',*,*,#19502,.F.);
#27748=ORIENTED_EDGE('',*,*,#19690,.T.);
#27749=ORIENTED_EDGE('',*,*,#19683,.F.);
#27750=ORIENTED_EDGE('',*,*,#19498,.F.);
#27751=ORIENTED_EDGE('',*,*,#19691,.F.);
#27752=ORIENTED_EDGE('',*,*,#19692,.T.);
#27753=ORIENTED_EDGE('',*,*,#19693,.T.);
#27754=ORIENTED_EDGE('',*,*,#19694,.F.);
#27755=ORIENTED_EDGE('',*,*,#19695,.T.);
#27756=ORIENTED_EDGE('',*,*,#19696,.T.);
#27757=ORIENTED_EDGE('',*,*,#19496,.T.);
#27758=ORIENTED_EDGE('',*,*,#19697,.F.);
#27759=ORIENTED_EDGE('',*,*,#19692,.F.);
#27760=ORIENTED_EDGE('',*,*,#19698,.T.);
#27761=ORIENTED_EDGE('',*,*,#19699,.F.);
#27762=ORIENTED_EDGE('',*,*,#19699,.T.);
#27763=ORIENTED_EDGE('',*,*,#19700,.T.);
#27764=ORIENTED_EDGE('',*,*,#19695,.F.);
#27765=ORIENTED_EDGE('',*,*,#19701,.F.);
#27766=ORIENTED_EDGE('',*,*,#19702,.T.);
#27767=ORIENTED_EDGE('',*,*,#19703,.T.);
#27768=ORIENTED_EDGE('',*,*,#19704,.T.);
#27769=ORIENTED_EDGE('',*,*,#19705,.F.);
#27770=ORIENTED_EDGE('',*,*,#19706,.F.);
#27771=ORIENTED_EDGE('',*,*,#19707,.F.);
#27772=ORIENTED_EDGE('',*,*,#19702,.F.);
#27773=ORIENTED_EDGE('',*,*,#19708,.F.);
#27774=ORIENTED_EDGE('',*,*,#19709,.T.);
#27775=ORIENTED_EDGE('',*,*,#19710,.F.);
#27776=ORIENTED_EDGE('',*,*,#19711,.T.);
#27777=ORIENTED_EDGE('',*,*,#19706,.T.);
#27778=ORIENTED_EDGE('',*,*,#19710,.T.);
#27779=ORIENTED_EDGE('',*,*,#19712,.F.);
#27780=ORIENTED_EDGE('',*,*,#19494,.F.);
#27781=ORIENTED_EDGE('',*,*,#19713,.T.);
#27782=ORIENTED_EDGE('',*,*,#19714,.T.);
#27783=ORIENTED_EDGE('',*,*,#19704,.F.);
#27784=ORIENTED_EDGE('',*,*,#19715,.T.);
#27785=ORIENTED_EDGE('',*,*,#19716,.T.);
#27786=ORIENTED_EDGE('',*,*,#19495,.T.);
#27787=ORIENTED_EDGE('',*,*,#19712,.T.);
#27788=ORIENTED_EDGE('',*,*,#19709,.F.);
#27789=ORIENTED_EDGE('',*,*,#19708,.T.);
#27790=ORIENTED_EDGE('',*,*,#19705,.T.);
#27791=ORIENTED_EDGE('',*,*,#19714,.F.);
#27792=ORIENTED_EDGE('',*,*,#19717,.T.);
#27793=ORIENTED_EDGE('',*,*,#19499,.T.);
#27794=ORIENTED_EDGE('',*,*,#19693,.F.);
#27795=ORIENTED_EDGE('',*,*,#19697,.T.);
#27796=ORIENTED_EDGE('',*,*,#19701,.T.);
#27797=ORIENTED_EDGE('',*,*,#19694,.T.);
#27798=ORIENTED_EDGE('',*,*,#19718,.T.);
#27799=ORIENTED_EDGE('',*,*,#19500,.T.);
#27800=ORIENTED_EDGE('',*,*,#19717,.F.);
#27801=ORIENTED_EDGE('',*,*,#19716,.F.);
#27802=ORIENTED_EDGE('',*,*,#19534,.T.);
#27803=ORIENTED_EDGE('',*,*,#19719,.F.);
#27804=ORIENTED_EDGE('',*,*,#19555,.F.);
#27805=ORIENTED_EDGE('',*,*,#19720,.F.);
#27806=ORIENTED_EDGE('',*,*,#19721,.F.);
#27807=ORIENTED_EDGE('',*,*,#19556,.F.);
#27808=ORIENTED_EDGE('',*,*,#19719,.T.);
#27809=ORIENTED_EDGE('',*,*,#19533,.F.);
#27810=ORIENTED_EDGE('',*,*,#19532,.F.);
#27811=ORIENTED_EDGE('',*,*,#19722,.F.);
#27812=ORIENTED_EDGE('',*,*,#19557,.T.);
#27813=ORIENTED_EDGE('',*,*,#19721,.T.);
#27814=ORIENTED_EDGE('',*,*,#19723,.F.);
#27815=ORIENTED_EDGE('',*,*,#19558,.F.);
#27816=ORIENTED_EDGE('',*,*,#19722,.T.);
#27817=ORIENTED_EDGE('',*,*,#19531,.F.);
#27818=ORIENTED_EDGE('',*,*,#19724,.T.);
#27819=ORIENTED_EDGE('',*,*,#19559,.T.);
#27820=ORIENTED_EDGE('',*,*,#19723,.T.);
#27821=ORIENTED_EDGE('',*,*,#19530,.F.);
#27822=ORIENTED_EDGE('',*,*,#19551,.T.);
#27823=ORIENTED_EDGE('',*,*,#19725,.F.);
#27824=ORIENTED_EDGE('',*,*,#19538,.F.);
#27825=ORIENTED_EDGE('',*,*,#19726,.F.);
#27826=ORIENTED_EDGE('',*,*,#19727,.F.);
#27827=ORIENTED_EDGE('',*,*,#19539,.F.);
#27828=ORIENTED_EDGE('',*,*,#19725,.T.);
#27829=ORIENTED_EDGE('',*,*,#19550,.F.);
#27830=ORIENTED_EDGE('',*,*,#19540,.T.);
#27831=ORIENTED_EDGE('',*,*,#19727,.T.);
#27832=ORIENTED_EDGE('',*,*,#19549,.F.);
#27833=ORIENTED_EDGE('',*,*,#19728,.F.);
#27834=ORIENTED_EDGE('',*,*,#19729,.F.);
#27835=ORIENTED_EDGE('',*,*,#19541,.F.);
#27836=ORIENTED_EDGE('',*,*,#19728,.T.);
#27837=ORIENTED_EDGE('',*,*,#19548,.F.);
#27838=ORIENTED_EDGE('',*,*,#19730,.T.);
#27839=ORIENTED_EDGE('',*,*,#19542,.T.);
#27840=ORIENTED_EDGE('',*,*,#19729,.T.);
#27841=ORIENTED_EDGE('',*,*,#19547,.F.);
#27842=ORIENTED_EDGE('',*,*,#19560,.T.);
#27843=ORIENTED_EDGE('',*,*,#19724,.F.);
#27844=ORIENTED_EDGE('',*,*,#19529,.T.);
#27845=ORIENTED_EDGE('',*,*,#19731,.T.);
#27846=ORIENTED_EDGE('',*,*,#19543,.T.);
#27847=ORIENTED_EDGE('',*,*,#19730,.F.);
#27848=ORIENTED_EDGE('',*,*,#19546,.T.);
#27849=ORIENTED_EDGE('',*,*,#19732,.T.);
#27850=ORIENTED_EDGE('',*,*,#19732,.F.);
#27851=ORIENTED_EDGE('',*,*,#19545,.T.);
#27852=ORIENTED_EDGE('',*,*,#19561,.T.);
#27853=ORIENTED_EDGE('',*,*,#19731,.F.);
#27854=ORIENTED_EDGE('',*,*,#19528,.F.);
#27855=ORIENTED_EDGE('',*,*,#19491,.F.);
#27856=ORIENTED_EDGE('',*,*,#19554,.T.);
#27857=ORIENTED_EDGE('',*,*,#19733,.F.);
#27858=ORIENTED_EDGE('',*,*,#19535,.T.);
#27859=ORIENTED_EDGE('',*,*,#19720,.T.);
#27860=ORIENTED_EDGE('',*,*,#19537,.T.);
#27861=ORIENTED_EDGE('',*,*,#19734,.F.);
#27862=ORIENTED_EDGE('',*,*,#19552,.T.);
#27863=ORIENTED_EDGE('',*,*,#19726,.T.);
#27864=ORIENTED_EDGE('',*,*,#19734,.T.);
#27865=ORIENTED_EDGE('',*,*,#19536,.F.);
#27866=ORIENTED_EDGE('',*,*,#19733,.T.);
#27867=ORIENTED_EDGE('',*,*,#19553,.F.);
#27868=ORIENTED_EDGE('',*,*,#19735,.F.);
#27869=ORIENTED_EDGE('',*,*,#19736,.T.);
#27870=ORIENTED_EDGE('',*,*,#19466,.F.);
#27871=ORIENTED_EDGE('',*,*,#19736,.F.);
#27872=ORIENTED_EDGE('',*,*,#19608,.T.);
#27873=ORIENTED_EDGE('',*,*,#19611,.F.);
#27874=ORIENTED_EDGE('',*,*,#19613,.T.);
#27875=ORIENTED_EDGE('',*,*,#19513,.F.);
#27876=ORIENTED_EDGE('',*,*,#19669,.T.);
#27877=ORIENTED_EDGE('',*,*,#19614,.F.);
#27878=ORIENTED_EDGE('',*,*,#19594,.F.);
#27879=ORIENTED_EDGE('',*,*,#19590,.F.);
#27880=ORIENTED_EDGE('',*,*,#19639,.T.);
#27881=ORIENTED_EDGE('',*,*,#19643,.T.);
#27882=ORIENTED_EDGE('',*,*,#19646,.T.);
#27883=ORIENTED_EDGE('',*,*,#19668,.T.);
#27884=ORIENTED_EDGE('',*,*,#19665,.F.);
#27885=ORIENTED_EDGE('',*,*,#19662,.T.);
#27886=ORIENTED_EDGE('',*,*,#19658,.F.);
#27887=ORIENTED_EDGE('',*,*,#19507,.F.);
#27888=ORIENTED_EDGE('',*,*,#19567,.F.);
#27889=ORIENTED_EDGE('',*,*,#19571,.F.);
#27890=ORIENTED_EDGE('',*,*,#19569,.F.);
#27891=ORIENTED_EDGE('',*,*,#19562,.T.);
#27892=ORIENTED_EDGE('',*,*,#19523,.F.);
#27893=ORIENTED_EDGE('',*,*,#19589,.F.);
#27894=ORIENTED_EDGE('',*,*,#19586,.F.);
#27895=ORIENTED_EDGE('',*,*,#19574,.F.);
#27896=ORIENTED_EDGE('',*,*,#19578,.T.);
#27897=ORIENTED_EDGE('',*,*,#19582,.F.);
#27898=ORIENTED_EDGE('',*,*,#19584,.F.);
#27899=ORIENTED_EDGE('',*,*,#19519,.F.);
#27900=ORIENTED_EDGE('',*,*,#19637,.T.);
#27901=ORIENTED_EDGE('',*,*,#19630,.T.);
#27902=ORIENTED_EDGE('',*,*,#19457,.F.);
#27903=ORIENTED_EDGE('',*,*,#19684,.F.);
#27904=ORIENTED_EDGE('',*,*,#19690,.F.);
#27905=ORIENTED_EDGE('',*,*,#19501,.F.);
#27906=ORIENTED_EDGE('',*,*,#19718,.F.);
#27907=ORIENTED_EDGE('',*,*,#19715,.F.);
#27908=ORIENTED_EDGE('',*,*,#19703,.F.);
#27909=ORIENTED_EDGE('',*,*,#19707,.T.);
#27910=ORIENTED_EDGE('',*,*,#19711,.F.);
#27911=ORIENTED_EDGE('',*,*,#19713,.F.);
#27912=ORIENTED_EDGE('',*,*,#19493,.F.);
#27913=ORIENTED_EDGE('',*,*,#19527,.F.);
#27914=ORIENTED_EDGE('',*,*,#19735,.T.);
#27915=ORIENTED_EDGE('',*,*,#19696,.F.);
#27916=ORIENTED_EDGE('',*,*,#19700,.F.);
#27917=ORIENTED_EDGE('',*,*,#19698,.F.);
#27918=ORIENTED_EDGE('',*,*,#19691,.T.);
#27919=ORIENTED_EDGE('',*,*,#19497,.F.);
#27920=ORIENTED_EDGE('',*,*,#19456,.T.);
#27921=ORIENTED_EDGE('',*,*,#19737,.F.);
#27922=ORIENTED_EDGE('',*,*,#19738,.F.);
#27923=ORIENTED_EDGE('',*,*,#19739,.F.);
#27924=ORIENTED_EDGE('',*,*,#19740,.F.);
#27925=ORIENTED_EDGE('',*,*,#19741,.F.);
#27926=ORIENTED_EDGE('',*,*,#19742,.F.);
#27927=ORIENTED_EDGE('',*,*,#19743,.F.);
#27928=ORIENTED_EDGE('',*,*,#19744,.F.);
#27929=ORIENTED_EDGE('',*,*,#19745,.F.);
#27930=ORIENTED_EDGE('',*,*,#19746,.F.);
#27931=ORIENTED_EDGE('',*,*,#19747,.F.);
#27932=ORIENTED_EDGE('',*,*,#19748,.F.);
#27933=ORIENTED_EDGE('',*,*,#19749,.F.);
#27934=ORIENTED_EDGE('',*,*,#19450,.T.);
#27935=ORIENTED_EDGE('',*,*,#19750,.T.);
#27936=ORIENTED_EDGE('',*,*,#19738,.T.);
#27937=ORIENTED_EDGE('',*,*,#19751,.F.);
#27938=ORIENTED_EDGE('',*,*,#19451,.F.);
#27939=ORIENTED_EDGE('',*,*,#19749,.T.);
#27940=ORIENTED_EDGE('',*,*,#19737,.T.);
#27941=ORIENTED_EDGE('',*,*,#19752,.F.);
#27942=ORIENTED_EDGE('',*,*,#19452,.T.);
#27943=ORIENTED_EDGE('',*,*,#19751,.T.);
#27944=ORIENTED_EDGE('',*,*,#19748,.T.);
#27945=ORIENTED_EDGE('',*,*,#19753,.F.);
#27946=ORIENTED_EDGE('',*,*,#19754,.F.);
#27947=ORIENTED_EDGE('',*,*,#19443,.F.);
#27948=ORIENTED_EDGE('',*,*,#19752,.T.);
#27949=ORIENTED_EDGE('',*,*,#19747,.T.);
#27950=ORIENTED_EDGE('',*,*,#19755,.F.);
#27951=ORIENTED_EDGE('',*,*,#19756,.T.);
#27952=ORIENTED_EDGE('',*,*,#19753,.T.);
#27953=ORIENTED_EDGE('',*,*,#19746,.T.);
#27954=ORIENTED_EDGE('',*,*,#19757,.F.);
#27955=ORIENTED_EDGE('',*,*,#19758,.F.);
#27956=ORIENTED_EDGE('',*,*,#19755,.T.);
#27957=ORIENTED_EDGE('',*,*,#19745,.T.);
#27958=ORIENTED_EDGE('',*,*,#19759,.F.);
#27959=ORIENTED_EDGE('',*,*,#19760,.T.);
#27960=ORIENTED_EDGE('',*,*,#19757,.T.);
#27961=ORIENTED_EDGE('',*,*,#19744,.T.);
#27962=ORIENTED_EDGE('',*,*,#19761,.F.);
#27963=ORIENTED_EDGE('',*,*,#19762,.F.);
#27964=ORIENTED_EDGE('',*,*,#19759,.T.);
#27965=ORIENTED_EDGE('',*,*,#19743,.T.);
#27966=ORIENTED_EDGE('',*,*,#19763,.F.);
#27967=ORIENTED_EDGE('',*,*,#19764,.T.);
#27968=ORIENTED_EDGE('',*,*,#19761,.T.);
#27969=ORIENTED_EDGE('',*,*,#19742,.T.);
#27970=ORIENTED_EDGE('',*,*,#19765,.F.);
#27971=ORIENTED_EDGE('',*,*,#19447,.F.);
#27972=ORIENTED_EDGE('',*,*,#19766,.F.);
#27973=ORIENTED_EDGE('',*,*,#19763,.T.);
#27974=ORIENTED_EDGE('',*,*,#19741,.T.);
#27975=ORIENTED_EDGE('',*,*,#19767,.F.);
#27976=ORIENTED_EDGE('',*,*,#19448,.T.);
#27977=ORIENTED_EDGE('',*,*,#19765,.T.);
#27978=ORIENTED_EDGE('',*,*,#19740,.T.);
#27979=ORIENTED_EDGE('',*,*,#19750,.F.);
#27980=ORIENTED_EDGE('',*,*,#19449,.T.);
#27981=ORIENTED_EDGE('',*,*,#19767,.T.);
#27982=ORIENTED_EDGE('',*,*,#19739,.T.);
#27983=ORIENTED_EDGE('',*,*,#19444,.F.);
#27984=ORIENTED_EDGE('',*,*,#19754,.T.);
#27985=ORIENTED_EDGE('',*,*,#19756,.F.);
#27986=ORIENTED_EDGE('',*,*,#19758,.T.);
#27987=ORIENTED_EDGE('',*,*,#19760,.F.);
#27988=ORIENTED_EDGE('',*,*,#19762,.T.);
#27989=ORIENTED_EDGE('',*,*,#19764,.F.);
#27990=ORIENTED_EDGE('',*,*,#19766,.T.);
#27991=ORIENTED_EDGE('',*,*,#19446,.T.);
#27992=ORIENTED_EDGE('',*,*,#19465,.F.);
#32026=CONICAL_SURFACE('',#36375,16.4,0.785398163397448);
#33166=ADVANCED_FACE('',(#4418),#59,.F.);
#33167=ADVANCED_FACE('',(#4419),#32026,.T.);
#33168=ADVANCED_FACE('',(#4420),#2891,.F.);
#33169=ADVANCED_FACE('',(#4421,#1301),#2323,.T.);
#33170=ADVANCED_FACE('',(#4422),#2324,.F.);
#33171=ADVANCED_FACE('',(#4423),#2325,.T.);
#33172=ADVANCED_FACE('',(#4424),#2326,.F.);
#33173=ADVANCED_FACE('',(#4425),#2327,.F.);
#33174=ADVANCED_FACE('',(#4426),#2328,.F.);
#33175=ADVANCED_FACE('',(#4427),#2329,.F.);
#33176=ADVANCED_FACE('',(#4428),#2330,.T.);
#33177=ADVANCED_FACE('',(#4429),#2331,.F.);
#33178=ADVANCED_FACE('',(#4430,#1302,#1303),#2892,.F.);
#33179=ADVANCED_FACE('',(#4431,#1304,#1305),#2893,.T.);
#33180=ADVANCED_FACE('',(#4432),#2332,.F.);
#33181=ADVANCED_FACE('',(#4433),#2333,.T.);
#33182=ADVANCED_FACE('',(#4434),#2894,.T.);
#33183=ADVANCED_FACE('',(#4435),#2895,.T.);
#33184=ADVANCED_FACE('',(#4436),#2896,.F.);
#33185=ADVANCED_FACE('',(#4437),#2897,.F.);
#33186=ADVANCED_FACE('',(#4438),#2898,.T.);
#33187=ADVANCED_FACE('',(#4439),#2334,.F.);
#33188=ADVANCED_FACE('',(#4440),#2899,.T.);
#33189=ADVANCED_FACE('',(#4441),#2335,.T.);
#33190=ADVANCED_FACE('',(#4442),#2336,.T.);
#33191=ADVANCED_FACE('',(#4443),#2900,.F.);
#33192=ADVANCED_FACE('',(#4444),#2337,.F.);
#33193=ADVANCED_FACE('',(#4445),#2901,.T.);
#33194=ADVANCED_FACE('',(#4446),#60,.F.);
#33195=ADVANCED_FACE('',(#4447),#2902,.T.);
#33196=ADVANCED_FACE('',(#4448),#2338,.T.);
#33197=ADVANCED_FACE('',(#4449),#2903,.F.);
#33198=ADVANCED_FACE('',(#4450),#2339,.F.);
#33199=ADVANCED_FACE('',(#4451),#2904,.F.);
#33200=ADVANCED_FACE('',(#4452),#1182,.T.);
#33201=ADVANCED_FACE('',(#4453),#2905,.T.);
#33202=ADVANCED_FACE('',(#4454),#1183,.T.);
#33203=ADVANCED_FACE('',(#4455),#214,.F.);
#33204=ADVANCED_FACE('',(#4456),#2906,.F.);
#33205=ADVANCED_FACE('',(#4457),#2340,.T.);
#33206=ADVANCED_FACE('',(#4458),#1184,.F.);
#33207=ADVANCED_FACE('',(#4459),#2907,.T.);
#33208=ADVANCED_FACE('',(#4460),#1185,.T.);
#33209=ADVANCED_FACE('',(#4461),#1186,.T.);
#33210=ADVANCED_FACE('',(#4462),#2908,.T.);
#33211=ADVANCED_FACE('',(#4463),#2341,.T.);
#33212=ADVANCED_FACE('',(#4464),#2909,.F.);
#33213=ADVANCED_FACE('',(#4465),#2910,.F.);
#33214=ADVANCED_FACE('',(#4466),#2342,.T.);
#33215=ADVANCED_FACE('',(#4467),#2911,.T.);
#33216=ADVANCED_FACE('',(#4468),#61,.F.);
#33217=ADVANCED_FACE('',(#4469,#1306),#2343,.T.);
#33218=ADVANCED_FACE('',(#4470),#2912,.T.);
#33219=ADVANCED_FACE('',(#4471),#2344,.F.);
#33220=ADVANCED_FACE('',(#4472),#2913,.F.);
#33221=ADVANCED_FACE('',(#4473),#2345,.T.);
#33222=ADVANCED_FACE('',(#4474),#2914,.F.);
#33223=ADVANCED_FACE('',(#4475),#2915,.T.);
#33224=ADVANCED_FACE('',(#4476),#215,.T.);
#33225=ADVANCED_FACE('',(#4477),#1187,.F.);
#33226=ADVANCED_FACE('',(#4478),#2916,.T.);
#33227=ADVANCED_FACE('',(#4479),#1188,.F.);
#33228=ADVANCED_FACE('',(#4480),#216,.F.);
#33229=ADVANCED_FACE('',(#4481),#2917,.F.);
#33230=ADVANCED_FACE('',(#4482),#2346,.T.);
#33231=ADVANCED_FACE('',(#4483),#1189,.T.);
#33232=ADVANCED_FACE('',(#4484),#2918,.T.);
#33233=ADVANCED_FACE('',(#4485),#1190,.F.);
#33234=ADVANCED_FACE('',(#4486),#1191,.F.);
#33235=ADVANCED_FACE('',(#4487),#2919,.T.);
#33236=ADVANCED_FACE('',(#4488),#2347,.F.);
#33237=ADVANCED_FACE('',(#4489),#2348,.F.);
#33238=ADVANCED_FACE('',(#4490),#2349,.T.);
#33239=ADVANCED_FACE('',(#4491),#2920,.T.);
#33240=ADVANCED_FACE('',(#4492),#2921,.T.);
#33241=ADVANCED_FACE('',(#4493),#2922,.F.);
#33242=ADVANCED_FACE('',(#4494),#2923,.F.);
#33243=ADVANCED_FACE('',(#4495),#2924,.T.);
#33244=ADVANCED_FACE('',(#4496),#2350,.F.);
#33245=ADVANCED_FACE('',(#4497),#2925,.T.);
#33246=ADVANCED_FACE('',(#4498),#2351,.T.);
#33247=ADVANCED_FACE('',(#4499),#2352,.T.);
#33248=ADVANCED_FACE('',(#4500),#2353,.T.);
#33249=ADVANCED_FACE('',(#4501),#2926,.F.);
#33250=ADVANCED_FACE('',(#4502),#2354,.T.);
#33251=ADVANCED_FACE('',(#4503),#2927,.F.);
#33252=ADVANCED_FACE('',(#4504),#2355,.F.);
#33253=ADVANCED_FACE('',(#4505),#2356,.T.);
#33254=ADVANCED_FACE('',(#4506),#2928,.F.);
#33255=ADVANCED_FACE('',(#4507),#2357,.T.);
#33256=ADVANCED_FACE('',(#4508),#2929,.F.);
#33257=ADVANCED_FACE('',(#4509),#2358,.F.);
#33258=ADVANCED_FACE('',(#4510),#2930,.T.);
#33259=ADVANCED_FACE('',(#4511),#2931,.T.);
#33260=ADVANCED_FACE('',(#4512),#2359,.F.);
#33261=ADVANCED_FACE('',(#4513),#2932,.T.);
#33262=ADVANCED_FACE('',(#4514),#2933,.T.);
#33263=ADVANCED_FACE('',(#4515),#2360,.F.);
#33264=ADVANCED_FACE('',(#4516),#2934,.F.);
#33265=ADVANCED_FACE('',(#4517),#2361,.F.);
#33266=ADVANCED_FACE('',(#4518),#2362,.F.);
#33267=ADVANCED_FACE('',(#4519),#2363,.F.);
#33268=ADVANCED_FACE('',(#4520),#2364,.F.);
#33269=ADVANCED_FACE('',(#4521,#1307),#2365,.F.);
#33270=ADVANCED_FACE('',(#4522),#2366,.F.);
#33271=ADVANCED_FACE('',(#4523,#1308),#2367,.T.);
#33272=ADVANCED_FACE('',(#4524),#2368,.F.);
#33273=ADVANCED_FACE('',(#4525),#2935,.T.);
#33274=ADVANCED_FACE('',(#4526),#2369,.F.);
#33275=ADVANCED_FACE('',(#4527),#2936,.T.);
#33276=ADVANCED_FACE('',(#4528),#2370,.F.);
#33277=ADVANCED_FACE('',(#4529),#2937,.T.);
#33278=ADVANCED_FACE('',(#4530),#2371,.F.);
#33279=ADVANCED_FACE('',(#4531),#2938,.T.);
#33280=ADVANCED_FACE('',(#4532),#2372,.F.);
#33281=ADVANCED_FACE('',(#4533),#2939,.T.);
#33282=ADVANCED_FACE('',(#4534),#2373,.F.);
#33283=ADVANCED_FACE('',(#4535),#2940,.T.);
#33284=ADVANCED_FACE('',(#4536),#62,.F.);
#34175=CLOSED_SHELL('',(#33166,#33167,#33168,#33169,#33170,#33171,#33172,
#33173,#33174,#33175,#33176,#33177,#33178,#33179,#33180,#33181,#33182,#33183,
#33184,#33185,#33186,#33187,#33188,#33189,#33190,#33191,#33192,#33193,#33194,
#33195,#33196,#33197,#33198,#33199,#33200,#33201,#33202,#33203,#33204,#33205,
#33206,#33207,#33208,#33209,#33210,#33211,#33212,#33213,#33214,#33215,#33216,
#33217,#33218,#33219,#33220,#33221,#33222,#33223,#33224,#33225,#33226,#33227,
#33228,#33229,#33230,#33231,#33232,#33233,#33234,#33235,#33236,#33237,#33238,
#33239,#33240,#33241,#33242,#33243,#33244,#33245,#33246,#33247,#33248,#33249,
#33250,#33251,#33252,#33253,#33254,#33255,#33256,#33257,#33258,#33259,#33260,
#33261,#33262,#33263,#33264,#33265,#33266,#33267,#33268,#33269,#33270,#33271,
#33272,#33273,#33274,#33275,#33276,#33277,#33278,#33279,#33280,#33281,#33282,
#33283,#33284));
#36369=AXIS2_PLACEMENT_3D('',#83281,#43795,#43796);
#36370=AXIS2_PLACEMENT_3D('',#83312,#43797,#43798);
#36371=AXIS2_PLACEMENT_3D('',#83319,#43799,#43800);
#36372=AXIS2_PLACEMENT_3D('',#83326,#43801,#43802);
#36373=AXIS2_PLACEMENT_3D('',#83359,#43803,#43804);
#36374=AXIS2_PLACEMENT_3D('',#83396,#43805,#43806);
#36375=AXIS2_PLACEMENT_3D('',#83427,#43807,#43808);
#36376=AXIS2_PLACEMENT_3D('',#83430,#43809,#43810);
#36377=AXIS2_PLACEMENT_3D('',#83431,#43811,#43812);
#36378=AXIS2_PLACEMENT_3D('',#83434,#43814,#43815);
#36379=AXIS2_PLACEMENT_3D('',#83435,#43816,#43817);
#36380=AXIS2_PLACEMENT_3D('',#83438,#43818,#43819);
#36381=AXIS2_PLACEMENT_3D('',#83455,#43822,#43823);
#36382=AXIS2_PLACEMENT_3D('',#83470,#43826,#43827);
#36383=AXIS2_PLACEMENT_3D('',#83471,#43828,#43829);
#36384=AXIS2_PLACEMENT_3D('',#83473,#43830,#43831);
#36385=AXIS2_PLACEMENT_3D('',#83474,#43832,#43833);
#36386=AXIS2_PLACEMENT_3D('',#83479,#43835,#43836);
#36387=AXIS2_PLACEMENT_3D('',#83482,#43838,#43839);
#36388=AXIS2_PLACEMENT_3D('',#83483,#43840,#43841);
#36389=AXIS2_PLACEMENT_3D('',#83489,#43845,#43846);
#36390=AXIS2_PLACEMENT_3D('',#83495,#43850,#43851);
#36391=AXIS2_PLACEMENT_3D('',#83496,#43852,#43853);
#36392=AXIS2_PLACEMENT_3D('',#83497,#43854,#43855);
#36393=AXIS2_PLACEMENT_3D('',#83498,#43856,#43857);
#36394=AXIS2_PLACEMENT_3D('',#83503,#43859,#43860);
#36395=AXIS2_PLACEMENT_3D('',#83506,#43862,#43863);
#36396=AXIS2_PLACEMENT_3D('',#83507,#43864,#43865);
#36397=AXIS2_PLACEMENT_3D('',#83513,#43869,#43870);
#36398=AXIS2_PLACEMENT_3D('',#83519,#43874,#43875);
#36399=AXIS2_PLACEMENT_3D('',#83520,#43876,#43877);
#36400=AXIS2_PLACEMENT_3D('',#83521,#43878,#43879);
#36401=AXIS2_PLACEMENT_3D('',#83522,#43880,#43881);
#36402=AXIS2_PLACEMENT_3D('',#83525,#43882,#43883);
#36403=AXIS2_PLACEMENT_3D('',#83529,#43885,#43886);
#36404=AXIS2_PLACEMENT_3D('',#83533,#43888,#43889);
#36405=AXIS2_PLACEMENT_3D('',#83537,#43891,#43892);
#36406=AXIS2_PLACEMENT_3D('',#83541,#43894,#43895);
#36407=AXIS2_PLACEMENT_3D('',#83545,#43897,#43898);
#36408=AXIS2_PLACEMENT_3D('',#83560,#43900,#43901);
#36409=AXIS2_PLACEMENT_3D('',#83575,#43903,#43904);
#36410=AXIS2_PLACEMENT_3D('',#83590,#43906,#43907);
#36411=AXIS2_PLACEMENT_3D('',#83605,#43909,#43910);
#36412=AXIS2_PLACEMENT_3D('',#83620,#43912,#43913);
#36413=AXIS2_PLACEMENT_3D('',#83635,#43915,#43916);
#36414=AXIS2_PLACEMENT_3D('',#83639,#43918,#43919);
#36415=AXIS2_PLACEMENT_3D('',#83643,#43921,#43922);
#36416=AXIS2_PLACEMENT_3D('',#83647,#43924,#43925);
#36417=AXIS2_PLACEMENT_3D('',#83650,#43927,#43928);
#36418=AXIS2_PLACEMENT_3D('',#83652,#43929,#43930);
#36419=AXIS2_PLACEMENT_3D('',#83678,#43932,#43933);
#36420=AXIS2_PLACEMENT_3D('',#83704,#43935,#43936);
#36421=AXIS2_PLACEMENT_3D('',#83730,#43938,#43939);
#36422=AXIS2_PLACEMENT_3D('',#83754,#43941,#43942);
#36423=AXIS2_PLACEMENT_3D('',#83758,#43944,#43945);
#36424=AXIS2_PLACEMENT_3D('',#83784,#43947,#43948);
#36425=AXIS2_PLACEMENT_3D('',#83810,#43950,#43951);
#36426=AXIS2_PLACEMENT_3D('',#83836,#43953,#43954);
#36427=AXIS2_PLACEMENT_3D('',#83861,#43956,#43957);
#36428=AXIS2_PLACEMENT_3D('',#83862,#43958,#43959);
#36429=AXIS2_PLACEMENT_3D('',#83868,#43963,#43964);
#36430=AXIS2_PLACEMENT_3D('',#83874,#43968,#43969);
#36431=AXIS2_PLACEMENT_3D('',#83876,#43970,#43971);
#36432=AXIS2_PLACEMENT_3D('',#83878,#43972,#43973);
#36433=AXIS2_PLACEMENT_3D('',#83880,#43975,#43976);
#36434=AXIS2_PLACEMENT_3D('',#83881,#43977,#43978);
#36435=AXIS2_PLACEMENT_3D('',#83882,#43979,#43980);
#36436=AXIS2_PLACEMENT_3D('',#83883,#43981,#43982);
#36437=AXIS2_PLACEMENT_3D('',#83888,#43984,#43985);
#36438=AXIS2_PLACEMENT_3D('',#83891,#43987,#43988);
#36439=AXIS2_PLACEMENT_3D('',#83892,#43989,#43990);
#36440=AXIS2_PLACEMENT_3D('',#83896,#43992,#43993);
#36441=AXIS2_PLACEMENT_3D('',#83897,#43994,#43995);
#36442=AXIS2_PLACEMENT_3D('',#83898,#43996,#43997);
#36443=AXIS2_PLACEMENT_3D('',#83900,#43998,#43999);
#36444=AXIS2_PLACEMENT_3D('',#83903,#44001,#44002);
#36445=AXIS2_PLACEMENT_3D('',#83904,#44003,#44004);
#36446=AXIS2_PLACEMENT_3D('',#83907,#44007,#44008);
#36447=AXIS2_PLACEMENT_3D('',#83909,#44009,#44010);
#36448=AXIS2_PLACEMENT_3D('',#83911,#44011,#44012);
#36449=AXIS2_PLACEMENT_3D('',#83913,#44014,#44015);
#36450=AXIS2_PLACEMENT_3D('',#83915,#44017,#44018);
#36451=AXIS2_PLACEMENT_3D('',#83917,#44020,#44021);
#36452=AXIS2_PLACEMENT_3D('',#83920,#44022,#44023);
#36453=AXIS2_PLACEMENT_3D('',#83924,#44025,#44026);
#36454=AXIS2_PLACEMENT_3D('',#83926,#44028,#44029);
#36455=AXIS2_PLACEMENT_3D('',#83932,#44033,#44034);
#36456=AXIS2_PLACEMENT_3D('',#83934,#44035,#44036);
#36457=AXIS2_PLACEMENT_3D('',#83936,#44037,#44038);
#36458=AXIS2_PLACEMENT_3D('',#83965,#44040,#44041);
#36459=AXIS2_PLACEMENT_3D('',#83966,#44042,#44043);
#36460=AXIS2_PLACEMENT_3D('',#83967,#44044,#44045);
#36461=AXIS2_PLACEMENT_3D('',#83968,#44046,#44047);
#36462=AXIS2_PLACEMENT_3D('',#83971,#44050,#44051);
#36463=AXIS2_PLACEMENT_3D('',#83975,#44053,#44054);
#36464=AXIS2_PLACEMENT_3D('',#83979,#44057,#44058);
#36465=AXIS2_PLACEMENT_3D('',#83989,#44060,#44061);
#36466=AXIS2_PLACEMENT_3D('',#83990,#44062,#44063);
#36467=AXIS2_PLACEMENT_3D('',#83993,#44066,#44067);
#36468=AXIS2_PLACEMENT_3D('',#83995,#44068,#44069);
#36469=AXIS2_PLACEMENT_3D('',#83998,#44071,#44072);
#36470=AXIS2_PLACEMENT_3D('',#84054,#44073,#44074);
#36471=AXIS2_PLACEMENT_3D('',#84110,#44075,#44076);
#36472=AXIS2_PLACEMENT_3D('',#84131,#44078,#44079);
#36473=AXIS2_PLACEMENT_3D('',#84132,#44080,#44081);
#36474=AXIS2_PLACEMENT_3D('',#84133,#44082,#44083);
#36475=AXIS2_PLACEMENT_3D('',#84135,#44084,#44085);
#36476=AXIS2_PLACEMENT_3D('',#84177,#44086,#44087);
#36477=AXIS2_PLACEMENT_3D('',#84186,#44089,#44090);
#36478=AXIS2_PLACEMENT_3D('',#84274,#44092,#44093);
#36479=AXIS2_PLACEMENT_3D('',#84275,#44094,#44095);
#36480=AXIS2_PLACEMENT_3D('',#84277,#44096,#44097);
#36481=AXIS2_PLACEMENT_3D('',#84383,#44099,#44100);
#36482=AXIS2_PLACEMENT_3D('',#84415,#44101,#44102);
#36483=AXIS2_PLACEMENT_3D('',#84416,#44103,#44104);
#36484=AXIS2_PLACEMENT_3D('',#84417,#44105,#44106);
#36485=AXIS2_PLACEMENT_3D('',#84419,#44108,#44109);
#36486=AXIS2_PLACEMENT_3D('',#84421,#44111,#44112);
#36487=AXIS2_PLACEMENT_3D('',#84425,#44114,#44115);
#36488=AXIS2_PLACEMENT_3D('',#84426,#44116,#44117);
#36489=AXIS2_PLACEMENT_3D('',#84427,#44118,#44119);
#36490=AXIS2_PLACEMENT_3D('',#84429,#44120,#44121);
#36491=AXIS2_PLACEMENT_3D('',#84432,#44123,#44124);
#36492=AXIS2_PLACEMENT_3D('',#84433,#44125,#44126);
#36493=AXIS2_PLACEMENT_3D('',#84439,#44130,#44131);
#36494=AXIS2_PLACEMENT_3D('',#84443,#44133,#44134);
#36495=AXIS2_PLACEMENT_3D('',#84444,#44135,#44136);
#36496=AXIS2_PLACEMENT_3D('',#84471,#44137,#44138);
#36497=AXIS2_PLACEMENT_3D('',#84473,#44139,#44140);
#36498=AXIS2_PLACEMENT_3D('',#84474,#44141,#44142);
#36499=AXIS2_PLACEMENT_3D('',#84475,#44143,#44144);
#36500=AXIS2_PLACEMENT_3D('',#84477,#44146,#44147);
#36501=AXIS2_PLACEMENT_3D('',#84479,#44148,#44149);
#36502=AXIS2_PLACEMENT_3D('',#84480,#44150,#44151);
#36503=AXIS2_PLACEMENT_3D('',#84481,#44152,#44153);
#36504=AXIS2_PLACEMENT_3D('',#84483,#44155,#44156);
#36505=AXIS2_PLACEMENT_3D('',#84489,#44159,#44160);
#36506=AXIS2_PLACEMENT_3D('',#84491,#44162,#44163);
#36507=AXIS2_PLACEMENT_3D('',#84493,#44164,#44165);
#36508=AXIS2_PLACEMENT_3D('',#84496,#44167,#44168);
#36509=AXIS2_PLACEMENT_3D('',#84497,#44169,#44170);
#36510=AXIS2_PLACEMENT_3D('',#84500,#44173,#44174);
#36511=AXIS2_PLACEMENT_3D('',#84503,#44176,#44177);
#36512=AXIS2_PLACEMENT_3D('',#84504,#44178,#44179);
#36513=AXIS2_PLACEMENT_3D('',#84505,#44180,#44181);
#36514=AXIS2_PLACEMENT_3D('',#84506,#44182,#44183);
#36515=AXIS2_PLACEMENT_3D('',#84562,#44184,#44185);
#36516=AXIS2_PLACEMENT_3D('',#84563,#44186,#44187);
#36517=AXIS2_PLACEMENT_3D('',#84564,#44188,#44189);
#36518=AXIS2_PLACEMENT_3D('',#84585,#44191,#44192);
#36519=AXIS2_PLACEMENT_3D('',#84586,#44193,#44194);
#36520=AXIS2_PLACEMENT_3D('',#84587,#44195,#44196);
#36521=AXIS2_PLACEMENT_3D('',#84667,#44197,#44198);
#36522=AXIS2_PLACEMENT_3D('',#84668,#44199,#44200);
#36523=AXIS2_PLACEMENT_3D('',#84677,#44202,#44203);
#36524=AXIS2_PLACEMENT_3D('',#84734,#44205,#44206);
#36525=AXIS2_PLACEMENT_3D('',#84763,#44207,#44208);
#36526=AXIS2_PLACEMENT_3D('',#84766,#44210,#44211);
#36527=AXIS2_PLACEMENT_3D('',#84822,#44212,#44213);
#36528=AXIS2_PLACEMENT_3D('',#84903,#44214,#44215);
#36529=AXIS2_PLACEMENT_3D('',#84904,#44216,#44217);
#36530=AXIS2_PLACEMENT_3D('',#84905,#44218,#44219);
#36531=AXIS2_PLACEMENT_3D('',#84907,#44221,#44222);
#36532=AXIS2_PLACEMENT_3D('',#84909,#44224,#44225);
#36533=AXIS2_PLACEMENT_3D('',#84915,#44229,#44230);
#36534=AXIS2_PLACEMENT_3D('',#84921,#44234,#44235);
#36535=AXIS2_PLACEMENT_3D('',#84923,#44236,#44237);
#36536=AXIS2_PLACEMENT_3D('',#84925,#44238,#44239);
#36537=AXIS2_PLACEMENT_3D('',#84927,#44241,#44242);
#36538=AXIS2_PLACEMENT_3D('',#84928,#44243,#44244);
#36539=AXIS2_PLACEMENT_3D('',#84929,#44245,#44246);
#36540=AXIS2_PLACEMENT_3D('',#84930,#44247,#44248);
#36541=AXIS2_PLACEMENT_3D('',#84935,#44250,#44251);
#36542=AXIS2_PLACEMENT_3D('',#84938,#44253,#44254);
#36543=AXIS2_PLACEMENT_3D('',#84939,#44255,#44256);
#36544=AXIS2_PLACEMENT_3D('',#84943,#44258,#44259);
#36545=AXIS2_PLACEMENT_3D('',#84944,#44260,#44261);
#36546=AXIS2_PLACEMENT_3D('',#84945,#44262,#44263);
#36547=AXIS2_PLACEMENT_3D('',#84947,#44264,#44265);
#36548=AXIS2_PLACEMENT_3D('',#84950,#44267,#44268);
#36549=AXIS2_PLACEMENT_3D('',#84951,#44269,#44270);
#36550=AXIS2_PLACEMENT_3D('',#84954,#44273,#44274);
#36551=AXIS2_PLACEMENT_3D('',#84956,#44275,#44276);
#36552=AXIS2_PLACEMENT_3D('',#84958,#44277,#44278);
#36553=AXIS2_PLACEMENT_3D('',#84960,#44280,#44281);
#36554=AXIS2_PLACEMENT_3D('',#84962,#44283,#44284);
#36555=AXIS2_PLACEMENT_3D('',#84964,#44286,#44287);
#36556=AXIS2_PLACEMENT_3D('',#84967,#44290,#44291);
#36557=AXIS2_PLACEMENT_3D('',#84969,#44293,#44294);
#36558=AXIS2_PLACEMENT_3D('',#84971,#44296,#44297);
#36559=AXIS2_PLACEMENT_3D('',#84973,#44299,#44300);
#36560=AXIS2_PLACEMENT_3D('',#84975,#44302,#44303);
#36561=AXIS2_PLACEMENT_3D('',#84978,#44306,#44307);
#36562=AXIS2_PLACEMENT_3D('',#84980,#44309,#44310);
#36563=AXIS2_PLACEMENT_3D('',#84982,#44312,#44313);
#36564=AXIS2_PLACEMENT_3D('',#84984,#44315,#44316);
#36565=AXIS2_PLACEMENT_3D('',#84986,#44318,#44319);
#36566=AXIS2_PLACEMENT_3D('',#84988,#44321,#44322);
#36567=AXIS2_PLACEMENT_3D('',#84990,#44324,#44325);
#36568=AXIS2_PLACEMENT_3D('',#84991,#44326,#44327);
#36569=AXIS2_PLACEMENT_3D('',#84993,#44329,#44330);
#36570=AXIS2_PLACEMENT_3D('',#84995,#44332,#44333);
#36571=AXIS2_PLACEMENT_3D('',#84996,#44334,#44335);
#36572=AXIS2_PLACEMENT_3D('',#84998,#44336,#44337);
#36573=AXIS2_PLACEMENT_3D('',#85000,#44339,#44340);
#36574=AXIS2_PLACEMENT_3D('',#85001,#44341,#44342);
#36575=AXIS2_PLACEMENT_3D('',#85002,#44343,#44344);
#36576=AXIS2_PLACEMENT_3D('',#85003,#44345,#44346);
#36577=AXIS2_PLACEMENT_3D('',#85004,#44347,#44348);
#36578=AXIS2_PLACEMENT_3D('',#85005,#44349,#44350);
#36579=AXIS2_PLACEMENT_3D('',#85006,#44351,#44352);
#36580=AXIS2_PLACEMENT_3D('',#85009,#44353,#44354);
#36581=AXIS2_PLACEMENT_3D('',#85013,#44356,#44357);
#36582=AXIS2_PLACEMENT_3D('',#85017,#44359,#44360);
#36583=AXIS2_PLACEMENT_3D('',#85021,#44362,#44363);
#36584=AXIS2_PLACEMENT_3D('',#85025,#44365,#44366);
#36585=AXIS2_PLACEMENT_3D('',#85029,#44368,#44369);
#36586=AXIS2_PLACEMENT_3D('',#85031,#44371,#44372);
#36587=AXIS2_PLACEMENT_3D('',#85034,#44375,#44376);
#36588=AXIS2_PLACEMENT_3D('',#85036,#44378,#44379);
#36589=AXIS2_PLACEMENT_3D('',#85038,#44381,#44382);
#36590=AXIS2_PLACEMENT_3D('',#85041,#44384,#44385);
#36591=AXIS2_PLACEMENT_3D('',#85042,#44386,#44387);
#36592=AXIS2_PLACEMENT_3D('',#85075,#44389,#44390);
#36593=AXIS2_PLACEMENT_3D('',#85078,#44392,#44393);
#36594=AXIS2_PLACEMENT_3D('',#85079,#44394,#44395);
#36595=AXIS2_PLACEMENT_3D('',#85116,#44397,#44398);
#36596=AXIS2_PLACEMENT_3D('',#85119,#44400,#44401);
#36597=AXIS2_PLACEMENT_3D('',#85120,#44402,#44403);
#36598=AXIS2_PLACEMENT_3D('',#85153,#44405,#44406);
#36599=AXIS2_PLACEMENT_3D('',#85155,#44408,#44409);
#36600=AXIS2_PLACEMENT_3D('',#85156,#44410,#44411);
#36601=AXIS2_PLACEMENT_3D('',#85158,#44413,#44414);
#43795=DIRECTION('axis',(0.,0.,1.));
#43796=DIRECTION('refdir',(1.,0.,0.));
#43797=DIRECTION('center_axis',(0.,1.,0.));
#43798=DIRECTION('ref_axis',(0.,0.,1.));
#43799=DIRECTION('center_axis',(0.,1.,0.));
#43800=DIRECTION('ref_axis',(0.,0.,1.));
#43801=DIRECTION('center_axis',(0.,1.,0.));
#43802=DIRECTION('ref_axis',(0.,0.,1.));
#43803=DIRECTION('center_axis',(0.,-1.,0.));
#43804=DIRECTION('ref_axis',(0.,0.,-1.));
#43805=DIRECTION('center_axis',(0.,1.,0.));
#43806=DIRECTION('ref_axis',(0.,0.,1.));
#43807=DIRECTION('center_axis',(0.,-1.,0.));
#43808=DIRECTION('ref_axis',(0.,0.,-1.));
#43809=DIRECTION('center_axis',(0.,-1.,0.));
#43810=DIRECTION('ref_axis',(0.,0.,1.));
#43811=DIRECTION('center_axis',(0.,-1.,0.));
#43812=DIRECTION('ref_axis',(0.,0.,1.));
#43813=DIRECTION('',(8.65956056235493E-17,0.707106781186548,-0.707106781186547));
#43814=DIRECTION('center_axis',(0.,1.,0.));
#43815=DIRECTION('ref_axis',(0.,0.,1.));
#43816=DIRECTION('center_axis',(0.,-1.,0.));
#43817=DIRECTION('ref_axis',(-6.04901474818E-16,0.,1.));
#43818=DIRECTION('center_axis',(0.,1.,0.));
#43819=DIRECTION('ref_axis',(4.81230659094137E-15,0.,1.));
#43820=DIRECTION('',(0.,-1.,0.));
#43821=DIRECTION('',(0.,-1.,0.));
#43822=DIRECTION('center_axis',(0.,-1.,0.));
#43823=DIRECTION('ref_axis',(1.,0.,0.));
#43824=DIRECTION('',(0.,-1.,0.));
#43825=DIRECTION('',(0.,-1.,0.));
#43826=DIRECTION('center_axis',(0.,1.,0.));
#43827=DIRECTION('ref_axis',(1.,0.,0.));
#43828=DIRECTION('center_axis',(0.,1.,0.));
#43829=DIRECTION('ref_axis',(0.,0.,1.));
#43830=DIRECTION('center_axis',(0.,-1.,0.));
#43831=DIRECTION('ref_axis',(1.,0.,0.));
#43832=DIRECTION('center_axis',(0.,1.,0.));
#43833=DIRECTION('ref_axis',(1.,0.,0.));
#43834=DIRECTION('',(-1.,0.,0.));
#43835=DIRECTION('center_axis',(0.,1.,0.));
#43836=DIRECTION('ref_axis',(1.,0.,0.));
#43837=DIRECTION('',(-1.,0.,0.));
#43838=DIRECTION('center_axis',(0.,1.,0.));
#43839=DIRECTION('ref_axis',(1.,0.,0.));
#43840=DIRECTION('center_axis',(0.,0.,1.));
#43841=DIRECTION('ref_axis',(1.,0.,0.));
#43842=DIRECTION('',(0.,1.,0.));
#43843=DIRECTION('',(0.,1.,0.));
#43844=DIRECTION('',(-1.,0.,0.));
#43845=DIRECTION('center_axis',(0.,0.,1.));
#43846=DIRECTION('ref_axis',(1.,0.,0.));
#43847=DIRECTION('',(-1.,0.,0.));
#43848=DIRECTION('',(0.,1.,0.));
#43849=DIRECTION('',(0.,1.,0.));
#43850=DIRECTION('center_axis',(0.,-1.,0.));
#43851=DIRECTION('ref_axis',(0.,0.,-1.));
#43852=DIRECTION('center_axis',(0.,-1.,0.));
#43853=DIRECTION('ref_axis',(1.,0.,0.));
#43854=DIRECTION('center_axis',(0.,-1.,0.));
#43855=DIRECTION('ref_axis',(1.,0.,0.));
#43856=DIRECTION('center_axis',(0.,1.,0.));
#43857=DIRECTION('ref_axis',(1.,0.,0.));
#43858=DIRECTION('',(-1.,0.,0.));
#43859=DIRECTION('center_axis',(0.,1.,0.));
#43860=DIRECTION('ref_axis',(1.,0.,0.));
#43861=DIRECTION('',(-1.,0.,0.));
#43862=DIRECTION('center_axis',(0.,1.,0.));
#43863=DIRECTION('ref_axis',(1.,0.,0.));
#43864=DIRECTION('center_axis',(0.,0.,1.));
#43865=DIRECTION('ref_axis',(1.,0.,0.));
#43866=DIRECTION('',(0.,1.,0.));
#43867=DIRECTION('',(-1.,0.,0.));
#43868=DIRECTION('',(0.,1.,0.));
#43869=DIRECTION('center_axis',(0.,0.,1.));
#43870=DIRECTION('ref_axis',(1.,0.,0.));
#43871=DIRECTION('',(0.,1.,0.));
#43872=DIRECTION('',(-1.,0.,0.));
#43873=DIRECTION('',(0.,1.,0.));
#43874=DIRECTION('center_axis',(0.,-1.,0.));
#43875=DIRECTION('ref_axis',(0.,0.,-1.));
#43876=DIRECTION('center_axis',(0.,-1.,0.));
#43877=DIRECTION('ref_axis',(1.,0.,0.));
#43878=DIRECTION('center_axis',(0.,-1.,0.));
#43879=DIRECTION('ref_axis',(1.,0.,0.));
#43880=DIRECTION('center_axis',(0.,1.,0.));
#43881=DIRECTION('ref_axis',(0.479425538604204,0.,0.877582561890372));
#43882=DIRECTION('center_axis',(0.,-1.,0.));
#43883=DIRECTION('ref_axis',(1.,0.,0.));
#43884=DIRECTION('',(0.,1.,0.));
#43885=DIRECTION('center_axis',(0.,1.,0.));
#43886=DIRECTION('ref_axis',(-0.971277075433192,0.,-0.237951345316528));
#43887=DIRECTION('',(0.,-1.,0.));
#43888=DIRECTION('center_axis',(0.,-1.,0.));
#43889=DIRECTION('ref_axis',(1.,0.,0.));
#43890=DIRECTION('',(0.,-1.,0.));
#43891=DIRECTION('center_axis',(0.,1.,0.));
#43892=DIRECTION('ref_axis',(-0.989856436210018,0.,0.142071234574779));
#43893=DIRECTION('',(0.,-1.,0.));
#43894=DIRECTION('center_axis',(0.,-1.,0.));
#43895=DIRECTION('ref_axis',(1.,0.,0.));
#43896=DIRECTION('',(0.,-1.,0.));
#43897=DIRECTION('center_axis',(0.,1.,0.));
#43898=DIRECTION('ref_axis',(-0.456844166721239,0.,0.889546742635134));
#43899=DIRECTION('',(0.,-1.,0.));
#43900=DIRECTION('center_axis',(0.,-1.,0.));
#43901=DIRECTION('ref_axis',(1.,0.,0.));
#43902=DIRECTION('',(0.,-1.,0.));
#43903=DIRECTION('center_axis',(0.,1.,0.));
#43904=DIRECTION('ref_axis',(-0.0624652415091979,0.,0.998047139970451));
#43905=DIRECTION('',(0.,-1.,0.));
#43906=DIRECTION('center_axis',(0.,1.,0.));
#43907=DIRECTION('ref_axis',(1.,0.,0.));
#43908=DIRECTION('',(0.,-1.,0.));
#43909=DIRECTION('center_axis',(0.,1.,0.));
#43910=DIRECTION('ref_axis',(0.361068082792987,0.,0.932539457389443));
#43911=DIRECTION('',(0.,-1.,0.));
#43912=DIRECTION('center_axis',(0.,1.,0.));
#43913=DIRECTION('ref_axis',(1.,0.,0.));
#43914=DIRECTION('',(0.,-1.,0.));
#43915=DIRECTION('center_axis',(0.,1.,0.));
#43916=DIRECTION('ref_axis',(0.479425538604341,0.,0.877582561890297));
#43917=DIRECTION('',(0.,-1.,0.));
#43918=DIRECTION('center_axis',(0.,-1.,0.));
#43919=DIRECTION('ref_axis',(1.,0.,0.));
#43920=DIRECTION('',(0.,-1.,0.));
#43921=DIRECTION('center_axis',(0.,1.,0.));
#43922=DIRECTION('ref_axis',(0.989856436210018,0.,-0.142071234574783));
#43923=DIRECTION('',(0.,-1.,0.));
#43924=DIRECTION('center_axis',(0.,-1.,0.));
#43925=DIRECTION('ref_axis',(1.,0.,0.));
#43926=DIRECTION('',(0.,-1.,0.));
#43927=DIRECTION('center_axis',(0.,1.,0.));
#43928=DIRECTION('ref_axis',(-0.971277075433192,0.,-0.237951345316528));
#43929=DIRECTION('center_axis',(0.,-1.,0.));
#43930=DIRECTION('ref_axis',(1.,0.,0.));
#43931=DIRECTION('',(0.,1.,0.));
#43932=DIRECTION('center_axis',(0.,-1.,0.));
#43933=DIRECTION('ref_axis',(1.,0.,0.));
#43934=DIRECTION('',(0.,1.,0.));
#43935=DIRECTION('center_axis',(0.,-1.,0.));
#43936=DIRECTION('ref_axis',(1.,0.,0.));
#43937=DIRECTION('',(0.,1.,0.));
#43938=DIRECTION('center_axis',(0.,1.,0.));
#43939=DIRECTION('ref_axis',(1.,0.,0.));
#43940=DIRECTION('',(0.,1.,0.));
#43941=DIRECTION('center_axis',(0.,1.,0.));
#43942=DIRECTION('ref_axis',(0.479425538604204,0.,0.877582561890372));
#43943=DIRECTION('',(0.,-1.,0.));
#43944=DIRECTION('center_axis',(0.,-1.,0.));
#43945=DIRECTION('ref_axis',(1.,0.,0.));
#43946=DIRECTION('',(0.,1.,0.));
#43947=DIRECTION('center_axis',(0.,1.,0.));
#43948=DIRECTION('ref_axis',(1.,0.,0.));
#43949=DIRECTION('',(0.,1.,0.));
#43950=DIRECTION('center_axis',(0.,1.,0.));
#43951=DIRECTION('ref_axis',(1.,0.,0.));
#43952=DIRECTION('',(0.,1.,0.));
#43953=DIRECTION('center_axis',(0.,-1.,0.));
#43954=DIRECTION('ref_axis',(1.,0.,0.));
#43955=DIRECTION('',(0.,1.,0.));
#43956=DIRECTION('center_axis',(0.,-1.,0.));
#43957=DIRECTION('ref_axis',(1.,0.,0.));
#43958=DIRECTION('center_axis',(-0.52238673488493,0.,-0.852708683675886));
#43959=DIRECTION('ref_axis',(-0.852708683675886,0.,0.52238673488493));
#43960=DIRECTION('',(0.85270868367354,0.,-0.522386734888759));
#43961=DIRECTION('',(0.,-1.,0.));
#43962=DIRECTION('',(0.852708683675886,0.,-0.52238673488493));
#43963=DIRECTION('center_axis',(0.52238673488493,0.,-0.852708683675886));
#43964=DIRECTION('ref_axis',(0.,-1.,0.));
#43965=DIRECTION('',(0.852708683675886,0.,0.52238673488493));
#43966=DIRECTION('',(0.,1.,0.));
#43967=DIRECTION('',(0.85270868366004,0.,0.522386734910796));
#43968=DIRECTION('center_axis',(0.,-1.,0.));
#43969=DIRECTION('ref_axis',(0.99973889499905,0.,-0.0228504228861944));
#43970=DIRECTION('center_axis',(0.,-1.,0.));
#43971=DIRECTION('ref_axis',(1.,0.,0.));
#43972=DIRECTION('center_axis',(0.,-1.,0.));
#43973=DIRECTION('ref_axis',(0.998419029265298,0.,0.0562089138921914));
#43974=DIRECTION('',(0.,1.,0.));
#43975=DIRECTION('center_axis',(0.,1.,0.));
#43976=DIRECTION('ref_axis',(-0.727788421795868,0.,-0.685801730166876));
#43977=DIRECTION('center_axis',(0.,-1.,0.));
#43978=DIRECTION('ref_axis',(0.928397903310364,0.,0.371587584734636));
#43979=DIRECTION('center_axis',(0.,-1.,0.));
#43980=DIRECTION('ref_axis',(1.,0.,0.));
#43981=DIRECTION('center_axis',(0.,-1.,0.));
#43982=DIRECTION('ref_axis',(0.985455636737957,0.,-0.169932892699993));
#43983=DIRECTION('',(0.,1.,0.));
#43984=DIRECTION('center_axis',(0.,1.,0.));
#43985=DIRECTION('ref_axis',(0.989299838612263,0.,-0.145896639172227));
#43986=DIRECTION('',(0.,-1.,0.));
#43987=DIRECTION('center_axis',(0.,1.,0.));
#43988=DIRECTION('ref_axis',(1.,0.,0.));
#43989=DIRECTION('center_axis',(0.,1.,0.));
#43990=DIRECTION('ref_axis',(0.115367964260996,0.,0.99332282407195));
#43991=DIRECTION('',(0.,-1.,0.));
#43992=DIRECTION('center_axis',(-1.93875202872386E-14,-1.,-1.52293552293204E-14));
#43993=DIRECTION('ref_axis',(0.291057680790064,-2.2204460492503E-14,0.956705506649308));
#43994=DIRECTION('center_axis',(0.,1.,0.));
#43995=DIRECTION('ref_axis',(1.,0.,0.));
#43996=DIRECTION('center_axis',(0.,1.,0.));
#43997=DIRECTION('ref_axis',(-0.291057680714125,0.,-0.956705506672411));
#43998=DIRECTION('center_axis',(0.,1.,0.));
#43999=DIRECTION('ref_axis',(1.,0.,0.));
#44000=DIRECTION('',(0.,-1.,0.));
#44001=DIRECTION('center_axis',(0.,-1.,0.));
#44002=DIRECTION('ref_axis',(-0.291057680796176,0.,-0.956705506647449));
#44003=DIRECTION('center_axis',(0.52238673488493,0.,-0.852708683675886));
#44004=DIRECTION('ref_axis',(0.,-1.,0.));
#44005=DIRECTION('',(-0.852708683675886,0.,-0.52238673488493));
#44006=DIRECTION('',(-0.852708683677683,0.,-0.522386734881996));
#44007=DIRECTION('center_axis',(0.,-1.,0.));
#44008=DIRECTION('ref_axis',(-0.98929983861229,0.,0.145896639172043));
#44009=DIRECTION('center_axis',(0.,1.,0.));
#44010=DIRECTION('ref_axis',(1.,0.,0.));
#44011=DIRECTION('center_axis',(0.,-1.,0.));
#44012=DIRECTION('ref_axis',(-0.52238673496676,0.,-0.852708683625755));
#44013=DIRECTION('',(0.,-1.,0.));
#44014=DIRECTION('center_axis',(0.,-1.,0.));
#44015=DIRECTION('ref_axis',(0.,0.,-1.));
#44016=DIRECTION('',(0.852708683675886,0.,-0.52238673488493));
#44017=DIRECTION('center_axis',(-0.52238673488493,0.,-0.852708683675886));
#44018=DIRECTION('ref_axis',(-0.852708683675886,0.,0.52238673488493));
#44019=DIRECTION('',(0.852708683678698,0.,-0.52238673488034));
#44020=DIRECTION('center_axis',(0.,-1.,0.));
#44021=DIRECTION('ref_axis',(0.952171177670241,0.,0.305565129578075));
#44022=DIRECTION('center_axis',(0.,1.,0.));
#44023=DIRECTION('ref_axis',(0.952171177838408,0.,0.305565129054051));
#44024=DIRECTION('',(0.,1.,0.));
#44025=DIRECTION('center_axis',(0.,-1.,0.));
#44026=DIRECTION('ref_axis',(1.,0.,0.));
#44027=DIRECTION('',(0.,1.,0.));
#44028=DIRECTION('center_axis',(0.952171177670241,0.,0.305565129578077));
#44029=DIRECTION('ref_axis',(0.,-1.,0.));
#44030=DIRECTION('',(0.305565129583039,0.,-0.952171177668648));
#44031=DIRECTION('',(0.,1.,0.));
#44032=DIRECTION('',(-0.305565129578077,0.,0.952171177670241));
#44033=DIRECTION('center_axis',(0.,-1.,0.));
#44034=DIRECTION('ref_axis',(-0.184788912514002,0.,-0.982778234299016));
#44035=DIRECTION('center_axis',(0.,1.,0.));
#44036=DIRECTION('ref_axis',(1.,0.,0.));
#44037=DIRECTION('center_axis',(0.,1.,0.));
#44038=DIRECTION('ref_axis',(1.,0.,0.));
#44039=DIRECTION('',(0.,-1.,0.));
#44040=DIRECTION('center_axis',(0.,1.,0.));
#44041=DIRECTION('ref_axis',(1.,0.,0.));
#44042=DIRECTION('center_axis',(0.982778234299016,0.,-0.184788912514004));
#44043=DIRECTION('ref_axis',(0.184788912514004,0.,0.982778234299016));
#44044=DIRECTION('center_axis',(-0.305565129578077,0.,0.952171177670241));
#44045=DIRECTION('ref_axis',(0.952171177670241,0.,0.305565129578077));
#44046=DIRECTION('center_axis',(-0.305565129578077,7.88432920788926E-29,
0.952171177670241));
#44047=DIRECTION('ref_axis',(-2.4091760760449E-29,-1.,7.50723102701579E-29));
#44048=DIRECTION('',(0.305565129578077,0.,-0.952171177670241));
#44049=DIRECTION('',(0.305565129578077,0.,-0.952171177670241));
#44050=DIRECTION('center_axis',(0.952171177670241,0.,0.305565129578077));
#44051=DIRECTION('ref_axis',(0.,-1.,0.));
#44052=DIRECTION('',(0.305565129578077,0.,-0.952171177670241));
#44053=DIRECTION('center_axis',(0.952171177669702,-1.65558619039422E-11,
0.305565129579756));
#44054=DIRECTION('ref_axis',(0.305564047343791,0.00266148306317448,-0.952167805315211));
#44055=DIRECTION('',(0.,-1.,0.));
#44056=DIRECTION('',(0.305565129582466,0.,-0.952171177668832));
#44057=DIRECTION('center_axis',(0.,1.,0.));
#44058=DIRECTION('ref_axis',(0.593785833940128,0.,-0.80462313129317));
#44059=DIRECTION('',(0.,-1.,0.));
#44060=DIRECTION('center_axis',(0.,1.,0.));
#44061=DIRECTION('ref_axis',(-0.952171177741116,0.,-0.305565129357222));
#44062=DIRECTION('center_axis',(0.593785833940127,0.,-0.804623131293172));
#44063=DIRECTION('ref_axis',(0.,-1.,0.));
#44064=DIRECTION('',(0.804623131293172,0.,0.593785833940126));
#44065=DIRECTION('',(0.804623131286062,0.,0.59378583394976));
#44066=DIRECTION('center_axis',(0.,1.,0.));
#44067=DIRECTION('ref_axis',(0.952171177670241,0.,0.305565129578075));
#44068=DIRECTION('center_axis',(0.,1.,0.));
#44069=DIRECTION('ref_axis',(-0.0867961056866223,0.,-0.996226096846312));
#44070=DIRECTION('',(0.,1.,0.));
#44071=DIRECTION('center_axis',(0.,-1.,0.));
#44072=DIRECTION('ref_axis',(1.,0.,0.));
#44073=DIRECTION('center_axis',(-0.305565319408436,1.99282937676548E-7,
0.952171116750966));
#44074=DIRECTION('ref_axis',(0.673337440012041,0.70705348480321,0.216083459583719));
#44075=DIRECTION('center_axis',(-0.804623131293172,2.27430927210528E-28,
-0.593785833940127));
#44076=DIRECTION('ref_axis',(-1.82996184805045E-28,-1.,-1.3504526277748E-28));
#44077=DIRECTION('',(0.804623131293172,0.,0.593785833940126));
#44078=DIRECTION('center_axis',(-0.333863836923852,0.942595934464823,0.00691684356269561));
#44079=DIRECTION('ref_axis',(-0.166136836043399,-0.0516188462595087,-0.984750753449992));
#44080=DIRECTION('center_axis',(0.502343691929506,0.859201694775685,-0.097073492124394));
#44081=DIRECTION('ref_axis',(-0.189730325478445,-5.12579610074604E-7,-0.981836240721222));
#44082=DIRECTION('center_axis',(0.,-1.,0.));
#44083=DIRECTION('ref_axis',(0.952171177670241,0.,0.305565129578077));
#44084=DIRECTION('center_axis',(-0.305565129578077,0.,0.952171177670241));
#44085=DIRECTION('ref_axis',(0.952171177670241,0.,0.305565129578077));
#44086=DIRECTION('center_axis',(0.305565129578077,0.,-0.952171177670241));
#44087=DIRECTION('ref_axis',(-0.952171177670241,0.,-0.305565129578077));
#44088=DIRECTION('',(0.305565129578077,0.,-0.952171177670241));
#44089=DIRECTION('center_axis',(0.,-1.,0.));
#44090=DIRECTION('ref_axis',(0.,0.,-1.));
#44091=DIRECTION('',(-0.804623131293172,0.,-0.593785833940126));
#44092=DIRECTION('center_axis',(0.750531794611774,0.36046055254421,0.55386840976567));
#44093=DIRECTION('ref_axis',(0.593786291820652,-9.54831594281741E-7,-0.804622793391393));
#44094=DIRECTION('center_axis',(0.,-1.,0.));
#44095=DIRECTION('ref_axis',(-0.189730742490933,0.,-0.981836160137647));
#44096=DIRECTION('center_axis',(-1.16339964917462E-14,1.,5.14376914730547E-14));
#44097=DIRECTION('ref_axis',(-0.189730742488058,4.88498130835068E-14,-0.981836160138203));
#44098=DIRECTION('',(0.,1.,0.));
#44099=DIRECTION('center_axis',(0.802919848716691,0.065033315405924,0.592528804720985));
#44100=DIRECTION('ref_axis',(-0.377801654618901,-0.713357017301177,0.590243742562671));
#44101=DIRECTION('center_axis',(-0.593785832104614,-6.52095874072556E-8,
0.804623132647718));
#44102=DIRECTION('ref_axis',(0.799228849499735,-0.115599692127252,0.589805016346432));
#44103=DIRECTION('center_axis',(0.804623251118834,-2.01435901831212E-7,
0.593785671567542));
#44104=DIRECTION('ref_axis',(0.419901543670372,0.707053636580093,-0.568997230768397));
#44105=DIRECTION('center_axis',(-0.804623131293172,0.,-0.593785833940127));
#44106=DIRECTION('ref_axis',(0.593785833940127,0.,-0.804623131293172));
#44107=DIRECTION('',(-0.804623131293172,0.,-0.593785833940126));
#44108=DIRECTION('center_axis',(0.593785833940127,0.,-0.804623131293172));
#44109=DIRECTION('ref_axis',(0.,-1.,0.));
#44110=DIRECTION('',(-0.804623131292045,0.,-0.593785833941653));
#44111=DIRECTION('center_axis',(0.,-1.,0.));
#44112=DIRECTION('ref_axis',(0.0149833744096974,0.,-0.999887742944826));
#44113=DIRECTION('',(0.,1.,0.));
#44114=DIRECTION('center_axis',(0.,1.,0.));
#44115=DIRECTION('ref_axis',(0.0149833744096974,0.,-0.999887742944826));
#44116=DIRECTION('center_axis',(0.,-1.,0.));
#44117=DIRECTION('ref_axis',(1.,0.,0.));
#44118=DIRECTION('center_axis',(0.,1.,0.));
#44119=DIRECTION('ref_axis',(-0.952171177670241,0.,0.305565129578075));
#44120=DIRECTION('center_axis',(0.,1.,0.));
#44121=DIRECTION('ref_axis',(1.,0.,0.));
#44122=DIRECTION('',(0.,1.,0.));
#44123=DIRECTION('center_axis',(0.,-1.,0.));
#44124=DIRECTION('ref_axis',(-0.952171177838413,0.,0.305565129054036));
#44125=DIRECTION('center_axis',(0.952171177670241,0.,-0.305565129578077));
#44126=DIRECTION('ref_axis',(0.,-1.,0.));
#44127=DIRECTION('',(0.305565129578077,0.,0.952171177670241));
#44128=DIRECTION('',(0.,1.,0.));
#44129=DIRECTION('',(-0.305565129583039,0.,-0.952171177668648));
#44130=DIRECTION('center_axis',(0.,1.,0.));
#44131=DIRECTION('ref_axis',(0.184788912514002,0.,-0.982778234299016));
#44132=DIRECTION('',(0.,-1.,0.));
#44133=DIRECTION('center_axis',(0.,-1.,0.));
#44134=DIRECTION('ref_axis',(1.,0.,0.));
#44135=DIRECTION('center_axis',(0.,-1.,0.));
#44136=DIRECTION('ref_axis',(1.,0.,0.));
#44137=DIRECTION('center_axis',(-0.305565129578077,0.,-0.952171177670241));
#44138=DIRECTION('ref_axis',(0.952171177670241,0.,-0.305565129578077));
#44139=DIRECTION('center_axis',(0.982778234299016,0.,0.184788912514004));
#44140=DIRECTION('ref_axis',(0.184788912514004,0.,-0.982778234299016));
#44141=DIRECTION('center_axis',(0.,-1.,0.));
#44142=DIRECTION('ref_axis',(1.,0.,0.));
#44143=DIRECTION('center_axis',(0.,-1.,0.));
#44144=DIRECTION('ref_axis',(0.,0.,-1.));
#44145=DIRECTION('',(-0.305565129578077,0.,-0.952171177670241));
#44146=DIRECTION('center_axis',(0.,1.,0.));
#44147=DIRECTION('ref_axis',(1.,0.,0.));
#44148=DIRECTION('center_axis',(0.,-1.,0.));
#44149=DIRECTION('ref_axis',(1.,0.,0.));
#44150=DIRECTION('center_axis',(0.,1.,0.));
#44151=DIRECTION('ref_axis',(1.,0.,0.));
#44152=DIRECTION('center_axis',(-0.305565129578077,-7.88432920788926E-29,
-0.952171177670241));
#44153=DIRECTION('ref_axis',(2.4091760760449E-29,-1.,7.50723102701579E-29));
#44154=DIRECTION('',(-0.305565129578077,0.,-0.952171177670241));
#44155=DIRECTION('center_axis',(0.952171177670241,0.,-0.305565129578077));
#44156=DIRECTION('ref_axis',(0.,-1.,0.));
#44157=DIRECTION('',(-0.305565129582466,0.,-0.952171177668832));
#44158=DIRECTION('',(0.,-1.,0.));
#44159=DIRECTION('center_axis',(0.952171177669702,1.65558619039422E-11,
-0.305565129579756));
#44160=DIRECTION('ref_axis',(0.305564047343791,-0.00266148306317448,0.952167805315211));
#44161=DIRECTION('',(-0.305565129578077,0.,-0.952171177670241));
#44162=DIRECTION('center_axis',(0.,-1.,0.));
#44163=DIRECTION('ref_axis',(-0.593785833940128,0.,-0.80462313129317));
#44164=DIRECTION('center_axis',(0.,-1.,0.));
#44165=DIRECTION('ref_axis',(0.952171177741116,0.,-0.305565129357222));
#44166=DIRECTION('',(0.,-1.,0.));
#44167=DIRECTION('center_axis',(2.16551588832688E-7,-0.999999999999974,
6.99060910068197E-8));
#44168=DIRECTION('ref_axis',(0.952171197960148,1.84833326422045E-7,-0.305565066352654));
#44169=DIRECTION('center_axis',(0.593785833940127,0.,0.804623131293172));
#44170=DIRECTION('ref_axis',(0.,-1.,0.));
#44171=DIRECTION('',(-0.804623131286062,0.,0.59378583394976));
#44172=DIRECTION('',(-0.804623131293172,0.,0.593785833940126));
#44173=DIRECTION('center_axis',(0.,-1.,0.));
#44174=DIRECTION('ref_axis',(-0.952171177670241,0.,0.305565129578075));
#44175=DIRECTION('',(0.,1.,0.));
#44176=DIRECTION('center_axis',(-3.88771230906498E-14,-1.,-3.10280620461979E-14));
#44177=DIRECTION('ref_axis',(0.0867961056866264,2.22044604925032E-14,-0.996226096846311));
#44178=DIRECTION('center_axis',(0.,-1.,0.));
#44179=DIRECTION('ref_axis',(0.105128000466025,0.,-0.994458698749232));
#44180=DIRECTION('center_axis',(0.,1.,0.));
#44181=DIRECTION('ref_axis',(0.086796105653726,0.,0.996226096849178));
#44182=DIRECTION('center_axis',(0.,-1.,0.));
#44183=DIRECTION('ref_axis',(-3.7470027081099E-16,0.,1.));
#44184=DIRECTION('center_axis',(0.999100306362134,-5.17100303120544E-8,
-0.04240964309078));
#44185=DIRECTION('ref_axis',(0.0424096425034725,0.000167646473684586,0.999100292321741));
#44186=DIRECTION('center_axis',(-0.305565353050774,-2.34615214704492E-7,
-0.95217110595465));
#44187=DIRECTION('ref_axis',(0.673337494350081,-0.70705342772588,-0.216083477025519));
#44188=DIRECTION('center_axis',(-0.804623131293172,-2.27430927210528E-28,
0.593785833940127));
#44189=DIRECTION('ref_axis',(1.82996184805045E-28,-1.,-1.3504526277748E-28));
#44190=DIRECTION('',(-0.804623131293172,0.,0.593785833940126));
#44191=DIRECTION('center_axis',(0.502343691929506,-0.859201694775685,0.097073492124394));
#44192=DIRECTION('ref_axis',(0.189730325478445,-5.12579610074604E-7,-0.981836240721222));
#44193=DIRECTION('center_axis',(-0.329648236156166,-0.942184923461378,-0.0601631980633227));
#44194=DIRECTION('ref_axis',(-0.00298910007657989,0.0647664414184453,-0.997895973208993));
#44195=DIRECTION('center_axis',(0.,-1.,0.));
#44196=DIRECTION('ref_axis',(-0.952171177670241,0.,0.305565129578077));
#44197=DIRECTION('center_axis',(-0.305565129578077,0.,-0.952171177670241));
#44198=DIRECTION('ref_axis',(0.952171177670241,0.,-0.305565129578077));
#44199=DIRECTION('center_axis',(0.305565129578077,0.,0.952171177670241));
#44200=DIRECTION('ref_axis',(0.952171177670241,0.,-0.305565129578077));
#44201=DIRECTION('',(-0.305565129578077,0.,-0.952171177670241));
#44202=DIRECTION('center_axis',(0.,-1.,0.));
#44203=DIRECTION('ref_axis',(0.,0.,-1.));
#44204=DIRECTION('',(0.804623131293172,0.,-0.593785833940126));
#44205=DIRECTION('center_axis',(0.750531467332585,-0.360460652348641,-0.553868788299169));
#44206=DIRECTION('ref_axis',(-0.593786666268931,-7.74994065794043E-7,-0.80462251706041));
#44207=DIRECTION('center_axis',(0.,1.,0.));
#44208=DIRECTION('ref_axis',(0.189730742490933,0.,-0.981836160137647));
#44209=DIRECTION('',(0.,1.,0.));
#44210=DIRECTION('center_axis',(0.,-1.,0.));
#44211=DIRECTION('ref_axis',(0.18973074248807,0.,-0.9818361601382));
#44212=DIRECTION('center_axis',(0.802920300631341,-0.0650326313851214,-0.592528267417854));
#44213=DIRECTION('ref_axis',(-0.377872514273543,0.713249764055606,-0.590327991061929));
#44214=DIRECTION('center_axis',(0.804623014253252,-1.97471803256364E-7,
-0.593785992537691));
#44215=DIRECTION('ref_axis',(0.419901584175499,-0.707053568412025,0.568997285584675));
#44216=DIRECTION('center_axis',(-0.593785832104614,6.52095874072556E-8,
-0.804623132647718));
#44217=DIRECTION('ref_axis',(0.799228849499735,0.115599692127252,-0.589805016346432));
#44218=DIRECTION('center_axis',(-0.804623131293172,0.,0.593785833940127));
#44219=DIRECTION('ref_axis',(-0.593785833940127,0.,-0.804623131293172));
#44220=DIRECTION('',(0.804623131293172,0.,-0.593785833940126));
#44221=DIRECTION('center_axis',(0.593785833940127,0.,0.804623131293172));
#44222=DIRECTION('ref_axis',(0.,-1.,0.));
#44223=DIRECTION('',(0.804623131292045,0.,-0.593785833941653));
#44224=DIRECTION('center_axis',(0.52238673488493,0.,0.852708683675886));
#44225=DIRECTION('ref_axis',(0.,-1.,0.));
#44226=DIRECTION('',(-0.85270868367354,0.,0.522386734888759));
#44227=DIRECTION('',(0.,-1.,0.));
#44228=DIRECTION('',(-0.852708683675886,0.,0.52238673488493));
#44229=DIRECTION('center_axis',(-0.52238673488493,0.,0.852708683675886));
#44230=DIRECTION('ref_axis',(0.,1.,0.));
#44231=DIRECTION('',(-0.852708683675886,0.,-0.52238673488493));
#44232=DIRECTION('',(0.,1.,0.));
#44233=DIRECTION('',(-0.85270868366004,0.,-0.522386734910796));
#44234=DIRECTION('center_axis',(0.,-1.,0.));
#44235=DIRECTION('ref_axis',(-0.99973889499905,0.,0.0228504228861944));
#44236=DIRECTION('center_axis',(0.,-1.,0.));
#44237=DIRECTION('ref_axis',(1.,0.,0.));
#44238=DIRECTION('center_axis',(0.,-1.,0.));
#44239=DIRECTION('ref_axis',(-0.998419029265298,0.,-0.0562089138921914));
#44240=DIRECTION('',(0.,1.,0.));
#44241=DIRECTION('center_axis',(0.,1.,0.));
#44242=DIRECTION('ref_axis',(0.727788421795868,0.,0.685801730166876));
#44243=DIRECTION('center_axis',(0.,-1.,0.));
#44244=DIRECTION('ref_axis',(-0.928397903310364,0.,-0.371587584734636));
#44245=DIRECTION('center_axis',(0.,-1.,0.));
#44246=DIRECTION('ref_axis',(1.,0.,0.));
#44247=DIRECTION('center_axis',(0.,-1.,0.));
#44248=DIRECTION('ref_axis',(-0.985455636737957,0.,0.169932892699993));
#44249=DIRECTION('',(0.,1.,0.));
#44250=DIRECTION('center_axis',(0.,1.,0.));
#44251=DIRECTION('ref_axis',(-0.989299838612263,0.,0.145896639172227));
#44252=DIRECTION('',(0.,-1.,0.));
#44253=DIRECTION('center_axis',(0.,1.,0.));
#44254=DIRECTION('ref_axis',(1.,0.,0.));
#44255=DIRECTION('center_axis',(0.,1.,0.));
#44256=DIRECTION('ref_axis',(-0.115367964260996,0.,-0.99332282407195));
#44257=DIRECTION('',(0.,-1.,0.));
#44258=DIRECTION('center_axis',(1.93875202872386E-14,-1.,1.52293552293204E-14));
#44259=DIRECTION('ref_axis',(-0.291057680790064,-2.2204460492503E-14,-0.956705506649308));
#44260=DIRECTION('center_axis',(0.,1.,0.));
#44261=DIRECTION('ref_axis',(1.,0.,0.));
#44262=DIRECTION('center_axis',(0.,1.,0.));
#44263=DIRECTION('ref_axis',(0.291057680714125,0.,0.956705506672411));
#44264=DIRECTION('center_axis',(0.,1.,0.));
#44265=DIRECTION('ref_axis',(1.,0.,0.));
#44266=DIRECTION('',(0.,-1.,0.));
#44267=DIRECTION('center_axis',(0.,-1.,0.));
#44268=DIRECTION('ref_axis',(0.291057680796176,0.,0.956705506647449));
#44269=DIRECTION('center_axis',(-0.52238673488493,0.,0.852708683675886));
#44270=DIRECTION('ref_axis',(0.,1.,0.));
#44271=DIRECTION('',(0.852708683675886,0.,0.52238673488493));
#44272=DIRECTION('',(0.852708683677683,0.,0.522386734881996));
#44273=DIRECTION('center_axis',(0.,-1.,0.));
#44274=DIRECTION('ref_axis',(0.98929983861229,0.,-0.145896639172043));
#44275=DIRECTION('center_axis',(0.,1.,0.));
#44276=DIRECTION('ref_axis',(1.,0.,0.));
#44277=DIRECTION('center_axis',(0.,-1.,0.));
#44278=DIRECTION('ref_axis',(0.52238673496676,0.,0.852708683625755));
#44279=DIRECTION('',(0.,-1.,0.));
#44280=DIRECTION('center_axis',(0.,-1.,0.));
#44281=DIRECTION('ref_axis',(0.,0.,-1.));
#44282=DIRECTION('',(-0.852708683675886,0.,0.52238673488493));
#44283=DIRECTION('center_axis',(0.52238673488493,0.,0.852708683675886));
#44284=DIRECTION('ref_axis',(0.,-1.,0.));
#44285=DIRECTION('',(-0.852708683678698,0.,0.52238673488034));
#44286=DIRECTION('center_axis',(-1.,0.,0.));
#44287=DIRECTION('ref_axis',(0.,0.,1.));
#44288=DIRECTION('',(0.,0.,1.));
#44289=DIRECTION('',(0.,0.,-1.));
#44290=DIRECTION('center_axis',(0.,0.,-1.));
#44291=DIRECTION('ref_axis',(0.,1.,0.));
#44292=DIRECTION('',(0.,0.,1.));
#44293=DIRECTION('center_axis',(0.,-1.,0.));
#44294=DIRECTION('ref_axis',(0.,0.,-1.));
#44295=DIRECTION('',(0.,0.,1.));
#44296=DIRECTION('center_axis',(0.,0.,-1.));
#44297=DIRECTION('ref_axis',(-1.,0.,0.));
#44298=DIRECTION('',(0.,0.,1.));
#44299=DIRECTION('center_axis',(-1.,0.,0.));
#44300=DIRECTION('ref_axis',(0.,0.,1.));
#44301=DIRECTION('',(0.,0.,-1.));
#44302=DIRECTION('center_axis',(-1.,0.,0.));
#44303=DIRECTION('ref_axis',(0.,0.,1.));
#44304=DIRECTION('',(0.,0.,1.));
#44305=DIRECTION('',(0.,0.,-1.));
#44306=DIRECTION('center_axis',(0.,0.,-1.));
#44307=DIRECTION('ref_axis',(0.,1.,0.));
#44308=DIRECTION('',(0.,0.,1.));
#44309=DIRECTION('center_axis',(0.,-1.,0.));
#44310=DIRECTION('ref_axis',(0.,0.,-1.));
#44311=DIRECTION('',(0.,0.,1.));
#44312=DIRECTION('center_axis',(0.,0.,-1.));
#44313=DIRECTION('ref_axis',(-1.,0.,0.));
#44314=DIRECTION('',(0.,0.,1.));
#44315=DIRECTION('center_axis',(-1.,0.,0.));
#44316=DIRECTION('ref_axis',(0.,0.,1.));
#44317=DIRECTION('',(0.,0.,-1.));
#44318=DIRECTION('center_axis',(0.,0.,-1.));
#44319=DIRECTION('ref_axis',(1.,0.,0.));
#44320=DIRECTION('',(0.,0.,-1.));
#44321=DIRECTION('center_axis',(0.,0.,-1.));
#44322=DIRECTION('ref_axis',(1.,0.,0.));
#44323=DIRECTION('',(0.,0.,-1.));
#44324=DIRECTION('center_axis',(0.,1.,0.));
#44325=DIRECTION('ref_axis',(1.,0.,0.));
#44326=DIRECTION('center_axis',(0.,0.,-1.));
#44327=DIRECTION('ref_axis',(0.,-1.,0.));
#44328=DIRECTION('',(0.,0.,-1.));
#44329=DIRECTION('center_axis',(0.,0.,-1.));
#44330=DIRECTION('ref_axis',(0.,-1.,0.));
#44331=DIRECTION('',(0.,0.,-1.));
#44332=DIRECTION('center_axis',(0.,1.,0.));
#44333=DIRECTION('ref_axis',(1.,0.,0.));
#44334=DIRECTION('center_axis',(0.,1.,0.));
#44335=DIRECTION('ref_axis',(0.479425538604203,0.,0.877582561890373));
#44336=DIRECTION('center_axis',(2.12964451632837E-16,1.,-1.16343010175233E-16));
#44337=DIRECTION('ref_axis',(-0.479425538604191,0.,-0.877582561890379));
#44338=DIRECTION('',(0.,1.,0.));
#44339=DIRECTION('center_axis',(0.,1.,0.));
#44340=DIRECTION('ref_axis',(1.,0.,0.));
#44341=DIRECTION('center_axis',(0.,1.,0.));
#44342=DIRECTION('ref_axis',(1.,0.,0.));
#44343=DIRECTION('center_axis',(0.,1.,0.));
#44344=DIRECTION('ref_axis',(1.,0.,0.));
#44345=DIRECTION('center_axis',(0.,1.,0.));
#44346=DIRECTION('ref_axis',(1.,0.,0.));
#44347=DIRECTION('center_axis',(0.,1.,0.));
#44348=DIRECTION('ref_axis',(1.,0.,0.));
#44349=DIRECTION('center_axis',(0.,1.,0.));
#44350=DIRECTION('ref_axis',(1.,0.,0.));
#44351=DIRECTION('center_axis',(0.,1.,0.));
#44352=DIRECTION('ref_axis',(1.,0.,0.));
#44353=DIRECTION('center_axis',(0.,1.,0.));
#44354=DIRECTION('ref_axis',(0.,0.,1.));
#44355=DIRECTION('',(1.,0.,-3.55668670831951E-15));
#44356=DIRECTION('center_axis',(0.,1.,0.));
#44357=DIRECTION('ref_axis',(0.,0.,1.));
#44358=DIRECTION('',(0.500000000000001,0.,0.866025403784438));
#44359=DIRECTION('center_axis',(0.,1.,0.));
#44360=DIRECTION('ref_axis',(0.,0.,1.));
#44361=DIRECTION('',(-0.499999999999995,0.,0.866025403784442));
#44362=DIRECTION('center_axis',(0.,1.,0.));
#44363=DIRECTION('ref_axis',(0.,0.,1.));
#44364=DIRECTION('',(-1.,0.,1.05277926566258E-14));
#44365=DIRECTION('center_axis',(0.,1.,0.));
#44366=DIRECTION('ref_axis',(0.,0.,1.));
#44367=DIRECTION('',(-0.500000000000007,0.,-0.866025403784435));
#44368=DIRECTION('center_axis',(0.,1.,0.));
#44369=DIRECTION('ref_axis',(0.,0.,1.));
#44370=DIRECTION('',(0.499999999999995,0.,-0.866025403784442));
#44371=DIRECTION('center_axis',(-3.55668670831951E-15,0.,-1.));
#44372=DIRECTION('ref_axis',(-1.,0.,3.55668670831951E-15));
#44373=DIRECTION('',(0.,-1.,0.));
#44374=DIRECTION('',(0.,-1.,0.));
#44375=DIRECTION('center_axis',(0.,-1.,0.));
#44376=DIRECTION('ref_axis',(0.,0.,-1.));
#44377=DIRECTION('',(0.,-1.,0.));
#44378=DIRECTION('center_axis',(-0.866025403784442,0.,-0.499999999999995));
#44379=DIRECTION('ref_axis',(-0.499999999999995,0.,0.866025403784442));
#44380=DIRECTION('',(0.,-1.,0.));
#44381=DIRECTION('center_axis',(0.,-1.,0.));
#44382=DIRECTION('ref_axis',(0.,0.,-1.));
#44383=DIRECTION('',(0.,-1.,0.));
#44384=DIRECTION('center_axis',(0.,1.,0.));
#44385=DIRECTION('ref_axis',(0.,0.,1.));
#44386=DIRECTION('center_axis',(-0.866025403784435,0.,0.500000000000007));
#44387=DIRECTION('ref_axis',(0.500000000000007,0.,0.866025403784435));
#44388=DIRECTION('',(0.,-1.,0.));
#44389=DIRECTION('center_axis',(0.,-1.,0.));
#44390=DIRECTION('ref_axis',(0.,0.,-1.));
#44391=DIRECTION('',(0.,-1.,0.));
#44392=DIRECTION('center_axis',(0.,1.,0.));
#44393=DIRECTION('ref_axis',(0.,0.,1.));
#44394=DIRECTION('center_axis',(1.05277926566258E-14,0.,1.));
#44395=DIRECTION('ref_axis',(1.,0.,-1.05277926566258E-14));
#44396=DIRECTION('',(0.,-1.,0.));
#44397=DIRECTION('center_axis',(0.,-1.,0.));
#44398=DIRECTION('ref_axis',(0.,0.,-1.));
#44399=DIRECTION('',(0.,-1.,0.));
#44400=DIRECTION('center_axis',(0.,1.,0.));
#44401=DIRECTION('ref_axis',(0.,0.,1.));
#44402=DIRECTION('center_axis',(0.866025403784442,0.,0.499999999999995));
#44403=DIRECTION('ref_axis',(0.499999999999995,0.,-0.866025403784442));
#44404=DIRECTION('',(0.,-1.,0.));
#44405=DIRECTION('center_axis',(0.,-1.,0.));
#44406=DIRECTION('ref_axis',(0.,0.,-1.));
#44407=DIRECTION('',(0.,-1.,0.));
#44408=DIRECTION('center_axis',(0.,1.,0.));
#44409=DIRECTION('ref_axis',(0.,0.,1.));
#44410=DIRECTION('center_axis',(0.866025403784438,0.,-0.500000000000001));
#44411=DIRECTION('ref_axis',(-0.500000000000001,0.,-0.866025403784438));
#44412=DIRECTION('',(0.,-1.,0.));
#44413=DIRECTION('center_axis',(0.,-1.,0.));
#44414=DIRECTION('ref_axis',(0.,0.,-1.));
#83281=CARTESIAN_POINT('',(0.,0.,0.));
#83282=CARTESIAN_POINT('Ctrl Pts',(-11.2571565141535,-6.63753909988913,
0.));
#83283=CARTESIAN_POINT('Ctrl Pts',(-11.2571565141535,-6.63753909988913,
22.5143130283071));
#83284=CARTESIAN_POINT('Ctrl Pts',(11.2571565141535,-6.63753909988913,22.5143130283071));
#83285=CARTESIAN_POINT('Ctrl Pts',(11.2571565141535,-6.63753909988913,1.37860406925589E-15));
#83286=CARTESIAN_POINT('Ctrl Pts',(-11.2316061906402,-5.55581078583997,
0.));
#83287=CARTESIAN_POINT('Ctrl Pts',(-11.2316061906402,-5.55581078583997,
22.4632123812804));
#83288=CARTESIAN_POINT('Ctrl Pts',(11.2316061906402,-5.55581078583997,22.4632123812804));
#83289=CARTESIAN_POINT('Ctrl Pts',(11.2316061906402,-5.55581078583997,1.37547505706511E-15));
#83290=CARTESIAN_POINT('Ctrl Pts',(-11.1603664914423,-4.97414426866896,
0.));
#83291=CARTESIAN_POINT('Ctrl Pts',(-11.1603664914423,-4.97414426866896,
22.3207329828847));
#83292=CARTESIAN_POINT('Ctrl Pts',(11.1603664914423,-4.97414426866896,22.3207329828847));
#83293=CARTESIAN_POINT('Ctrl Pts',(11.1603664914423,-4.97414426866896,1.36675071010562E-15));
#83294=CARTESIAN_POINT('Ctrl Pts',(-10.527435261753,-4.27423561284,0.));
#83295=CARTESIAN_POINT('Ctrl Pts',(-10.527435261753,-4.27423561284,21.054870523506));
#83296=CARTESIAN_POINT('Ctrl Pts',(10.527435261753,-4.27423561284,21.054870523506));
#83297=CARTESIAN_POINT('Ctrl Pts',(10.527435261753,-4.27423561284,1.28923898965368E-15));
#83298=CARTESIAN_POINT('Ctrl Pts',(-10.5228448600506,-4.26915945016304,
0.));
#83299=CARTESIAN_POINT('Ctrl Pts',(-10.5228448600506,-4.26915945016304,
21.0456897201012));
#83300=CARTESIAN_POINT('Ctrl Pts',(10.5228448600506,-4.26915945016304,21.0456897201012));
#83301=CARTESIAN_POINT('Ctrl Pts',(10.5228448600506,-4.26915945016304,1.28867682757851E-15));
#83302=CARTESIAN_POINT('Ctrl Pts',(-10.5182544583482,-4.26408328748608,
0.));
#83303=CARTESIAN_POINT('Ctrl Pts',(-10.5182544583482,-4.26408328748608,
21.0365089166964));
#83304=CARTESIAN_POINT('Ctrl Pts',(10.5182544583482,-4.26408328748608,21.0365089166964));
#83305=CARTESIAN_POINT('Ctrl Pts',(10.5182544583482,-4.26408328748608,1.28811466550335E-15));
#83306=CARTESIAN_POINT('Ctrl Pts',(-10.5136640566458,-4.25900712480911,
0.));
#83307=CARTESIAN_POINT('Ctrl Pts',(-10.5136640566458,-4.25900712480911,
21.0273281132916));
#83308=CARTESIAN_POINT('Ctrl Pts',(10.5136640566458,-4.25900712480911,21.0273281132916));
#83309=CARTESIAN_POINT('Ctrl Pts',(10.5136640566458,-4.25900712480911,1.28755250342819E-15));
#83310=CARTESIAN_POINT('',(11.0953289065065,-6.63753909988913,1.90190673814221));
#83311=CARTESIAN_POINT('',(11.2571565141535,-6.63753909988913,1.37860406925589E-15));
#83312=CARTESIAN_POINT('Origin',(0.,-6.63753909988913,0.));
#83313=CARTESIAN_POINT('',(10.527435261753,-4.27423561284,1.28923898965368E-15));
#83314=CARTESIAN_POINT('Ctrl Pts',(11.2571565141535,-6.63753909988913,1.37860406925589E-15));
#83315=CARTESIAN_POINT('Ctrl Pts',(11.2316061906402,-5.55581078583997,1.37547505706511E-15));
#83316=CARTESIAN_POINT('Ctrl Pts',(11.1603664914423,-4.97414426866896,1.36675071010562E-15));
#83317=CARTESIAN_POINT('Ctrl Pts',(10.527435261753,-4.27423561284,1.28923898965368E-15));
#83318=CARTESIAN_POINT('',(-10.527435261753,-4.27423561284,0.));
#83319=CARTESIAN_POINT('Origin',(0.,-4.27423561284,0.));
#83320=CARTESIAN_POINT('',(-11.2571565141535,-6.63753909988913,0.));
#83321=CARTESIAN_POINT('Ctrl Pts',(-11.2571565141535,-6.63753909988913,
0.));
#83322=CARTESIAN_POINT('Ctrl Pts',(-11.2316061906402,-5.55581078583997,
0.));
#83323=CARTESIAN_POINT('Ctrl Pts',(-11.1603664914423,-4.97414426866896,
0.));
#83324=CARTESIAN_POINT('Ctrl Pts',(-10.527435261753,-4.27423561284,0.));
#83325=CARTESIAN_POINT('',(-11.0953289065065,-6.63753909988913,1.90190673814229));
#83326=CARTESIAN_POINT('Origin',(0.,-6.63753909988913,0.));
#83327=CARTESIAN_POINT('',(-7.19476400411325,-6.63753909988913,8.65788332730729));
#83328=CARTESIAN_POINT('Ctrl Pts',(-7.19476400411324,-6.63753909988912,
8.6578833273073));
#83329=CARTESIAN_POINT('Ctrl Pts',(-7.20793342429833,-6.25115677756972,
8.6350732224405));
#83330=CARTESIAN_POINT('Ctrl Pts',(-7.22957597298833,-5.92703963684568,
8.59758722850414));
#83331=CARTESIAN_POINT('Ctrl Pts',(-7.33264605094298,-5.48248933517018,
8.4190646167466));
#83332=CARTESIAN_POINT('Ctrl Pts',(-7.38587885165345,-5.33005160890817,
8.32686270128687));
#83333=CARTESIAN_POINT('Ctrl Pts',(-7.55351534711913,-5.02205392516935,
8.03650777393752));
#83334=CARTESIAN_POINT('Ctrl Pts',(-7.68241549558843,-4.85741613145636,
7.81324616768553));
#83335=CARTESIAN_POINT('Ctrl Pts',(-8.0780580468698,-4.55925658398769,7.12797316723002));
#83336=CARTESIAN_POINT('Ctrl Pts',(-8.29873608204807,-4.4610264457769,6.74574759818678));
#83337=CARTESIAN_POINT('Ctrl Pts',(-8.61875324812282,-4.36808225563914,
6.19146160725111));
#83338=CARTESIAN_POINT('Ctrl Pts',(-8.73033406055842,-4.34507072735131,
5.99819797096284));
#83339=CARTESIAN_POINT('Ctrl Pts',(-8.89953062521159,-4.32271936364378,
5.70514092451745));
#83340=CARTESIAN_POINT('Ctrl Pts',(-8.95774725247859,-4.31728665962078,
5.60430676824569));
#83341=CARTESIAN_POINT('Ctrl Pts',(-9.05873727376953,-4.31167125033784,
5.42938692031232));
#83342=CARTESIAN_POINT('Ctrl Pts',(-9.10160080381226,-4.31047752426154,
5.35514510848656));
#83343=CARTESIAN_POINT('Ctrl Pts',(-9.18843216468573,-4.31045476730958,
5.20474877976337));
#83344=CARTESIAN_POINT('Ctrl Pts',(-9.23245827883183,-4.31169063776259,
5.12849331320241));
#83345=CARTESIAN_POINT('Ctrl Pts',(-9.33992086438237,-4.31777109093092,
4.94236265511615));
#83346=CARTESIAN_POINT('Ctrl Pts',(-9.40346807156986,-4.32398244074387,
4.8322956635884));
#83347=CARTESIAN_POINT('Ctrl Pts',(-9.59164397495291,-4.35037319724938,
4.5063654381688));
#83348=CARTESIAN_POINT('Ctrl Pts',(-9.71718683007748,-4.37846636964579,
4.28891883456579));
#83349=CARTESIAN_POINT('Ctrl Pts',(-10.0959505184891,-4.50027701908412,
3.6328808821747));
#83350=CARTESIAN_POINT('Ctrl Pts',(-10.3416323810422,-4.63190537710756,
3.20734741373457));
#83351=CARTESIAN_POINT('Ctrl Pts',(-10.7018033055645,-4.9692390378482,2.58351307305293));
#83352=CARTESIAN_POINT('Ctrl Pts',(-10.8039037926249,-5.13032755417158,
2.40666984198668));
#83353=CARTESIAN_POINT('Ctrl Pts',(-10.9344613444127,-5.41302767928393,
2.18053752897839));
#83354=CARTESIAN_POINT('Ctrl Pts',(-10.9804393462863,-5.56176401030116,
2.10090129370282));
#83355=CARTESIAN_POINT('Ctrl Pts',(-11.0647640875135,-5.99351761929468,
1.95484655756219));
#83356=CARTESIAN_POINT('Ctrl Pts',(-11.0834813101589,-6.28993823923336,
1.92242737696384));
#83357=CARTESIAN_POINT('Ctrl Pts',(-11.0953289065065,-6.63753909988913,
1.90190673814229));
#83358=CARTESIAN_POINT('',(-3.90056490239319,-6.63753909988913,10.5597900654496));
#83359=CARTESIAN_POINT('Origin',(0.,-6.63753909988913,0.));
#83360=CARTESIAN_POINT('',(3.90056490239326,-6.63753909988913,10.5597900654496));
#83361=CARTESIAN_POINT('Ctrl Pts',(3.90056490239325,-6.63753909988913,10.5597900654496));
#83362=CARTESIAN_POINT('Ctrl Pts',(3.88650640714011,-6.43130549325031,10.5597900654496));
#83363=CARTESIAN_POINT('Ctrl Pts',(3.86750921833427,-6.24077478304519,10.5597900654496));
#83364=CARTESIAN_POINT('Ctrl Pts',(3.79603527122585,-5.88328867547875,10.5597900654496));
#83365=CARTESIAN_POINT('Ctrl Pts',(3.74111739908575,-5.70969285765482,10.5597900656594));
#83366=CARTESIAN_POINT('Ctrl Pts',(3.56226471943089,-5.38996752638001,10.5597900656594));
#83367=CARTESIAN_POINT('Ctrl Pts',(3.43858592823323,-5.23989257637326,10.5597900654496));
#83368=CARTESIAN_POINT('Ctrl Pts',(2.92900810424278,-4.84096372109964,10.5597900654496));
#83369=CARTESIAN_POINT('Ctrl Pts',(2.50413756504136,-4.6858650511529,10.5597900654496));
#83370=CARTESIAN_POINT('Ctrl Pts',(1.80048019244854,-4.48301709563196,10.5597900654496));
#83371=CARTESIAN_POINT('Ctrl Pts',(1.40703076126875,-4.41160065323694,10.5597900654496));
#83372=CARTESIAN_POINT('Ctrl Pts',(0.841933717031905,-4.34702984071186,
10.5597900654496));
#83373=CARTESIAN_POINT('Ctrl Pts',(0.658043722812898,-4.33203279124676,
10.5597900654496));
#83374=CARTESIAN_POINT('Ctrl Pts',(0.382154538654409,-4.31786065829337,
10.5597900654496));
#83375=CARTESIAN_POINT('Ctrl Pts',(0.289586349001999,-4.31451406956158,
10.5597900654496));
#83376=CARTESIAN_POINT('Ctrl Pts',(0.131799833370187,-4.31116993398485,
10.5597900654496));
#83377=CARTESIAN_POINT('Ctrl Pts',(0.0664976322661047,-4.31047485185275,
10.5597900654496));
#83378=CARTESIAN_POINT('Ctrl Pts',(-0.0639173571933893,-4.31045776213067,
10.5597900654496));
#83379=CARTESIAN_POINT('Ctrl Pts',(-0.129079361026244,-4.31113280201933,
10.5597900654496));
#83380=CARTESIAN_POINT('Ctrl Pts',(-0.286057044143298,-4.31441138123185,
10.5597900654496));
#83381=CARTESIAN_POINT('Ctrl Pts',(-0.377955322537848,-4.31769531886315,
10.5597900654496));
#83382=CARTESIAN_POINT('Ctrl Pts',(-0.651486594053972,-4.33160004901355,
10.5597900654496));
#83383=CARTESIAN_POINT('Ctrl Pts',(-0.833670646936046,-4.34630752826427,
10.5597900654496));
#83384=CARTESIAN_POINT('Ctrl Pts',(-1.3930903593616,-4.40956151168579,10.5597900654496));
#83385=CARTESIAN_POINT('Ctrl Pts',(-1.78195277809543,-4.47937544741227,
10.5597900654496));
#83386=CARTESIAN_POINT('Ctrl Pts',(-2.48599710360177,-4.67915031046562,
10.5597900654496));
#83387=CARTESIAN_POINT('Ctrl Pts',(-2.91820462596571,-4.83459622286678,
10.5597900654496));
#83388=CARTESIAN_POINT('Ctrl Pts',(-3.43432853419096,-5.23545667439743,
10.5597900654496));
#83389=CARTESIAN_POINT('Ctrl Pts',(-3.55892444433017,-5.38544981580468,
10.5597900657021));
#83390=CARTESIAN_POINT('Ctrl Pts',(-3.73882514968007,-5.70415223222546,
10.5597900657021));
#83391=CARTESIAN_POINT('Ctrl Pts',(-3.79423029833334,-5.87690202689054,
10.5597900654496));
#83392=CARTESIAN_POINT('Ctrl Pts',(-3.86701620951239,-6.23579968922602,
10.5597900654496));
#83393=CARTESIAN_POINT('Ctrl Pts',(-3.88632393679757,-6.42862871197633,
10.5597900654496));
#83394=CARTESIAN_POINT('Ctrl Pts',(-3.90056490239319,-6.63753909988913,
10.5597900654496));
#83395=CARTESIAN_POINT('',(7.1947640041133,-6.63753909988913,8.65788332730725));
#83396=CARTESIAN_POINT('Origin',(0.,-6.63753909988913,0.));
#83397=CARTESIAN_POINT('Ctrl Pts',(11.0953289065065,-6.63753909988913,1.90190673814222));
#83398=CARTESIAN_POINT('Ctrl Pts',(11.0835931462191,-6.29321943734551,1.92223367122543));
#83399=CARTESIAN_POINT('Ctrl Pts',(11.0651161129459,-5.99918609364608,1.95423683162777));
#83400=CARTESIAN_POINT('Ctrl Pts',(10.9824464115036,-5.56957898521084,2.09742495477241));
#83401=CARTESIAN_POINT('Ctrl Pts',(10.9371509020333,-5.42068513211763,2.17587907852961));
#83402=CARTESIAN_POINT('Ctrl Pts',(10.8075382554254,-5.13626438454726,2.40037476775806));
#83403=CARTESIAN_POINT('Ctrl Pts',(10.706766468623,-4.97635007968677,2.57491662246921));
#83404=CARTESIAN_POINT('Ctrl Pts',(10.3498218261676,-4.6366205362042,3.19316287869144));
#83405=CARTESIAN_POINT('Ctrl Pts',(10.102224520358,-4.50300238908698,3.62201399217098));
#83406=CARTESIAN_POINT('Ctrl Pts',(9.72143984871376,-4.37950172223957,4.2815523902022));
#83407=CARTESIAN_POINT('Ctrl Pts',(9.59502849226354,-4.3509924062512,4.50050328222767));
#83408=CARTESIAN_POINT('Ctrl Pts',(9.4056501266249,-4.32421736597006,4.82851623336816));
#83409=CARTESIAN_POINT('Ctrl Pts',(9.34174413003697,-4.31791520443557,4.93920466636667));
#83410=CARTESIAN_POINT('Ctrl Pts',(9.23384225124111,-4.3117414707732,5.12609620267325));
#83411=CARTESIAN_POINT('Ctrl Pts',(9.18973415909192,-4.31047784978131,5.20249365930066));
#83412=CARTESIAN_POINT('Ctrl Pts',(9.1028760836397,-4.31045508582793,5.35293625903157));
#83413=CARTESIAN_POINT('Ctrl Pts',(9.06006776325592,-4.31162331048586,5.42708244492296));
#83414=CARTESIAN_POINT('Ctrl Pts',(8.95941636902022,-4.31715957848669,5.60141577359183));
#83415=CARTESIAN_POINT('Ctrl Pts',(8.90148409311069,-4.32252007109623,5.70175741886524));
#83416=CARTESIAN_POINT('Ctrl Pts',(8.73325091212282,-4.34457631956746,5.99314583585518));
#83417=CARTESIAN_POINT('Ctrl Pts',(8.62236299560943,-4.36727979901887,6.18520934120182));
#83418=CARTESIAN_POINT('Ctrl Pts',(8.30433573130963,-4.45894533929482,6.73604872116122));
#83419=CARTESIAN_POINT('Ctrl Pts',(8.08539249003287,-4.55566580971443,7.11526953902639));
#83420=CARTESIAN_POINT('Ctrl Pts',(7.68947767855933,-4.85020226805387,7.80101410796761));
#83421=CARTESIAN_POINT('Ctrl Pts',(7.55829760823951,-5.01478805334236,8.02822465470201));
#83422=CARTESIAN_POINT('Ctrl Pts',(7.38777942464449,-5.32531557816686,8.32357081230295));
#83423=CARTESIAN_POINT('Ctrl Pts',(7.33403218269023,-5.47793756447169,8.41666376613443));
#83424=CARTESIAN_POINT('Ctrl Pts',(7.22979823884862,-5.92365652676787,8.59720225274137));
#83425=CARTESIAN_POINT('Ctrl Pts',(7.20800124955009,-6.24916682828626,8.63495574565847));
#83426=CARTESIAN_POINT('Ctrl Pts',(7.19476400411331,-6.63753909988913,8.65788332730724));
#83427=CARTESIAN_POINT('Origin',(0.,-14.6742356128,0.));
#83428=CARTESIAN_POINT('',(-8.34200437171315,-15.6742356128,-15.2699365768925));
#83429=CARTESIAN_POINT('',(-2.1308854305164E-15,-15.6742356128,17.4));
#83430=CARTESIAN_POINT('Origin',(0.,-15.6742356128,0.));
#83431=CARTESIAN_POINT('Origin',(0.,-15.6742356128,0.));
#83432=CARTESIAN_POINT('',(-2.00842075060166E-15,-14.6742356128,16.4));
#83433=CARTESIAN_POINT('',(-2.00842075060166E-15,-14.6742356128,16.4));
#83434=CARTESIAN_POINT('Origin',(0.,-14.6742356128,0.));
#83435=CARTESIAN_POINT('Origin',(0.,-18.0242356128,0.));
#83436=CARTESIAN_POINT('',(-2.0870381674,-16.6742356128,10.8001977615));
#83437=CARTESIAN_POINT('',(2.0870381674,-16.6742356128,10.8001977615));
#83438=CARTESIAN_POINT('Origin',(-5.49560397189452E-14,-16.6742356128,-4.21884749357559E-14));
#83439=CARTESIAN_POINT('',(2.08703816887115,-19.5762208096,10.800197769113));
#83440=CARTESIAN_POINT('',(2.0870381674,-18.0242356128,10.8001977615));
#83441=CARTESIAN_POINT('',(2.03267803765,-19.6742356128,10.8105605773));
#83442=CARTESIAN_POINT('Ctrl Pts',(2.08703816739882,-19.5762208096,10.8001977614939));
#83443=CARTESIAN_POINT('Ctrl Pts',(2.07857179402344,-19.5911991209122,10.8018331158543));
#83444=CARTESIAN_POINT('Ctrl Pts',(2.07030745035201,-19.605954198511,10.8034201368899));
#83445=CARTESIAN_POINT('Ctrl Pts',(2.0621770638366,-19.6206102877713,10.8049722242346));
#83446=CARTESIAN_POINT('Ctrl Pts',(2.05414457024727,-19.6350899121785,10.8065056238611));
#83447=CARTESIAN_POINT('Ctrl Pts',(2.04624300011735,-19.6494727516023,10.8080049411755));
#83448=CARTESIAN_POINT('Ctrl Pts',(2.03836798365886,-19.6638468112158,10.8094895879609));
#83449=CARTESIAN_POINT('Ctrl Pts',(2.03647058914484,-19.6673100753243,10.8098472965042));
#83450=CARTESIAN_POINT('Ctrl Pts',(2.03457454933455,-19.670772688533,10.8102041831093));
#83451=CARTESIAN_POINT('Ctrl Pts',(2.03267803765,-19.6742356128,10.8105605773));
#83452=CARTESIAN_POINT('',(2.03267803765,-20.5742356128,10.8105605773));
#83453=CARTESIAN_POINT('',(2.03267803765,-18.0242356128,10.8105605773));
#83454=CARTESIAN_POINT('',(-2.03267803765,-20.5742356128,10.8105605773));
#83455=CARTESIAN_POINT('Origin',(0.,-20.5742356128,0.));
#83456=CARTESIAN_POINT('',(-2.03267803765,-19.6742356128,10.8105605773));
#83457=CARTESIAN_POINT('',(-2.03267803765,-18.0242356128,10.8105605773));
#83458=CARTESIAN_POINT('',(-2.08703816887115,-19.5762208096,10.800197769113));
#83459=CARTESIAN_POINT('Ctrl Pts',(-2.08703816739882,-19.5762208096,10.8001977614939));
#83460=CARTESIAN_POINT('Ctrl Pts',(-2.07851836458347,-19.5912936327508,
10.8018434362202));
#83461=CARTESIAN_POINT('Ctrl Pts',(-2.07020057505286,-19.6061447702175,
10.803440661169));
#83462=CARTESIAN_POINT('Ctrl Pts',(-2.06201879505428,-19.6208943062105,
10.8050024359317));
#83463=CARTESIAN_POINT('Ctrl Pts',(-2.05455817949112,-19.6343437778167,
10.8064265516013));
#83464=CARTESIAN_POINT('Ctrl Pts',(-2.04721036756645,-19.6477083057653,
10.8078212728186));
#83465=CARTESIAN_POINT('Ctrl Pts',(-2.03989637952827,-19.6610552454502,
10.8092013212638));
#83466=CARTESIAN_POINT('Ctrl Pts',(-2.03748869684149,-19.6654489080366,
10.8096556177066));
#83467=CARTESIAN_POINT('Ctrl Pts',(-2.03508470198871,-19.6698411784241,
10.8101083147612));
#83468=CARTESIAN_POINT('Ctrl Pts',(-2.03267803765,-19.6742356128,10.8105605773));
#83469=CARTESIAN_POINT('',(-2.0870381674,-18.7742356128,10.8001977615));
#83470=CARTESIAN_POINT('Origin',(0.,-4.27423561284,11.15));
#83471=CARTESIAN_POINT('Origin',(0.,-4.27423561284,0.));
#83472=CARTESIAN_POINT('',(-4.38674367823,-4.27423561284,-8.0298804413));
#83473=CARTESIAN_POINT('Origin',(0.,-4.27423561284,0.));
#83474=CARTESIAN_POINT('Origin',(0.,-32.7742356128,2.4));
#83475=CARTESIAN_POINT('',(-16.2234398325,-32.7742356128,2.4));
#83476=CARTESIAN_POINT('',(-17.2336879396,-32.7742356128,2.4));
#83477=CARTESIAN_POINT('',(-16.7285638861,-32.7742356128,2.4));
#83478=CARTESIAN_POINT('',(-17.2336879396,-32.7742356128,-2.4));
#83479=CARTESIAN_POINT('Origin',(0.,-32.7742356128,0.));
#83480=CARTESIAN_POINT('',(-16.2234398325,-32.7742356128,-2.4));
#83481=CARTESIAN_POINT('',(-16.7285638861,-32.7742356128,-2.4));
#83482=CARTESIAN_POINT('Origin',(0.,-32.7742356128,0.));
#83483=CARTESIAN_POINT('Origin',(0.,-34.4742356128,-2.4));
#83484=CARTESIAN_POINT('',(-16.2234398325,-34.4742356128,-2.4));
#83485=CARTESIAN_POINT('',(-16.2234398325,-27.9742356128,-2.4));
#83486=CARTESIAN_POINT('',(-17.2336879396,-34.4742356128,-2.4));
#83487=CARTESIAN_POINT('',(-17.2336879396,-26.9742356128,-2.4));
#83488=CARTESIAN_POINT('',(-16.7285638861,-34.4742356128,-2.4));
#83489=CARTESIAN_POINT('Origin',(0.,-34.4742356128,2.4));
#83490=CARTESIAN_POINT('',(-16.2234398325,-34.4742356128,2.4));
#83491=CARTESIAN_POINT('',(-17.2336879396,-34.4742356128,2.4));
#83492=CARTESIAN_POINT('',(-16.7285638861,-34.4742356128,2.4));
#83493=CARTESIAN_POINT('',(-17.2336879396,-26.9742356128,2.4));
#83494=CARTESIAN_POINT('',(-16.2234398325,-27.9742356128,2.4));
#83495=CARTESIAN_POINT('Origin',(0.,-34.4742356128,-2.4));
#83496=CARTESIAN_POINT('Origin',(0.,-34.4742356128,0.));
#83497=CARTESIAN_POINT('Origin',(0.,-34.4742356128,0.));
#83498=CARTESIAN_POINT('Origin',(0.,-32.7742356128,2.4));
#83499=CARTESIAN_POINT('',(17.2336879396,-32.7742356128,-2.4));
#83500=CARTESIAN_POINT('',(16.2234398325,-32.7742356128,-2.4));
#83501=CARTESIAN_POINT('',(16.7285638861,-32.7742356128,-2.4));
#83502=CARTESIAN_POINT('',(17.2336879396,-32.7742356128,2.4));
#83503=CARTESIAN_POINT('Origin',(0.,-32.7742356128,0.));
#83504=CARTESIAN_POINT('',(16.2234398325,-32.7742356128,2.4));
#83505=CARTESIAN_POINT('',(16.7285638861,-32.7742356128,2.4));
#83506=CARTESIAN_POINT('Origin',(0.,-32.7742356128,0.));
#83507=CARTESIAN_POINT('Origin',(0.,-34.4742356128,2.4));
#83508=CARTESIAN_POINT('',(17.2336879396,-34.4742356128,2.4));
#83509=CARTESIAN_POINT('',(17.2336879396,-26.9742356128,2.4));
#83510=CARTESIAN_POINT('',(16.2234398325,-34.4742356128,2.4));
#83511=CARTESIAN_POINT('',(16.7285638861,-34.4742356128,2.4));
#83512=CARTESIAN_POINT('',(16.2234398325,-27.9742356128,2.4));
#83513=CARTESIAN_POINT('Origin',(0.,-34.4742356128,-2.4));
#83514=CARTESIAN_POINT('',(16.2234398325,-34.4742356128,-2.4));
#83515=CARTESIAN_POINT('',(16.2234398325,-27.9742356128,-2.4));
#83516=CARTESIAN_POINT('',(17.2336879396,-34.4742356128,-2.4));
#83517=CARTESIAN_POINT('',(16.7285638861,-34.4742356128,-2.4));
#83518=CARTESIAN_POINT('',(17.2336879396,-26.9742356128,-2.4));
#83519=CARTESIAN_POINT('Origin',(0.,-34.4742356128,-2.4));
#83520=CARTESIAN_POINT('Origin',(0.,-34.4742356128,0.));
#83521=CARTESIAN_POINT('Origin',(0.,-34.4742356128,0.));
#83522=CARTESIAN_POINT('Origin',(0.,-21.7742356128,0.));
#83523=CARTESIAN_POINT('',(-4.5,-39.2742356128,15.7705421594));
#83524=CARTESIAN_POINT('',(-7.86257883310895,-39.2742356128016,-14.3923540150021));
#83525=CARTESIAN_POINT('Origin',(0.,-39.2742356128,0.));
#83526=CARTESIAN_POINT('',(-7.86257883310895,-16.6742356128,-14.3923540150021));
#83527=CARTESIAN_POINT('',(-7.86257883310895,-21.7742356128,-14.3923540150021));
#83528=CARTESIAN_POINT('',(-15.9289440371,-16.6742356128,-3.90240206319));
#83529=CARTESIAN_POINT('Origin',(1.22124532708767E-14,-16.6742356128,-4.44089209850063E-15));
#83530=CARTESIAN_POINT('',(-15.9289440371,-19.3742356128,-3.90240206319));
#83531=CARTESIAN_POINT('',(-15.9289440371,-18.0242356128,-3.90240206319));
#83532=CARTESIAN_POINT('',(-16.2336455538,-19.3742356128,-2.32996824702));
#83533=CARTESIAN_POINT('Origin',(0.,-19.3742356128,0.));
#83534=CARTESIAN_POINT('',(-16.2336455538,-16.6742356128,-2.32996824702));
#83535=CARTESIAN_POINT('',(-16.2336455538,-18.0242356128,-2.32996824702));
#83536=CARTESIAN_POINT('',(-16.2336455538,-16.6742356128,2.32996824702));
#83537=CARTESIAN_POINT('Origin',(3.5527136788005E-14,-16.6742356128,-2.91433543964104E-14));
#83538=CARTESIAN_POINT('',(-16.2336455538,-19.3742356128,2.32996824702));
#83539=CARTESIAN_POINT('',(-16.2336455538,-18.0242356128,2.32996824702));
#83540=CARTESIAN_POINT('',(-15.9289440371,-19.3742356128,3.90240206319));
#83541=CARTESIAN_POINT('Origin',(0.,-19.3742356128,0.));
#83542=CARTESIAN_POINT('',(-15.9289440371,-16.6742356128,3.90240206319));
#83543=CARTESIAN_POINT('',(-15.9289440371,-18.0242356128,3.90240206319));
#83544=CARTESIAN_POINT('',(-7.49224433422,-16.6742356128,14.5885665792));
#83545=CARTESIAN_POINT('Origin',(-8.88178419700125E-15,-16.6742356128,3.44169137633799E-14));
#83546=CARTESIAN_POINT('',(-7.49224433422,-19.0742356128,14.5885665792));
#83547=CARTESIAN_POINT('',(-7.49224433422,-17.8742356128,14.5885665792));
#83548=CARTESIAN_POINT('',(-7.19123109516,-19.3742356128,14.739273908));
#83549=CARTESIAN_POINT('Ctrl Pts',(-7.19123109512951,-19.3742356128,14.7392739080473));
#83550=CARTESIAN_POINT('Ctrl Pts',(-7.22952132866876,-19.3742356127946,
14.7205922606481));
#83551=CARTESIAN_POINT('Ctrl Pts',(-7.27057773529867,-19.3666953834606,
14.7003573162235));
#83552=CARTESIAN_POINT('Ctrl Pts',(-7.34666159172428,-19.3348937450062,
14.6624816891679));
#83553=CARTESIAN_POINT('Ctrl Pts',(-7.38168615217903,-19.3106128070347,
14.6448516028746));
#83554=CARTESIAN_POINT('Ctrl Pts',(-7.43385501333582,-19.2559632146065,
14.618431778239));
#83555=CARTESIAN_POINT('Ctrl Pts',(-7.45563951291232,-19.2234139907703,
14.6073169516831));
#83556=CARTESIAN_POINT('Ctrl Pts',(-7.48484529484258,-19.1512739974414,
14.5923733499151));
#83557=CARTESIAN_POINT('Ctrl Pts',(-7.4922443341904,-19.111669668748,14.5885665792357));
#83558=CARTESIAN_POINT('Ctrl Pts',(-7.4922443341904,-19.0742356128,14.5885665792357));
#83559=CARTESIAN_POINT('',(-6.24926904222,-19.3742356128,15.1626724702));
#83560=CARTESIAN_POINT('Origin',(0.,-19.3742356128,0.));
#83561=CARTESIAN_POINT('',(-5.92151655781,-19.0742356128,15.2936471012));
#83562=CARTESIAN_POINT('Ctrl Pts',(-5.92151655783295,-19.0742356128,15.293647101176));
#83563=CARTESIAN_POINT('Ctrl Pts',(-5.92151655783295,-19.1116715424785,
15.293647101176));
#83564=CARTESIAN_POINT('Ctrl Pts',(-5.92976192802622,-19.1510542471533,
15.2904615732935));
#83565=CARTESIAN_POINT('Ctrl Pts',(-5.96159367196029,-19.2224116359375,
15.2780788235699));
#83566=CARTESIAN_POINT('Ctrl Pts',(-5.98511656924299,-19.2544169262194,
15.2688949021608));
#83567=CARTESIAN_POINT('Ctrl Pts',(-6.04180004067785,-19.309437956177,15.2465652051803));
#83568=CARTESIAN_POINT('Ctrl Pts',(-6.08040370020595,-19.3341462543713,
15.2312408052802));
#83569=CARTESIAN_POINT('Ctrl Pts',(-6.16349766956827,-19.3665421888705,
15.1978058318927));
#83570=CARTESIAN_POINT('Ctrl Pts',(-6.20798298226436,-19.3742356128,15.1796884478622));
#83571=CARTESIAN_POINT('Ctrl Pts',(-6.24926904224182,-19.3742356128,15.1626724701709));
#83572=CARTESIAN_POINT('',(-5.92151655781,-16.6742356128,15.2936471012));
#83573=CARTESIAN_POINT('',(-5.92151655781,-18.0242356128,15.2936471012));
#83574=CARTESIAN_POINT('',(-1.02442996075,-16.6742356128,16.3679730955));
#83575=CARTESIAN_POINT('Origin',(-1.18793863634892E-13,-16.6742356128,3.99680288865056E-14));
#83576=CARTESIAN_POINT('',(-1.02442996075,-20.5742356128,16.3679730955));
#83577=CARTESIAN_POINT('',(-1.02442996075,-18.7742356128,16.3679730955));
#83578=CARTESIAN_POINT('',(-0.703933081317,-20.8742356128,16.3848856638));
#83579=CARTESIAN_POINT('Ctrl Pts',(-0.703933081313263,-20.8742356128,16.3848856638377));
#83580=CARTESIAN_POINT('Ctrl Pts',(-0.74430255434404,-20.8742356127994,
16.3831512966822));
#83581=CARTESIAN_POINT('Ctrl Pts',(-0.787517237531629,-20.8666318008058,
16.3811299589766));
#83582=CARTESIAN_POINT('Ctrl Pts',(-0.867468556859285,-20.8352672300064,
16.377090719509));
#83583=CARTESIAN_POINT('Ctrl Pts',(-0.904202386296281,-20.8114982977688,
16.3750807377873));
#83584=CARTESIAN_POINT('Ctrl Pts',(-0.96040637329737,-20.7575520580267,
16.371876958888));
#83585=CARTESIAN_POINT('Ctrl Pts',(-0.984367443611667,-20.7245301270092,
16.3704391530226));
#83586=CARTESIAN_POINT('Ctrl Pts',(-1.01639053666175,-20.6516587395374,
16.3684821411247));
#83587=CARTESIAN_POINT('Ctrl Pts',(-1.02442996074781,-20.6117990817782,
16.3679730955156));
#83588=CARTESIAN_POINT('Ctrl Pts',(-1.02442996074781,-20.5742356128,16.3679730955156));
#83589=CARTESIAN_POINT('',(0.703933081317,-20.8742356128,16.3848856638));
#83590=CARTESIAN_POINT('Origin',(0.,-20.8742356128,0.));
#83591=CARTESIAN_POINT('',(1.02442996075,-20.5742356128,16.3679730955));
#83592=CARTESIAN_POINT('Ctrl Pts',(0.703933081313263,-20.8742356128,16.3848856638377));
#83593=CARTESIAN_POINT('Ctrl Pts',(0.74430255434404,-20.8742356127994,16.3831512966822));
#83594=CARTESIAN_POINT('Ctrl Pts',(0.787517237531627,-20.8666318008058,
16.3811299589766));
#83595=CARTESIAN_POINT('Ctrl Pts',(0.867468556859283,-20.8352672300064,
16.377090719509));
#83596=CARTESIAN_POINT('Ctrl Pts',(0.904202386296281,-20.8114982977688,
16.3750807377873));
#83597=CARTESIAN_POINT('Ctrl Pts',(0.96040637329737,-20.7575520580267,16.371876958888));
#83598=CARTESIAN_POINT('Ctrl Pts',(0.984367443611667,-20.7245301270092,
16.3704391530226));
#83599=CARTESIAN_POINT('Ctrl Pts',(1.01639053666175,-20.6516587395374,16.3684821411247));
#83600=CARTESIAN_POINT('Ctrl Pts',(1.02442996074781,-20.6117990817782,16.3679730955156));
#83601=CARTESIAN_POINT('Ctrl Pts',(1.02442996074781,-20.5742356128,16.3679730955156));
#83602=CARTESIAN_POINT('',(1.02442996075,-16.6742356128,16.3679730955));
#83603=CARTESIAN_POINT('',(1.02442996075,-18.7742356128,16.3679730955));
#83604=CARTESIAN_POINT('',(5.92151655781,-16.6742356128,15.2936471012));
#83605=CARTESIAN_POINT('Origin',(-1.0172418463128E-13,-16.6742356128,-8.21565038222616E-14));
#83606=CARTESIAN_POINT('',(5.92151655781,-19.0742356128,15.2936471012));
#83607=CARTESIAN_POINT('',(5.92151655781,-18.0242356128,15.2936471012));
#83608=CARTESIAN_POINT('',(6.24926904222,-19.3742356128,15.1626724702));
#83609=CARTESIAN_POINT('Ctrl Pts',(5.92151655783295,-19.0742356128,15.293647101176));
#83610=CARTESIAN_POINT('Ctrl Pts',(5.92151655783295,-19.1116715424785,15.293647101176));
#83611=CARTESIAN_POINT('Ctrl Pts',(5.92976192802622,-19.1510542471533,15.2904615732935));
#83612=CARTESIAN_POINT('Ctrl Pts',(5.96159367196029,-19.2224116359375,15.2780788235699));
#83613=CARTESIAN_POINT('Ctrl Pts',(5.985116569243,-19.2544169262194,15.2688949021608));
#83614=CARTESIAN_POINT('Ctrl Pts',(6.04180004067786,-19.309437956177,15.2465652051803));
#83615=CARTESIAN_POINT('Ctrl Pts',(6.08040370020595,-19.3341462543713,15.2312408052802));
#83616=CARTESIAN_POINT('Ctrl Pts',(6.16349766956827,-19.3665421888705,15.1978058318927));
#83617=CARTESIAN_POINT('Ctrl Pts',(6.20798298226436,-19.3742356128,15.1796884478622));
#83618=CARTESIAN_POINT('Ctrl Pts',(6.24926904224182,-19.3742356128,15.1626724701709));
#83619=CARTESIAN_POINT('',(7.19123109516,-19.3742356128,14.739273908));
#83620=CARTESIAN_POINT('Origin',(0.,-19.3742356128,0.));
#83621=CARTESIAN_POINT('',(7.49224433422,-19.0742356128,14.5885665792));
#83622=CARTESIAN_POINT('Ctrl Pts',(7.19123109512951,-19.3742356128,14.7392739080473));
#83623=CARTESIAN_POINT('Ctrl Pts',(7.22952132866876,-19.3742356127946,14.7205922606481));
#83624=CARTESIAN_POINT('Ctrl Pts',(7.27057773529867,-19.3666953834606,14.7003573162235));
#83625=CARTESIAN_POINT('Ctrl Pts',(7.34666159172428,-19.3348937450062,14.6624816891679));
#83626=CARTESIAN_POINT('Ctrl Pts',(7.38168615217903,-19.3106128070347,14.6448516028746));
#83627=CARTESIAN_POINT('Ctrl Pts',(7.43385501333582,-19.2559632146065,14.618431778239));
#83628=CARTESIAN_POINT('Ctrl Pts',(7.45563951291232,-19.2234139907703,14.6073169516831));
#83629=CARTESIAN_POINT('Ctrl Pts',(7.48484529484258,-19.1512739974414,14.5923733499151));
#83630=CARTESIAN_POINT('Ctrl Pts',(7.4922443341904,-19.111669668748,14.5885665792357));
#83631=CARTESIAN_POINT('Ctrl Pts',(7.4922443341904,-19.0742356128,14.5885665792357));
#83632=CARTESIAN_POINT('',(7.49224433422,-16.6742356128,14.5885665792));
#83633=CARTESIAN_POINT('',(7.49224433422,-17.8742356128,14.5885665792));
#83634=CARTESIAN_POINT('',(15.9289440371,-16.6742356128,3.90240206319));
#83635=CARTESIAN_POINT('Origin',(5.36126698591488E-12,-16.6742356128,1.11088915843993E-11));
#83636=CARTESIAN_POINT('',(15.9289440371,-19.3742356128,3.90240206319));
#83637=CARTESIAN_POINT('',(15.9289440371,-18.0242356128,3.90240206319));
#83638=CARTESIAN_POINT('',(16.2336455538,-19.3742356128,2.32996824702));
#83639=CARTESIAN_POINT('Origin',(0.,-19.3742356128,0.));
#83640=CARTESIAN_POINT('',(16.2336455538,-16.6742356128,2.32996824702));
#83641=CARTESIAN_POINT('',(16.2336455538,-18.0242356128,2.32996824702));
#83642=CARTESIAN_POINT('',(16.2336455538,-16.6742356128,-2.32996824702));
#83643=CARTESIAN_POINT('Origin',(1.90958360235527E-13,-16.6742356128,5.16253706450698E-14));
#83644=CARTESIAN_POINT('',(16.2336455538,-19.3742356128,-2.32996824702));
#83645=CARTESIAN_POINT('',(16.2336455538,-18.0242356128,-2.32996824702));
#83646=CARTESIAN_POINT('',(15.9289440371,-19.3742356128,-3.90240206319));
#83647=CARTESIAN_POINT('Origin',(0.,-19.3742356128,0.));
#83648=CARTESIAN_POINT('',(15.9289440371,-16.6742356128,-3.90240206319));
#83649=CARTESIAN_POINT('',(15.9289440371,-18.0242356128,-3.90240206319));
#83650=CARTESIAN_POINT('Origin',(1.22124532708767E-14,-16.6742356128,-4.44089209850063E-15));
#83651=CARTESIAN_POINT('',(-5.5,-39.2742356128,-15.4502427165));
#83652=CARTESIAN_POINT('Origin',(0.,-39.2742356128,0.));
#83653=CARTESIAN_POINT('',(-5.,-38.7742356128,-15.6192189305));
#83654=CARTESIAN_POINT('Ctrl Pts',(-5.,-38.7742356128,-15.6192189305355));
#83655=CARTESIAN_POINT('Ctrl Pts',(-5.,-38.8368018315904,-15.6192189305355));
#83656=CARTESIAN_POINT('Ctrl Pts',(-5.01248103067696,-38.9033171525403,
-15.6152401633624));
#83657=CARTESIAN_POINT('Ctrl Pts',(-5.06252926091632,-39.0251462300073,
-15.5990861568434));
#83658=CARTESIAN_POINT('Ctrl Pts',(-5.10007609417628,-39.0804660078343,
-15.5868932416425));
#83659=CARTESIAN_POINT('Ctrl Pts',(-5.18809492268901,-39.1703688520033,
-15.5578261400603));
#83660=CARTESIAN_POINT('Ctrl Pts',(-5.24538280864814,-39.2098107413741,
-15.5386709530016));
#83661=CARTESIAN_POINT('Ctrl Pts',(-5.3699886467473,-39.2617319238639,-15.4960497459829));
#83662=CARTESIAN_POINT('Ctrl Pts',(-5.43729042387462,-39.2742356128,-15.4725661631692));
#83663=CARTESIAN_POINT('Ctrl Pts',(-5.5,-39.2742356128,-15.4502427165401));
#83664=CARTESIAN_POINT('',(-5.,-35.2742356128,-15.6192189305));
#83665=CARTESIAN_POINT('',(-5.,-37.0242356128,-15.6192189305));
#83666=CARTESIAN_POINT('',(-4.,-34.2742356128,-15.9047162817));
#83667=CARTESIAN_POINT('Ctrl Pts',(-5.,-35.2742356128,-15.6192189305355));
#83668=CARTESIAN_POINT('Ctrl Pts',(-5.,-35.1487422268978,-15.6192189305355));
#83669=CARTESIAN_POINT('Ctrl Pts',(-4.97490968370107,-35.0153658897602,
-15.6273177607417));
#83670=CARTESIAN_POINT('Ctrl Pts',(-4.87420273104728,-34.7710139518027,
-15.6590208655925));
#83671=CARTESIAN_POINT('Ctrl Pts',(-4.79862638132674,-34.6600074810144,
-15.6825150669345));
#83672=CARTESIAN_POINT('Ctrl Pts',(-4.62282043142789,-34.4815119728997,
-15.7352562259596));
#83673=CARTESIAN_POINT('Ctrl Pts',(-4.50949514531374,-34.4033230413762,
-15.7683552560566));
#83674=CARTESIAN_POINT('Ctrl Pts',(-4.26139179450132,-34.2996852813123,
-15.837206632462));
#83675=CARTESIAN_POINT('Ctrl Pts',(-4.126591817014,-34.2742356128,-15.8728787273686));
#83676=CARTESIAN_POINT('Ctrl Pts',(-4.,-34.2742356128,-15.9047162816568));
#83677=CARTESIAN_POINT('',(4.,-34.2742356128,-15.9047162817));
#83678=CARTESIAN_POINT('Origin',(0.,-34.2742356128,0.));
#83679=CARTESIAN_POINT('',(5.,-35.2742356128,-15.6192189305));
#83680=CARTESIAN_POINT('Ctrl Pts',(4.,-34.2742356128,-15.9047162816568));
#83681=CARTESIAN_POINT('Ctrl Pts',(4.12659181701402,-34.2742356127987,-15.8728787273687));
#83682=CARTESIAN_POINT('Ctrl Pts',(4.26139179450132,-34.2996852813123,-15.837206632462));
#83683=CARTESIAN_POINT('Ctrl Pts',(4.50949514531374,-34.4033230413762,-15.7683552560566));
#83684=CARTESIAN_POINT('Ctrl Pts',(4.62282043142789,-34.4815119728997,-15.7352562259596));
#83685=CARTESIAN_POINT('Ctrl Pts',(4.79862638132674,-34.6600074810144,-15.6825150669345));
#83686=CARTESIAN_POINT('Ctrl Pts',(4.87420273104728,-34.7710139518027,-15.6590208655925));
#83687=CARTESIAN_POINT('Ctrl Pts',(4.97490968370107,-35.0153658897602,-15.6273177607417));
#83688=CARTESIAN_POINT('Ctrl Pts',(5.,-35.1487422268978,-15.6192189305355));
#83689=CARTESIAN_POINT('Ctrl Pts',(5.,-35.2742356128,-15.6192189305355));
#83690=CARTESIAN_POINT('',(5.,-38.7742356128,-15.6192189305));
#83691=CARTESIAN_POINT('',(5.,-37.0242356128,-15.6192189305));
#83692=CARTESIAN_POINT('',(5.5,-39.2742356128,-15.4502427165));
#83693=CARTESIAN_POINT('Ctrl Pts',(5.5,-39.2742356128,-15.4502427165401));
#83694=CARTESIAN_POINT('Ctrl Pts',(5.43729042387464,-39.2742356128016,-15.4725661631693));
#83695=CARTESIAN_POINT('Ctrl Pts',(5.3699886467473,-39.2617319238639,-15.4960497459829));
#83696=CARTESIAN_POINT('Ctrl Pts',(5.24538280864814,-39.2098107413741,-15.5386709530016));
#83697=CARTESIAN_POINT('Ctrl Pts',(5.18809492268901,-39.1703688520033,-15.5578261400603));
#83698=CARTESIAN_POINT('Ctrl Pts',(5.10007609417628,-39.0804660078343,-15.5868932416425));
#83699=CARTESIAN_POINT('Ctrl Pts',(5.06252926091632,-39.0251462300073,-15.5990861568434));
#83700=CARTESIAN_POINT('Ctrl Pts',(5.01248103067696,-38.9033171525403,-15.6152401633624));
#83701=CARTESIAN_POINT('Ctrl Pts',(5.,-38.8368018315904,-15.6192189305355));
#83702=CARTESIAN_POINT('Ctrl Pts',(5.,-38.7742356128,-15.6192189305355));
#83703=CARTESIAN_POINT('',(4.5,-39.2742356128,15.7705421594));
#83704=CARTESIAN_POINT('Origin',(0.,-39.2742356128,0.));
#83705=CARTESIAN_POINT('',(4.,-38.7742356128,15.9047162817));
#83706=CARTESIAN_POINT('Ctrl Pts',(4.,-38.7742356128,15.9047162816568));
#83707=CARTESIAN_POINT('Ctrl Pts',(4.,-38.836872188068,15.9047162816568));
#83708=CARTESIAN_POINT('Ctrl Pts',(4.01250244639384,-38.9035481102566,15.9015879733306));
#83709=CARTESIAN_POINT('Ctrl Pts',(4.06290022618683,-39.0258690198089,15.8887859105305));
#83710=CARTESIAN_POINT('Ctrl Pts',(4.10078344949377,-39.0815169257637,15.8790923795176));
#83711=CARTESIAN_POINT('Ctrl Pts',(4.18908794953576,-39.1710308075913,15.8560306789731));
#83712=CARTESIAN_POINT('Ctrl Pts',(4.24601666452162,-39.2101357988612,15.8409431205528));
#83713=CARTESIAN_POINT('Ctrl Pts',(4.37012998316081,-39.2617294942499,15.8071534564237));
#83714=CARTESIAN_POINT('Ctrl Pts',(4.43730220859644,-39.2742356128,15.7884324803388));
#83715=CARTESIAN_POINT('Ctrl Pts',(4.5,-39.2742356128,15.7705421593552));
#83716=CARTESIAN_POINT('',(4.,-35.2742356128,15.9047162817));
#83717=CARTESIAN_POINT('',(4.,-36.7742356128,15.9047162817));
#83718=CARTESIAN_POINT('',(3.,-34.2742356128,16.1232751015));
#83719=CARTESIAN_POINT('Ctrl Pts',(4.,-35.2742356128,15.9047162816568));
#83720=CARTESIAN_POINT('Ctrl Pts',(4.,-35.1486858517753,15.9047162816568));
#83721=CARTESIAN_POINT('Ctrl Pts',(3.97489679058695,-35.0150679349663,15.9110940851556));
#83722=CARTESIAN_POINT('Ctrl Pts',(3.87362953483757,-34.7698913888191,15.9360507557735));
#83723=CARTESIAN_POINT('Ctrl Pts',(3.79749048511181,-34.6583124843852,15.9545317615642));
#83724=CARTESIAN_POINT('Ctrl Pts',(3.62103634952688,-34.4802687438727,15.9955146214762));
#83725=CARTESIAN_POINT('Ctrl Pts',(3.50813186616486,-34.4025975216227,16.0208922692526));
#83726=CARTESIAN_POINT('Ctrl Pts',(3.26076324768218,-34.2995800372216,16.0730644662099));
#83727=CARTESIAN_POINT('Ctrl Pts',(3.12628134821427,-34.2742356128,16.0997783837685));
#83728=CARTESIAN_POINT('Ctrl Pts',(3.,-34.2742356128,16.1232751015419));
#83729=CARTESIAN_POINT('',(-3.,-34.2742356128,16.1232751015));
#83730=CARTESIAN_POINT('Origin',(0.,-34.2742356128,0.));
#83731=CARTESIAN_POINT('',(-4.,-35.2742356128,15.9047162817));
#83732=CARTESIAN_POINT('Ctrl Pts',(-3.,-34.2742356128,16.1232751015419));
#83733=CARTESIAN_POINT('Ctrl Pts',(-3.12628134821426,-34.274235612801,16.0997783837685));
#83734=CARTESIAN_POINT('Ctrl Pts',(-3.26076324768218,-34.2995800372216,
16.0730644662099));
#83735=CARTESIAN_POINT('Ctrl Pts',(-3.50813186616486,-34.4025975216227,
16.0208922692526));
#83736=CARTESIAN_POINT('Ctrl Pts',(-3.62103634952688,-34.4802687438727,
15.9955146214762));
#83737=CARTESIAN_POINT('Ctrl Pts',(-3.79749048511181,-34.6583124843852,
15.9545317615642));
#83738=CARTESIAN_POINT('Ctrl Pts',(-3.87362953483757,-34.7698913888191,
15.9360507557735));
#83739=CARTESIAN_POINT('Ctrl Pts',(-3.97489679058695,-35.0150679349663,
15.9110940851556));
#83740=CARTESIAN_POINT('Ctrl Pts',(-4.,-35.1486858517753,15.9047162816568));
#83741=CARTESIAN_POINT('Ctrl Pts',(-4.,-35.2742356128,15.9047162816568));
#83742=CARTESIAN_POINT('',(-4.,-38.7742356128,15.9047162817));
#83743=CARTESIAN_POINT('',(-4.,-36.7742356128,15.9047162817));
#83744=CARTESIAN_POINT('Ctrl Pts',(-4.5,-39.2742356128,15.7705421593552));
#83745=CARTESIAN_POINT('Ctrl Pts',(-4.43730220859643,-39.2742356127985,
15.7884324803387));
#83746=CARTESIAN_POINT('Ctrl Pts',(-4.37012998316081,-39.2617294942499,
15.8071534564237));
#83747=CARTESIAN_POINT('Ctrl Pts',(-4.24601666452162,-39.2101357988612,
15.8409431205528));
#83748=CARTESIAN_POINT('Ctrl Pts',(-4.18908794953576,-39.1710308075913,
15.8560306789731));
#83749=CARTESIAN_POINT('Ctrl Pts',(-4.10078344949377,-39.0815169257637,
15.8790923795176));
#83750=CARTESIAN_POINT('Ctrl Pts',(-4.06290022618683,-39.0258690198089,
15.8887859105305));
#83751=CARTESIAN_POINT('Ctrl Pts',(-4.01250244639384,-38.9035481102566,
15.9015879733306));
#83752=CARTESIAN_POINT('Ctrl Pts',(-4.,-38.836872188068,15.9047162816568));
#83753=CARTESIAN_POINT('Ctrl Pts',(-4.,-38.7742356128,15.9047162816568));
#83754=CARTESIAN_POINT('Origin',(0.,-21.7742356128,0.));
#83755=CARTESIAN_POINT('',(-8.34200437171315,-39.2742356128003,-15.2699365768925));
#83756=CARTESIAN_POINT('',(-8.34200437171315,-21.7742356128,-15.2699365768925));
#83757=CARTESIAN_POINT('',(-4.5,-39.2742356128,16.8080337934));
#83758=CARTESIAN_POINT('Origin',(0.,-39.2742356128,0.));
#83759=CARTESIAN_POINT('',(-4.,-38.7742356128,16.9339894886));
#83760=CARTESIAN_POINT('Ctrl Pts',(-4.,-38.7742356128,16.9339894885996));
#83761=CARTESIAN_POINT('Ctrl Pts',(-4.,-38.8368887914994,16.9339894885996));
#83762=CARTESIAN_POINT('Ctrl Pts',(-4.01250760002811,-38.903598396939,16.9310500506214));
#83763=CARTESIAN_POINT('Ctrl Pts',(-4.06297796817314,-39.0260198677362,
16.9190095185695));
#83764=CARTESIAN_POINT('Ctrl Pts',(-4.10093014199565,-39.0817342544231,
16.9098896615843));
#83765=CARTESIAN_POINT('Ctrl Pts',(-4.18928809817478,-39.1711621467437,
16.8882209976741));
#83766=CARTESIAN_POINT('Ctrl Pts',(-4.24613535186385,-39.2101954912713,
16.8740756815564));
#83767=CARTESIAN_POINT('Ctrl Pts',(-4.37014285930182,-39.2617244815659,
16.8423854285274));
#83768=CARTESIAN_POINT('Ctrl Pts',(-4.43729208625343,-39.2742356128,16.8248225276024));
#83769=CARTESIAN_POINT('Ctrl Pts',(-4.5,-39.2742356128,16.8080337933977));
#83770=CARTESIAN_POINT('',(-4.,-35.2742356128,16.9339894886));
#83771=CARTESIAN_POINT('',(-4.,-36.7742356128,16.9339894886));
#83772=CARTESIAN_POINT('',(-3.,-34.2742356128,17.1394282285));
#83773=CARTESIAN_POINT('Ctrl Pts',(-4.,-35.2742356128,16.9339894885996));
#83774=CARTESIAN_POINT('Ctrl Pts',(-4.,-35.1486855593285,16.9339894885996));
#83775=CARTESIAN_POINT('Ctrl Pts',(-3.97489818350414,-35.0150317313568,
16.9399790550091));
#83776=CARTESIAN_POINT('Ctrl Pts',(-3.87354117753779,-34.7697170783414,
16.9634425952617));
#83777=CARTESIAN_POINT('Ctrl Pts',(-3.79730805944039,-34.6580384861345,
16.9808260582146));
#83778=CARTESIAN_POINT('Ctrl Pts',(-3.6207263799214,-34.4800481242703,17.0193617118533));
#83779=CARTESIAN_POINT('Ctrl Pts',(-3.5078727043035,-34.4024577097155,17.0432013993171));
#83780=CARTESIAN_POINT('Ctrl Pts',(-3.26061624783525,-34.2995507541585,
17.0922282494331));
#83781=CARTESIAN_POINT('Ctrl Pts',(-3.12619777878762,-34.2742356128,17.1173391989672));
#83782=CARTESIAN_POINT('Ctrl Pts',(-3.,-34.2742356128,17.1394282285029));
#83783=CARTESIAN_POINT('',(3.,-34.2742356128,17.1394282285));
#83784=CARTESIAN_POINT('Origin',(0.,-34.2742356128,0.));
#83785=CARTESIAN_POINT('',(4.,-35.2742356128,16.9339894886));
#83786=CARTESIAN_POINT('Ctrl Pts',(3.,-34.2742356128,17.1394282285029));
#83787=CARTESIAN_POINT('Ctrl Pts',(3.12619777878762,-34.2742356128001,17.1173391989672));
#83788=CARTESIAN_POINT('Ctrl Pts',(3.26061624783525,-34.2995507541585,17.0922282494331));
#83789=CARTESIAN_POINT('Ctrl Pts',(3.5078727043035,-34.4024577097155,17.0432013993171));
#83790=CARTESIAN_POINT('Ctrl Pts',(3.6207263799214,-34.4800481242703,17.0193617118533));
#83791=CARTESIAN_POINT('Ctrl Pts',(3.79730805944039,-34.6580384861345,16.9808260582146));
#83792=CARTESIAN_POINT('Ctrl Pts',(3.87354117753779,-34.7697170783414,16.9634425952617));
#83793=CARTESIAN_POINT('Ctrl Pts',(3.97489818350414,-35.0150317313568,16.9399790550091));
#83794=CARTESIAN_POINT('Ctrl Pts',(4.,-35.1486855593285,16.9339894885996));
#83795=CARTESIAN_POINT('Ctrl Pts',(4.,-35.2742356128,16.9339894885996));
#83796=CARTESIAN_POINT('',(4.,-38.7742356128,16.9339894886));
#83797=CARTESIAN_POINT('',(4.,-36.7742356128,16.9339894886));
#83798=CARTESIAN_POINT('',(4.5,-39.2742356128,16.8080337934));
#83799=CARTESIAN_POINT('Ctrl Pts',(4.5,-39.2742356128,16.8080337933977));
#83800=CARTESIAN_POINT('Ctrl Pts',(4.43729208625343,-39.2742356127999,16.8248225276024));
#83801=CARTESIAN_POINT('Ctrl Pts',(4.37014285930182,-39.2617244815659,16.8423854285274));
#83802=CARTESIAN_POINT('Ctrl Pts',(4.24613535186385,-39.2101954912713,16.8740756815564));
#83803=CARTESIAN_POINT('Ctrl Pts',(4.18928809817478,-39.1711621467437,16.8882209976741));
#83804=CARTESIAN_POINT('Ctrl Pts',(4.10093014199565,-39.0817342544231,16.9098896615843));
#83805=CARTESIAN_POINT('Ctrl Pts',(4.06297796817314,-39.0260198677362,16.9190095185695));
#83806=CARTESIAN_POINT('Ctrl Pts',(4.0125076000281,-38.903598396939,16.9310500506214));
#83807=CARTESIAN_POINT('Ctrl Pts',(4.,-38.8368887914994,16.9339894885996));
#83808=CARTESIAN_POINT('Ctrl Pts',(4.,-38.7742356128,16.9339894885996));
#83809=CARTESIAN_POINT('',(5.5,-39.2742356128,-16.5078769077));
#83810=CARTESIAN_POINT('Origin',(0.,-39.2742356128,0.));
#83811=CARTESIAN_POINT('',(5.,-38.7742356128,-16.6661333248));
#83812=CARTESIAN_POINT('Ctrl Pts',(5.,-38.7742356128,-16.6661333247997));
#83813=CARTESIAN_POINT('Ctrl Pts',(5.,-38.8368267820667,-16.6661333247997));
#83814=CARTESIAN_POINT('Ctrl Pts',(5.01248880952419,-38.9033956100947,-16.6624020649352));
#83815=CARTESIAN_POINT('Ctrl Pts',(5.06265202735881,-39.0253853950253,-16.647229231688));
#83816=CARTESIAN_POINT('Ctrl Pts',(5.10030872977378,-39.0808115065366,-16.6357705740154));
#83817=CARTESIAN_POINT('Ctrl Pts',(5.18841286970923,-39.1705785286071,-16.6085103506913));
#83818=CARTESIAN_POINT('Ctrl Pts',(5.24557566629518,-39.2099085842528,-16.5906059126269));
#83819=CARTESIAN_POINT('Ctrl Pts',(5.37001700861689,-39.2617262283776,-16.5507457822022));
#83820=CARTESIAN_POINT('Ctrl Pts',(5.43728107900467,-39.2742356128,-16.5287732390402));
#83821=CARTESIAN_POINT('Ctrl Pts',(5.5,-39.2742356128,-16.5078769077068));
#83822=CARTESIAN_POINT('',(5.,-35.2742356128,-16.6661333248));
#83823=CARTESIAN_POINT('',(5.,-37.0242356128,-16.6661333248));
#83824=CARTESIAN_POINT('',(4.,-34.2742356128,-16.9339894886));
#83825=CARTESIAN_POINT('Ctrl Pts',(5.,-35.2742356128,-16.6661333247997));
#83826=CARTESIAN_POINT('Ctrl Pts',(5.,-35.1487369636031,-16.6661333247997));
#83827=CARTESIAN_POINT('Ctrl Pts',(4.97490998956982,-35.0152959233024,-16.6737229014171));
#83828=CARTESIAN_POINT('Ctrl Pts',(4.87404705295522,-34.7707070374517,-16.7034855674542));
#83829=CARTESIAN_POINT('Ctrl Pts',(4.79830954261467,-34.6595323663436,-16.7255581246326));
#83830=CARTESIAN_POINT('Ctrl Pts',(4.62229972372855,-34.481143286089,-16.7750706933282));
#83831=CARTESIAN_POINT('Ctrl Pts',(4.50907276305283,-34.403095624184,-16.8060902401953));
#83832=CARTESIAN_POINT('Ctrl Pts',(4.2611669496739,-34.299642472023,-16.8706509231256));
#83833=CARTESIAN_POINT('Ctrl Pts',(4.12646889394831,-34.2742356128,-16.9041161042955));
#83834=CARTESIAN_POINT('Ctrl Pts',(4.,-34.2742356128,-16.9339894885996));
#83835=CARTESIAN_POINT('',(-4.,-34.2742356128,-16.9339894886));
#83836=CARTESIAN_POINT('Origin',(0.,-34.2742356128,0.));
#83837=CARTESIAN_POINT('',(-5.,-35.2742356128,-16.6661333248));
#83838=CARTESIAN_POINT('Ctrl Pts',(-4.,-34.2742356128,-16.9339894885996));
#83839=CARTESIAN_POINT('Ctrl Pts',(-4.12646889394831,-34.2742356128,-16.9041161042955));
#83840=CARTESIAN_POINT('Ctrl Pts',(-4.26116694967389,-34.299642472023,-16.8706509231256));
#83841=CARTESIAN_POINT('Ctrl Pts',(-4.50907276305283,-34.403095624184,-16.8060902401953));
#83842=CARTESIAN_POINT('Ctrl Pts',(-4.62229972372855,-34.481143286089,-16.7750706933282));
#83843=CARTESIAN_POINT('Ctrl Pts',(-4.79830954261467,-34.6595323663436,
-16.7255581246326));
#83844=CARTESIAN_POINT('Ctrl Pts',(-4.87404705295522,-34.7707070374517,
-16.7034855674542));
#83845=CARTESIAN_POINT('Ctrl Pts',(-4.97490998956982,-35.0152959233024,
-16.6737229014171));
#83846=CARTESIAN_POINT('Ctrl Pts',(-5.,-35.1487369636031,-16.6661333247997));
#83847=CARTESIAN_POINT('Ctrl Pts',(-5.,-35.2742356128,-16.6661333247997));
#83848=CARTESIAN_POINT('',(-5.,-38.7742356128,-16.6661333248));
#83849=CARTESIAN_POINT('',(-5.,-37.0242356128,-16.6661333248));
#83850=CARTESIAN_POINT('',(-5.5,-39.2742356128,-16.5078769077));
#83851=CARTESIAN_POINT('Ctrl Pts',(-5.5,-39.2742356128,-16.5078769077068));
#83852=CARTESIAN_POINT('Ctrl Pts',(-5.43728107900467,-39.2742356128003,
-16.5287732390402));
#83853=CARTESIAN_POINT('Ctrl Pts',(-5.37001700861689,-39.2617262283776,
-16.5507457822022));
#83854=CARTESIAN_POINT('Ctrl Pts',(-5.24557566629518,-39.2099085842528,
-16.5906059126269));
#83855=CARTESIAN_POINT('Ctrl Pts',(-5.18841286970923,-39.1705785286071,
-16.6085103506913));
#83856=CARTESIAN_POINT('Ctrl Pts',(-5.10030872977378,-39.0808115065366,
-16.6357705740154));
#83857=CARTESIAN_POINT('Ctrl Pts',(-5.06265202735881,-39.0253853950253,
-16.647229231688));
#83858=CARTESIAN_POINT('Ctrl Pts',(-5.01248880952419,-38.9033956100947,
-16.6624020649352));
#83859=CARTESIAN_POINT('Ctrl Pts',(-5.,-38.8368267820667,-16.6661333247997));
#83860=CARTESIAN_POINT('Ctrl Pts',(-5.,-38.7742356128,-16.6661333247997));
#83861=CARTESIAN_POINT('Origin',(0.,-39.2742356128,0.));
#83862=CARTESIAN_POINT('Origin',(14.0872311983,-16.6742356128,-1.01503102594));
#83863=CARTESIAN_POINT('',(14.9221240862,-16.6742356128,-1.52650344091));
#83864=CARTESIAN_POINT('',(14.9221240862,-16.6742356128,-1.52650344091));
#83865=CARTESIAN_POINT('',(14.9221240862,-19.3742356128,-1.52650344091));
#83866=CARTESIAN_POINT('',(14.9221240862,-18.0242356128,-1.52650344091));
#83867=CARTESIAN_POINT('',(15.57788482,-19.3742356128,-1.92823584397));
#83868=CARTESIAN_POINT('Origin',(13.4419608479,-16.6742356128,0.619725245787));
#83869=CARTESIAN_POINT('',(14.8362431871,-19.3742356128,1.4738910501));
#83870=CARTESIAN_POINT('',(15.5349443705,-19.3742356128,1.90192964856));
#83871=CARTESIAN_POINT('',(14.8362431871,-16.6742356128,1.4738910501));
#83872=CARTESIAN_POINT('',(14.8362431871,-18.0242356128,1.4738910501));
#83873=CARTESIAN_POINT('',(14.8362431871,-16.6742356128,1.4738910501));
#83874=CARTESIAN_POINT('Origin',(0.,-18.0242356128,0.));
#83875=CARTESIAN_POINT('',(14.976285439,-19.3742356128,0.843133708384));
#83876=CARTESIAN_POINT('Origin',(0.,-19.3742356128,0.));
#83877=CARTESIAN_POINT('',(14.976285439,-16.6742356128,0.843133708384));
#83878=CARTESIAN_POINT('Origin',(-3.5527136788005E-13,-16.6742356128,-5.24580379135386E-14));
#83879=CARTESIAN_POINT('',(14.976285439,-18.0242356128,0.843133708384));
#83880=CARTESIAN_POINT('Origin',(12.9794473804,-18.0242356128,0.730715880599));
#83881=CARTESIAN_POINT('Origin',(12.9794473804,-16.6742356128,0.730715880599));
#83882=CARTESIAN_POINT('Origin',(12.9794473804,-19.3742356128,0.730715880599));
#83883=CARTESIAN_POINT('Origin',(0.,-18.0242356128,0.));
#83884=CARTESIAN_POINT('',(13.4786568951,-19.3742356128,0.758820337546));
#83885=CARTESIAN_POINT('',(13.4786568951,-16.6742356128,0.758820337546));
#83886=CARTESIAN_POINT('',(13.4786568951,-18.0242356128,0.758820337546));
#83887=CARTESIAN_POINT('',(13.3555478213,-16.6742356128,-1.96960462883));
#83888=CARTESIAN_POINT('Origin',(1.04360964314765E-13,-16.6742356128,1.24761312392252E-13));
#83889=CARTESIAN_POINT('',(13.3555478213,-19.3742356128,-1.96960462883));
#83890=CARTESIAN_POINT('',(13.3555478213,-18.0242356128,-1.96960462883));
#83891=CARTESIAN_POINT('Origin',(0.,-19.3742356128,0.));
#83892=CARTESIAN_POINT('Origin',(12.9794473804,-18.0242356128,0.730715880599));
#83893=CARTESIAN_POINT('',(13.1249762208,-16.6742356128,1.20906863394));
#83894=CARTESIAN_POINT('',(13.1249762208,-19.3742356128,1.20906863394));
#83895=CARTESIAN_POINT('',(13.1249762208,-18.0242356128,1.20906863394));
#83896=CARTESIAN_POINT('Origin',(12.9794473804,-16.6742356128,0.730715880598998));
#83897=CARTESIAN_POINT('Origin',(12.9794473804,-19.3742356128,0.730715880599));
#83898=CARTESIAN_POINT('Origin',(13.2705050612,-18.0242356128,1.68742138727));
#83899=CARTESIAN_POINT('',(13.0093116937,-19.3742356128,2.11377572911));
#83900=CARTESIAN_POINT('Origin',(13.2705050612,-19.3742356128,1.68742138727));
#83901=CARTESIAN_POINT('',(13.0093116937,-16.6742356128,2.11377572911));
#83902=CARTESIAN_POINT('',(13.0093116937,-18.0242356128,2.11377572911));
#83903=CARTESIAN_POINT('Origin',(13.2705050612,-16.6742356128,1.68742138727));
#83904=CARTESIAN_POINT('Origin',(12.6583807456,-16.6742356128,1.8987882713));
#83905=CARTESIAN_POINT('',(14.4691278654,-19.3742356128,3.00808889615));
#83906=CARTESIAN_POINT('',(15.9289440371,-16.6742356128,3.90240206319));
#83907=CARTESIAN_POINT('Origin',(13.8501977406,-18.0242356128,-2.04255294841));
#83908=CARTESIAN_POINT('',(13.5890043731,-19.3742356128,-2.46890729025));
#83909=CARTESIAN_POINT('Origin',(13.8501977406,-19.3742356128,-2.04255294841));
#83910=CARTESIAN_POINT('',(13.5890043731,-16.6742356128,-2.46890729025));
#83911=CARTESIAN_POINT('Origin',(13.8501977406,-16.6742356128,-2.04255294841));
#83912=CARTESIAN_POINT('',(13.5890043731,-18.0242356128,-2.46890729025));
#83913=CARTESIAN_POINT('Origin',(0.,-19.3742356128,0.));
#83914=CARTESIAN_POINT('',(14.7589742051,-19.3742356128,-3.18565467672));
#83915=CARTESIAN_POINT('Origin',(13.303651096,-16.6742356128,-2.29409405145));
#83916=CARTESIAN_POINT('',(13.5890043731,-16.6742356128,-2.46890729025));
#83917=CARTESIAN_POINT('Origin',(0.212376136953,-18.7742356128,15.2985259544));
#83918=CARTESIAN_POINT('',(0.213764216279,-16.6742356128,15.3985163201));
#83919=CARTESIAN_POINT('',(0.30759325472,-16.6742356128,15.3290824673));
#83920=CARTESIAN_POINT('Origin',(0.212376136952997,-16.6742356128,15.2985259544));
#83921=CARTESIAN_POINT('',(0.30759325472,-20.8742356128,15.3290824673));
#83922=CARTESIAN_POINT('',(0.30759325472,-18.7742356128,15.3290824673));
#83923=CARTESIAN_POINT('',(0.213764216279,-20.8742356128,15.3985163201));
#83924=CARTESIAN_POINT('Origin',(0.212376136953,-20.8742356128,15.2985259544));
#83925=CARTESIAN_POINT('',(0.213764216279,-18.7742356128,15.3985163201));
#83926=CARTESIAN_POINT('Origin',(1.82391441117,-19.3742356128,10.6040757126));
#83927=CARTESIAN_POINT('',(1.188848049,-16.6742356128,12.5830053333));
#83928=CARTESIAN_POINT('',(0.30759325472,-16.6742356128,15.3290824673));
#83929=CARTESIAN_POINT('',(1.188848049,-20.8742356128,12.5830053333));
#83930=CARTESIAN_POINT('',(1.188848049,-18.7742356128,12.5830053333));
#83931=CARTESIAN_POINT('',(0.748220651862,-20.8742356128,13.9560439003));
#83932=CARTESIAN_POINT('Origin',(2.12507249391,-18.7742356128,11.3019496944));
#83933=CARTESIAN_POINT('',(2.60115808275,-20.5742356128,11.4547322592));
#83934=CARTESIAN_POINT('Origin',(2.12507249391,-20.5742356128,11.3019496944));
#83935=CARTESIAN_POINT('',(2.60115808275,-19.6742356128,11.4547322592));
#83936=CARTESIAN_POINT('Origin',(2.12507249391,-19.6742356128,11.3019496944));
#83937=CARTESIAN_POINT('',(2.60115808275,-18.7742356128,11.4547322592));
#83938=CARTESIAN_POINT('Ctrl Pts',(2.03267803763261,-20.5742356128,10.8105605772543));
#83939=CARTESIAN_POINT('Ctrl Pts',(2.31194217506952,-20.5742356128,10.7580513595367));
#83940=CARTESIAN_POINT('Ctrl Pts',(2.49996449209242,-20.5742356128,10.9711083582602));
#83941=CARTESIAN_POINT('Ctrl Pts',(2.68798680911532,-20.5742356128,11.1841653569836));
#83942=CARTESIAN_POINT('Ctrl Pts',(2.60115808268513,-20.5742356128,11.454732259376));
#83943=CARTESIAN_POINT('Ctrl Pts',(2.03267803763261,-20.6984996815293,10.8105605772543));
#83944=CARTESIAN_POINT('Ctrl Pts',(2.31194217506952,-20.6984996815293,10.7580513595367));
#83945=CARTESIAN_POINT('Ctrl Pts',(2.49996449209242,-20.6984996815293,10.9711083582602));
#83946=CARTESIAN_POINT('Ctrl Pts',(2.68798680911532,-20.6984996815293,11.1841653569836));
#83947=CARTESIAN_POINT('Ctrl Pts',(2.60115808268513,-20.6984996815293,11.454732259376));
#83948=CARTESIAN_POINT('Ctrl Pts',(2.04891506345624,-20.7863676471769,10.8969153014013));
#83949=CARTESIAN_POINT('Ctrl Pts',(2.27910245761361,-20.7863676471769,10.8536338399628));
#83950=CARTESIAN_POINT('Ctrl Pts',(2.43408249764367,-20.7863676471769,11.0292490685892));
#83951=CARTESIAN_POINT('Ctrl Pts',(2.58906253767373,-20.7863676471769,11.2048642972156));
#83952=CARTESIAN_POINT('Ctrl Pts',(2.51749273834894,-20.7863676471769,11.4278828730289));
#83953=CARTESIAN_POINT('Ctrl Pts',(2.06515208927988,-20.8742356128246,10.9832700255484));
#83954=CARTESIAN_POINT('Ctrl Pts',(2.24626274015771,-20.8742356128246,10.9492163203888));
#83955=CARTESIAN_POINT('Ctrl Pts',(2.36820050319492,-20.8742356128246,11.0873897789182));
#83956=CARTESIAN_POINT('Ctrl Pts',(2.49013826623214,-20.8742356128246,11.2255632374475));
#83957=CARTESIAN_POINT('Ctrl Pts',(2.43382739401276,-20.8742356128246,11.4010334866819));
#83958=CARTESIAN_POINT('Ctrl Pts',(2.08811471141,-20.8742356128,11.1053940476));
#83959=CARTESIAN_POINT('Ctrl Pts',(2.19982036635165,-20.8742356128,11.0843903605192));
#83960=CARTESIAN_POINT('Ctrl Pts',(2.27502929313851,-20.8742356128,11.1696131599833));
#83961=CARTESIAN_POINT('Ctrl Pts',(2.35023821992538,-20.8742356128,11.2548359594474));
#83962=CARTESIAN_POINT('Ctrl Pts',(2.3155067293636,-20.8742356128,11.3630627203723));
#83963=CARTESIAN_POINT('',(2.31550672945,-20.8742356128,11.3630627204));
#83964=CARTESIAN_POINT('',(2.08811471141,-20.8742356128,11.1053940476));
#83965=CARTESIAN_POINT('Origin',(2.12507249391,-20.8742356128,11.3019496944));
#83966=CARTESIAN_POINT('Origin',(2.08811471141,-20.5742356128,11.1053940476));
#83967=CARTESIAN_POINT('Origin',(2.31550672945,-20.5742356128,11.3630627204));
#83968=CARTESIAN_POINT('Origin',(1.59732923672,-20.5742356128,13.6009748472));
#83969=CARTESIAN_POINT('',(1.50971990538,-20.8742356128,13.8739741921));
#83970=CARTESIAN_POINT('',(1.94732913984,-20.5742356128,13.4921279379));
#83971=CARTESIAN_POINT('Origin',(2.77608558884,-19.3742356128,10.9096408422));
#83972=CARTESIAN_POINT('',(2.30669397219696,-19.6742353176957,12.3723115634183));
#83973=CARTESIAN_POINT('',(1.91660155908,-19.6742356128,13.5878781199));
#83974=CARTESIAN_POINT('',(2.11321243347333,-19.0742355019,12.9752191818));
#83975=CARTESIAN_POINT('Origin',(2.30675324894277,-19.0740005634869,12.37212685105));
#83976=CARTESIAN_POINT('',(2.11321243752,-16.6742356128,12.9752191692));
#83977=CARTESIAN_POINT('',(2.11321243752,-18.7742356128,12.9752191692));
#83978=CARTESIAN_POINT('',(1.02442996075,-16.6742356128,16.3679730955));
#83979=CARTESIAN_POINT('Origin',(2.39886379082,-18.7742356128,13.066888708));
#83980=CARTESIAN_POINT('',(2.57699954471655,-19.074235612975,12.8255017742882));
#83981=CARTESIAN_POINT('Ctrl Pts',(2.57699954611,-19.0742356128,12.8255017724));
#83982=CARTESIAN_POINT('Ctrl Pts',(2.48546463599,-19.0742356274384,12.7579519823));
#83983=CARTESIAN_POINT('Ctrl Pts',(2.36191078436,-19.0742356216407,12.7337901943));
#83984=CARTESIAN_POINT('Ctrl Pts',(2.23407965787,-19.0742355909528,12.7750559918));
#83985=CARTESIAN_POINT('Ctrl Pts',(2.14797389499,-19.0742355464704,12.8668990358));
#83986=CARTESIAN_POINT('Ctrl Pts',(2.11321243145,-19.0742355019,12.9752191881));
#83987=CARTESIAN_POINT('',(2.576999541,-16.6742356128,12.8255017686));
#83988=CARTESIAN_POINT('',(2.576999541,-18.0242356128,12.8255017686));
#83989=CARTESIAN_POINT('Origin',(2.39886379082,-16.6742356128,13.066888708));
#83990=CARTESIAN_POINT('Origin',(1.40932124909,-16.6742356128,11.9637929743));
#83991=CARTESIAN_POINT('',(4.11574708991,-19.0742356128,13.9610476671));
#83992=CARTESIAN_POINT('',(2.576999541,-16.6742356128,12.8255017686));
#83993=CARTESIAN_POINT('Origin',(1.09363093124,-18.7742356128,12.5524488203));
#83994=CARTESIAN_POINT('',(1.08495132067,-16.6742356128,12.4528262106));
#83995=CARTESIAN_POINT('Origin',(1.09363093124,-16.6742356128,12.5524488203));
#83996=CARTESIAN_POINT('',(1.08495132067,-20.8742356128,12.4528262106));
#83997=CARTESIAN_POINT('',(1.08495132067,-18.7742356128,12.4528262106));
#83998=CARTESIAN_POINT('Origin',(1.09363093124,-20.8742356128,12.5524488203));
#83999=CARTESIAN_POINT('Ctrl Pts',(2.11321243145,-19.0742355019,12.9752191881));
#84000=CARTESIAN_POINT('Ctrl Pts',(2.14797389499,-19.0742355464,12.8668990358));
#84001=CARTESIAN_POINT('Ctrl Pts',(2.23407965787,-19.0742355909,12.7750559918));
#84002=CARTESIAN_POINT('Ctrl Pts',(2.36191078436,-19.0742356216,12.7337901943));
#84003=CARTESIAN_POINT('Ctrl Pts',(2.48546463599,-19.0742356274,12.7579519823));
#84004=CARTESIAN_POINT('Ctrl Pts',(2.57699954053,-19.0742356132,12.82550178));
#84005=CARTESIAN_POINT('Ctrl Pts',(2.11321242505,-19.1612543019,12.975219208));
#84006=CARTESIAN_POINT('Ctrl Pts',(2.14797389154,-19.1438426701,12.8668990456));
#84007=CARTESIAN_POINT('Ctrl Pts',(2.23407965879,-19.1264310382,12.7750559919));
#84008=CARTESIAN_POINT('Ctrl Pts',(2.36191078991,-19.1144387816,12.7337901893));
#84009=CARTESIAN_POINT('Ctrl Pts',(2.48546464338,-19.112181627,12.7579519792));
#84010=CARTESIAN_POINT('Ctrl Pts',(2.57699954662,-19.1177450086,12.825501783));
#84011=CARTESIAN_POINT('Ctrl Pts',(2.11829710106,-19.248306695,12.9593748545));
#84012=CARTESIAN_POINT('Ctrl Pts',(2.15187949666,-19.2134621794,12.8547287833));
#84013=CARTESIAN_POINT('Ctrl Pts',(2.23632644193,-19.1786176639,12.7664058619));
#84014=CARTESIAN_POINT('Ctrl Pts',(2.3624655556,-19.1546253192,12.7270177415));
#84015=CARTESIAN_POINT('Ctrl Pts',(2.48537378308,-19.1501233479,12.7505876284));
#84016=CARTESIAN_POINT('Ctrl Pts',(2.57740280629,-19.1612710822,12.8160010902));
#84017=CARTESIAN_POINT('Ctrl Pts',(2.1284939378,-19.3306965513,12.9276005023));
#84018=CARTESIAN_POINT('Ctrl Pts',(2.15970428933,-19.2801076689,12.8303459527));
#84019=CARTESIAN_POINT('Ctrl Pts',(2.24081540097,-19.2295187866,12.7491052593));
#84020=CARTESIAN_POINT('Ctrl Pts',(2.36355540449,-19.1943772592,12.7134885287));
#84021=CARTESIAN_POINT('Ctrl Pts',(2.48517594342,-19.1870911735,12.7358510743));
#84022=CARTESIAN_POINT('Ctrl Pts',(2.5782116467,-19.2024661641,12.796948158));
#84023=CARTESIAN_POINT('Ctrl Pts',(2.16109563614,-19.4975344726,12.8260103845));
#84024=CARTESIAN_POINT('Ctrl Pts',(2.18524115037,-19.4177125414,12.7507705807));
#84025=CARTESIAN_POINT('Ctrl Pts',(2.25630596622,-19.3378906101,12.6905878411));
#84026=CARTESIAN_POINT('Ctrl Pts',(2.36852442786,-19.2809552961,12.6666894295));
#84027=CARTESIAN_POINT('Ctrl Pts',(2.48552961718,-19.2657636574,12.6866327467));
#84028=CARTESIAN_POINT('Ctrl Pts',(2.58079725879,-19.2858849393,12.7360320273));
#84029=CARTESIAN_POINT('Ctrl Pts',(2.21060765367,-19.6106096232,12.6717260389));
#84030=CARTESIAN_POINT('Ctrl Pts',(2.22542521735,-19.5162497602,12.6255530347));
#84031=CARTESIAN_POINT('Ctrl Pts',(2.28292923485,-19.4218898972,12.5930787142));
#84032=CARTESIAN_POINT('Ctrl Pts',(2.38019466467,-19.3518501373,12.5859609253));
#84033=CARTESIAN_POINT('Ctrl Pts',(2.48889752329,-19.3268991358,12.6060157728));
#84034=CARTESIAN_POINT('Ctrl Pts',(2.58472445083,-19.3424227485,12.6435184464));
#84035=CARTESIAN_POINT('Ctrl Pts',(2.24157751669,-19.6529683202,12.5752208815));
#84036=CARTESIAN_POINT('Ctrl Pts',(2.25115370883,-19.5552809276,12.5453805297));
#84037=CARTESIAN_POINT('Ctrl Pts',(2.30089868661,-19.4575935349,12.5284309064));
#84038=CARTESIAN_POINT('Ctrl Pts',(2.3892638599,-19.383367284,12.5313593346));
#84039=CARTESIAN_POINT('Ctrl Pts',(2.49223570108,-19.3530489966,12.553066847));
#84040=CARTESIAN_POINT('Ctrl Pts',(2.58718049198,-19.36360193,12.5856515981));
#84041=CARTESIAN_POINT('Ctrl Pts',(2.27413005219,-19.6742347534,12.47378396));
#84042=CARTESIAN_POINT('Ctrl Pts',(2.2787229772,-19.5767604829,12.4594719462));
#84043=CARTESIAN_POINT('Ctrl Pts',(2.32096970846,-19.4792862125,12.4572435686));
#84044=CARTESIAN_POINT('Ctrl Pts',(2.40043923714,-19.4036435793,12.4702692455));
#84045=CARTESIAN_POINT('Ctrl Pts',(2.49695035202,-19.3691668211,12.4950419018));
#84046=CARTESIAN_POINT('Ctrl Pts',(2.58976267699,-19.3742352023,12.5248266884));
#84047=CARTESIAN_POINT('Ctrl Pts',(2.30669397214,-19.6742350234,12.3723115634));
#84048=CARTESIAN_POINT('Ctrl Pts',(2.30669398607,-19.579987326,12.3723115185));
#84049=CARTESIAN_POINT('Ctrl Pts',(2.34193483095,-19.4857396287,12.3836207521));
#84050=CARTESIAN_POINT('Ctrl Pts',(2.41286534931,-19.4112462739,12.4063833145));
#84051=CARTESIAN_POINT('Ctrl Pts',(2.50260539009,-19.374235302,12.4351821369));
#84052=CARTESIAN_POINT('Ctrl Pts',(2.5923454193,-19.3742353183,12.4639809751));
#84053=CARTESIAN_POINT('',(2.59234532544548,-19.3742354655498,12.4639811022925));
#84054=CARTESIAN_POINT('Origin',(2.59032542786042,-19.6721136845399,12.4633329506423));
#84055=CARTESIAN_POINT('Ctrl Pts',(2.57699954051151,-19.0742356132,12.8255017799864));
#84056=CARTESIAN_POINT('Ctrl Pts',(2.57699954076031,-19.090097926119,12.8255017796252));
#84057=CARTESIAN_POINT('Ctrl Pts',(2.57701922698783,-19.1061952220878,12.8239491830546));
#84058=CARTESIAN_POINT('Ctrl Pts',(2.57709880509,-19.12230194734,12.8207578866714));
#84059=CARTESIAN_POINT('Ctrl Pts',(2.57717957791688,-19.138650486634,12.8175186786076));
#84060=CARTESIAN_POINT('Ctrl Pts',(2.57732193153449,-19.1550088429505,12.8125913121783));
#84061=CARTESIAN_POINT('Ctrl Pts',(2.57756630925782,-19.1711234874925,12.8059362580234));
#84062=CARTESIAN_POINT('Ctrl Pts',(2.57765386220267,-19.1768968639105,12.8035519589085));
#84063=CARTESIAN_POINT('Ctrl Pts',(2.57775450453884,-19.1826387868041,12.8009463571809));
#84064=CARTESIAN_POINT('Ctrl Pts',(2.57787008290454,-19.1883370166356,12.7981191469069));
#84065=CARTESIAN_POINT('Ctrl Pts',(2.57817481420733,-19.2033608404254,12.7906649882946));
#84066=CARTESIAN_POINT('Ctrl Pts',(2.57857607419071,-19.2180779034073,12.7816630814634));
#84067=CARTESIAN_POINT('Ctrl Pts',(2.57906577997038,-19.2322424680007,12.7711186642919));
#84068=CARTESIAN_POINT('Ctrl Pts',(2.57918353240181,-19.23564841498,12.7685832015478));
#84069=CARTESIAN_POINT('Ctrl Pts',(2.57930638722896,-19.2390223625536,12.7659587844579));
#84070=CARTESIAN_POINT('Ctrl Pts',(2.57943420930647,-19.2423608205184,12.7632459251213));
#84071=CARTESIAN_POINT('Ctrl Pts',(2.57976391192748,-19.2509719960097,12.7562484106769));
#84072=CARTESIAN_POINT('Ctrl Pts',(2.58012584519649,-19.2593468309819,12.7486613252388));
#84073=CARTESIAN_POINT('Ctrl Pts',(2.58051138970481,-19.2674240519412,12.7404963491802));
#84074=CARTESIAN_POINT('Ctrl Pts',(2.58056816614879,-19.2686135277951,12.7392939502465));
#84075=CARTESIAN_POINT('Ctrl Pts',(2.58062545046643,-19.269796552749,12.73807903108));
#84076=CARTESIAN_POINT('Ctrl Pts',(2.58068320201332,-19.2709729333731,12.7368516370555));
#84077=CARTESIAN_POINT('Ctrl Pts',(2.58082153347369,-19.2737907011809,12.7339116775742));
#84078=CARTESIAN_POINT('Ctrl Pts',(2.58096254608146,-19.2765703481791,12.7309001375071));
#84079=CARTESIAN_POINT('Ctrl Pts',(2.58110567068349,-19.2793091646015,12.7278178308886));
#84080=CARTESIAN_POINT('Ctrl Pts',(2.58120710929444,-19.2812502825475,12.7256332665479));
#84081=CARTESIAN_POINT('Ctrl Pts',(2.58130960682343,-19.2831708968851,12.7234131488369));
#84082=CARTESIAN_POINT('Ctrl Pts',(2.5814129424722,-19.2850700547872,12.7211577769492));
#84083=CARTESIAN_POINT('Ctrl Pts',(2.58147759529574,-19.2862582790078,12.7197466844325));
#84084=CARTESIAN_POINT('Ctrl Pts',(2.58155841255508,-19.2877354635363,12.7179601732247));
#84085=CARTESIAN_POINT('Ctrl Pts',(2.58162455597423,-19.2889406945427,12.7164741655177));
#84086=CARTESIAN_POINT('Ctrl Pts',(2.58166413064681,-19.2896618036579,12.7155850631821));
#84087=CARTESIAN_POINT('Ctrl Pts',(2.58169840521701,-19.2902866388584,12.7148046420957));
#84088=CARTESIAN_POINT('Ctrl Pts',(2.58172051136112,-19.290701337284,12.7142838635621));
#84089=CARTESIAN_POINT('Ctrl Pts',(2.58205066174859,-19.2968947668227,12.7065061510011));
#84090=CARTESIAN_POINT('Ctrl Pts',(2.58236159329862,-19.3033427590597,12.6976710607334));
#84091=CARTESIAN_POINT('Ctrl Pts',(2.58269944763325,-19.3098398763417,12.687678603169));
#84092=CARTESIAN_POINT('Ctrl Pts',(2.58301649266678,-19.3159368197739,12.6783016062834));
#84093=CARTESIAN_POINT('Ctrl Pts',(2.58335731531155,-19.3220767709619,12.6679046408337));
#84094=CARTESIAN_POINT('Ctrl Pts',(2.58375973823555,-19.3280499192408,12.6564230442139));
#84095=CARTESIAN_POINT('Ctrl Pts',(2.58415576141217,-19.3339280763109,12.6451240398706));
#84096=CARTESIAN_POINT('Ctrl Pts',(2.58461157955433,-19.3396446663915,12.6327736690589));
#84097=CARTESIAN_POINT('Ctrl Pts',(2.58516141713524,-19.3449612196282,12.6193410240067));
#84098=CARTESIAN_POINT('Ctrl Pts',(2.58566365303769,-19.3498174972007,12.607071297738));
#84099=CARTESIAN_POINT('Ctrl Pts',(2.5862673264569,-19.3543409250383,12.5939094274449));
#84100=CARTESIAN_POINT('Ctrl Pts',(2.58693635426293,-19.3583167707245,12.5798423788928));
#84101=CARTESIAN_POINT('Ctrl Pts',(2.58758944940851,-19.3621979330527,12.5661103321239));
#84102=CARTESIAN_POINT('Ctrl Pts',(2.58830473859446,-19.3655569150395,12.5515153321523));
#84103=CARTESIAN_POINT('Ctrl Pts',(2.58904729022186,-19.3681783800973,12.5360915504371));
#84104=CARTESIAN_POINT('Ctrl Pts',(2.58976947620421,-19.3707279473572,12.5210907901685));
#84105=CARTESIAN_POINT('Ctrl Pts',(2.59051733423415,-19.3725797009973,12.5053059280041));
#84106=CARTESIAN_POINT('Ctrl Pts',(2.59125889447743,-19.373524845373,12.4888164992638));
#84107=CARTESIAN_POINT('Ctrl Pts',(2.59162376646249,-19.3739898874349,12.4807031589771));
#84108=CARTESIAN_POINT('Ctrl Pts',(2.59198712693089,-19.3742352985182,12.4724200069811));
#84109=CARTESIAN_POINT('Ctrl Pts',(2.59234532544022,-19.3742353182997,12.4639811022993));
#84110=CARTESIAN_POINT('Origin',(4.29388284009,-19.0742356128,13.7196607277));
#84111=CARTESIAN_POINT('',(4.42080718383,-19.3742356128,13.8133267862));
#84112=CARTESIAN_POINT('Ctrl Pts',(2.03267803765,-19.6742356128,10.8105605773));
#84113=CARTESIAN_POINT('Ctrl Pts',(2.03267803765,-19.6742356128,10.8105605773));
#84114=CARTESIAN_POINT('Ctrl Pts',(2.03267803765,-19.6742356128,10.8105605773));
#84115=CARTESIAN_POINT('Ctrl Pts',(2.03267803765,-19.6742356128,10.8105605773));
#84116=CARTESIAN_POINT('Ctrl Pts',(2.03267803765,-19.6742356128,10.8105605773));
#84117=CARTESIAN_POINT('Ctrl Pts',(2.03267803765,-19.6742356128,10.8105605773));
#84118=CARTESIAN_POINT('Ctrl Pts',(2.05894886759,-19.6259152622,10.8056234563));
#84119=CARTESIAN_POINT('Ctrl Pts',(2.06734285289645,-19.6307029517914,10.8040622488486));
#84120=CARTESIAN_POINT('Ctrl Pts',(2.07573485238451,-19.6354906438259,10.802501411656));
#84121=CARTESIAN_POINT('Ctrl Pts',(2.08416049881215,-19.6403007330939,10.8009343190103));
#84122=CARTESIAN_POINT('Ctrl Pts',(2.09265549117115,-19.6451556121481,10.7993543328483));
#84123=CARTESIAN_POINT('Ctrl Pts',(2.10125198398,-19.6500754685,10.7977554742));
#84124=CARTESIAN_POINT('Ctrl Pts',(2.0870381674,-19.5762206261,10.8001977615));
#84125=CARTESIAN_POINT('Ctrl Pts',(2.1034870056,-19.586196795,10.7970191759));
#84126=CARTESIAN_POINT('Ctrl Pts',(2.1202364023,-19.596172964,10.7953959482));
#84127=CARTESIAN_POINT('Ctrl Pts',(2.13714159915,-19.6060613319,10.795356101));
#84128=CARTESIAN_POINT('Ctrl Pts',(2.15405252281,-19.6157741162,10.796899988));
#84129=CARTESIAN_POINT('Ctrl Pts',(2.17082159168,-19.6252281195,10.8000002758));
#84130=CARTESIAN_POINT('',(2.17082158289334,-19.625228208562,10.8000002947161));
#84131=CARTESIAN_POINT('Origin',(2.15163545644867,-19.6372754487651,11.5156625316905));
#84132=CARTESIAN_POINT('Origin',(2.14395737416692,-19.5762206558258,11.0947491984194));
#84133=CARTESIAN_POINT('Origin',(2.12507249391,-19.6742356128,11.3019496944));
#84134=CARTESIAN_POINT('',(2.86720992902818,-19.3749426154318,11.5401120404683));
#84135=CARTESIAN_POINT('Origin',(2.88680943605,-19.6742356128,11.5464017981));
#84136=CARTESIAN_POINT('',(2.49881053590011,-19.5594863527756,10.9363631916917));
#84137=CARTESIAN_POINT('Ctrl Pts',(2.49881057490515,-19.5594863753635,10.9363631535376));
#84138=CARTESIAN_POINT('Ctrl Pts',(2.48189321230393,-19.5616279484725,10.9203363430907));
#84139=CARTESIAN_POINT('Ctrl Pts',(2.46385740336137,-19.5640380169532,10.9055168337234));
#84140=CARTESIAN_POINT('Ctrl Pts',(2.44489566614884,-19.5667483129689,10.8920449861814));
#84141=CARTESIAN_POINT('Ctrl Pts',(2.43732153123321,-19.5678309219859,10.8866637497629));
#84142=CARTESIAN_POINT('Ctrl Pts',(2.42960011206188,-19.5689617226717,10.8814972313772));
#84143=CARTESIAN_POINT('Ctrl Pts',(2.42174516216224,-19.5701438338236,10.8765530967493));
#84144=CARTESIAN_POINT('Ctrl Pts',(2.40085003502617,-19.5732883940211,10.8634010941334));
#84145=CARTESIAN_POINT('Ctrl Pts',(2.37900647676366,-19.576794631005,10.851824341331));
#84146=CARTESIAN_POINT('Ctrl Pts',(2.35649261223513,-19.5807393452508,10.8419423005584));
#84147=CARTESIAN_POINT('Ctrl Pts',(2.34862227224651,-19.5821183285094,10.8384877616646));
#84148=CARTESIAN_POINT('Ctrl Pts',(2.34067012527774,-19.5835511190477,10.8352399234243));
#84149=CARTESIAN_POINT('Ctrl Pts',(2.33264814825159,-19.5850416728663,10.8322025543555));
#84150=CARTESIAN_POINT('Ctrl Pts',(2.31659588540332,-19.5880243243507,10.8261246702505));
#84151=CARTESIAN_POINT('Ctrl Pts',(2.30026230264194,-19.5912378419647,10.8208866290135));
#84152=CARTESIAN_POINT('Ctrl Pts',(2.28377162562935,-19.5947588383549,10.8165105761754));
#84153=CARTESIAN_POINT('Ctrl Pts',(2.27121598386632,-19.5974396482021,10.8131787450001));
#84154=CARTESIAN_POINT('Ctrl Pts',(2.25856722444482,-19.6002954429563,10.8103468853162));
#84155=CARTESIAN_POINT('Ctrl Pts',(2.24588993027475,-19.6033758386239,10.8080180359072));
#84156=CARTESIAN_POINT('Ctrl Pts',(2.24191676821981,-19.6043412584538,10.8072881564882));
#84157=CARTESIAN_POINT('Ctrl Pts',(2.23794098212931,-19.6053290264032,10.8066076133275));
#84158=CARTESIAN_POINT('Ctrl Pts',(2.23396517538284,-19.6063416556388,10.8059762733988));
#84159=CARTESIAN_POINT('Ctrl Pts',(2.22528476776626,-19.6085525363706,10.8045978643677));
#84160=CARTESIAN_POINT('Ctrl Pts',(2.21660055076944,-19.6108808098985,10.8034535416467));
#84161=CARTESIAN_POINT('Ctrl Pts',(2.20794528221928,-19.6133598336687,10.8025389750823));
#84162=CARTESIAN_POINT('Ctrl Pts',(2.19929001366913,-19.6158388574389,10.8016244085179));
#84163=CARTESIAN_POINT('Ctrl Pts',(2.19066341384667,-19.6184721846969,10.8009406384501));
#84164=CARTESIAN_POINT('Ctrl Pts',(2.18211944040195,-19.6213167700468,10.8004807714098));
#84165=CARTESIAN_POINT('Ctrl Pts',(2.17833689867943,-19.622576109491,10.8002771815604));
#84166=CARTESIAN_POINT('Ctrl Pts',(2.17456948674399,-19.6238775578788,10.800117324421));
#84167=CARTESIAN_POINT('Ctrl Pts',(2.17082158489314,-19.6252282072342,10.800000304529));
#84168=CARTESIAN_POINT('Ctrl Pts',(2.86720992947,-19.3749426154,11.5401120406));
#84169=CARTESIAN_POINT('Ctrl Pts',(2.83073115845,-19.3783306343,11.4925686116));
#84170=CARTESIAN_POINT('Ctrl Pts',(2.796245355,-19.3917000854,11.4409843867));
#84171=CARTESIAN_POINT('Ctrl Pts',(2.76681414133,-19.4133420624,11.3857731806));
#84172=CARTESIAN_POINT('Ctrl Pts',(2.71098021085,-19.4644758001,11.2604631973));
#84173=CARTESIAN_POINT('Ctrl Pts',(2.64928177187,-19.5134920611,11.1278449523));
#84174=CARTESIAN_POINT('Ctrl Pts',(2.60971873368,-19.5351693857,11.0585616091));
#84175=CARTESIAN_POINT('Ctrl Pts',(2.55903583297,-19.5518626834,10.9934181309));
#84176=CARTESIAN_POINT('Ctrl Pts',(2.49881045789,-19.5594863076,10.936363268));
#84177=CARTESIAN_POINT('Origin',(2.20225291238,-19.6742356128,13.6795476588));
#84178=CARTESIAN_POINT('',(2.8825676448599,-19.3742356866711,11.5596196699867));
#84179=CARTESIAN_POINT('',(2.7374564764,-19.3742356128,12.011800398));
#84180=CARTESIAN_POINT('Ctrl Pts',(2.88256762736,-19.3742356128,11.5596196937));
#84181=CARTESIAN_POINT('Ctrl Pts',(2.87949410326,-19.3742359194,11.555715524));
#84182=CARTESIAN_POINT('Ctrl Pts',(2.87642049893,-19.3743066351,11.5518113974));
#84183=CARTESIAN_POINT('Ctrl Pts',(2.87334791066,-19.3744480562,11.5479085637));
#84184=CARTESIAN_POINT('Ctrl Pts',(2.87027737467,-19.3746601605,11.544008339));
#84185=CARTESIAN_POINT('Ctrl Pts',(2.86720992947,-19.3749426154,11.5401120406));
#84186=CARTESIAN_POINT('Origin',(0.,-19.3742356128,0.));
#84187=CARTESIAN_POINT('',(4.88509763285,-19.3742356128,13.0374220375));
#84188=CARTESIAN_POINT('Ctrl Pts',(2.47879655924,-19.4447372417,10.8888042378));
#84189=CARTESIAN_POINT('Ctrl Pts',(2.4861493729,-19.4683844343,10.8942303744));
#84190=CARTESIAN_POINT('Ctrl Pts',(2.49191208452,-19.4920316269,10.9018112135));
#84191=CARTESIAN_POINT('Ctrl Pts',(2.49597515407,-19.5153269748,10.9114662072));
#84192=CARTESIAN_POINT('Ctrl Pts',(2.49827725138,-19.5379188455,10.9230496178));
#84193=CARTESIAN_POINT('Ctrl Pts',(2.49881059449,-19.5594864256,10.9363632033));
#84194=CARTESIAN_POINT('Ctrl Pts',(2.44089425171,-19.4520187736,10.8608335));
#84195=CARTESIAN_POINT('Ctrl Pts',(2.44963136368,-19.4748973849,10.8662112305));
#84196=CARTESIAN_POINT('Ctrl Pts',(2.45702223689,-19.4977759963,10.8738380918));
#84197=CARTESIAN_POINT('Ctrl Pts',(2.46293957656,-19.5203232432,10.8836363306));
#84198=CARTESIAN_POINT('Ctrl Pts',(2.4672956606,-19.5422079505,10.8954618457));
#84199=CARTESIAN_POINT('Ctrl Pts',(2.47004984489,-19.5631271909,10.9091164123));
#84200=CARTESIAN_POINT('Ctrl Pts',(2.40004991429,-19.4606048121,10.8375867107));
#84201=CARTESIAN_POINT('Ctrl Pts',(2.41019998813,-19.4825787168,10.8426296142));
#84202=CARTESIAN_POINT('Ctrl Pts',(2.41925749864,-19.5045526216,10.8499715311));
#84203=CARTESIAN_POINT('Ctrl Pts',(2.42707877395,-19.5262185084,10.8595420691));
#84204=CARTESIAN_POINT('Ctrl Pts',(2.43355105359,-19.5472685228,10.8712051552));
#84205=CARTESIAN_POINT('Ctrl Pts',(2.43860186298,-19.5674202148,10.8847702011));
#84206=CARTESIAN_POINT('Ctrl Pts',(2.35714755108,-19.4705790255,10.8194836801));
#84207=CARTESIAN_POINT('Ctrl Pts',(2.36865799258,-19.4915042786,10.8238986479));
#84208=CARTESIAN_POINT('Ctrl Pts',(2.3793283911,-19.5124295317,10.8306149778));
#84209=CARTESIAN_POINT('Ctrl Pts',(2.38900185162,-19.5330726947,10.839573774));
#84210=CARTESIAN_POINT('Ctrl Pts',(2.3975442085,-19.5531518159,10.850652948));
#84211=CARTESIAN_POINT('Ctrl Pts',(2.40485476239,-19.5724073147,10.863676829));
#84212=CARTESIAN_POINT('Ctrl Pts',(2.27560738165,-19.4921831081,10.7955818101));
#84213=CARTESIAN_POINT('Ctrl Pts',(2.2893900823,-19.510844473,10.7983487664));
#84214=CARTESIAN_POINT('Ctrl Pts',(2.30277704132,-19.5295058379,10.8033357254));
#84215=CARTESIAN_POINT('Ctrl Pts',(2.31559552336,-19.5479374484,10.8105100727));
#84216=CARTESIAN_POINT('Ctrl Pts',(2.32768219961,-19.5659096429,10.8197835155));
#84217=CARTESIAN_POINT('Ctrl Pts',(2.33889513807,-19.5832093643,10.8310183547));
#84218=CARTESIAN_POINT('Ctrl Pts',(2.19384540622,-19.5207627351,10.7891484524));
#84219=CARTESIAN_POINT('Ctrl Pts',(2.2092243494,-19.5364515236,10.7895844661));
#84220=CARTESIAN_POINT('Ctrl Pts',(2.22456910998,-19.5521403122,10.7920171276));
#84221=CARTESIAN_POINT('Ctrl Pts',(2.23970912867,-19.56765722,10.7964428));
#84222=CARTESIAN_POINT('Ctrl Pts',(2.25447433499,-19.5828304221,10.8028133883));
#84223=CARTESIAN_POINT('Ctrl Pts',(2.26870622615,-19.5974991706,10.8110393571));
#84224=CARTESIAN_POINT('Ctrl Pts',(2.15676147687,-19.5361420848,10.7897230447));
#84225=CARTESIAN_POINT('Ctrl Pts',(2.17269814184,-19.5502379741,10.7889802082));
#84226=CARTESIAN_POINT('Ctrl Pts',(2.18874339027,-19.5643338633,10.7901046703));
#84227=CARTESIAN_POINT('Ctrl Pts',(2.20473176783,-19.578285603,10.7931055871));
#84228=CARTESIAN_POINT('Ctrl Pts',(2.22049530483,-19.591949083,10.7979533276));
#84229=CARTESIAN_POINT('Ctrl Pts',(2.23587372456,-19.6051888511,10.8045811578));
#84230=CARTESIAN_POINT('Ctrl Pts',(2.12065129512,-19.5532237866,10.7937022943));
#84231=CARTESIAN_POINT('Ctrl Pts',(2.13693992507,-19.565556494,10.7917229743));
#84232=CARTESIAN_POINT('Ctrl Pts',(2.15344959477,-19.5778892014,10.7914591884));
#84233=CARTESIAN_POINT('Ctrl Pts',(2.1700239605,-19.5901054864,10.7929309325));
#84234=CARTESIAN_POINT('Ctrl Pts',(2.18650229981,-19.6020889553,10.7961251723));
#84235=CARTESIAN_POINT('Ctrl Pts',(2.20272856722,-19.6137296999,10.8009965235));
#84236=CARTESIAN_POINT('Ctrl Pts',(2.08703817283,-19.5762208096,10.800197792));
#84237=CARTESIAN_POINT('Ctrl Pts',(2.10348700925,-19.5861969598,10.7970192075));
#84238=CARTESIAN_POINT('Ctrl Pts',(2.12023640403,-19.59617311,10.7953959802));
#84239=CARTESIAN_POINT('Ctrl Pts',(2.13714159891,-19.6060614593,10.7953561328));
#84240=CARTESIAN_POINT('Ctrl Pts',(2.1540525206,-19.6157742254,10.7969000191));
#84241=CARTESIAN_POINT('Ctrl Pts',(2.17082158758,-19.625228211,10.8000003054));
#84242=CARTESIAN_POINT('',(2.47879649228767,-19.4447371256487,10.8888042456754));
#84243=CARTESIAN_POINT('Ctrl Pts',(2.47879653467763,-19.4447372464188,10.8888042196737));
#84244=CARTESIAN_POINT('Ctrl Pts',(2.46236153595402,-19.4478946260502,10.876675697395));
#84245=CARTESIAN_POINT('Ctrl Pts',(2.44568006662651,-19.4512658354645,10.8659214494554));
#84246=CARTESIAN_POINT('Ctrl Pts',(2.42898429620936,-19.4548281576759,10.8564327768725));
#84247=CARTESIAN_POINT('Ctrl Pts',(2.41178359825752,-19.4584982146326,10.8466571398709));
#84248=CARTESIAN_POINT('Ctrl Pts',(2.39456825807104,-19.4623715596554,10.838223851903));
#84249=CARTESIAN_POINT('Ctrl Pts',(2.37754518539451,-19.4664312188039,10.8309864958141));
#84250=CARTESIAN_POINT('Ctrl Pts',(2.36024497993418,-19.4705569685263,10.8236313167752));
#84251=CARTESIAN_POINT('Ctrl Pts',(2.34314342187394,-19.4748754849818,10.8175104777587));
#84252=CARTESIAN_POINT('Ctrl Pts',(2.32640542393977,-19.479370938867,10.8124560770319));
#84253=CARTESIAN_POINT('Ctrl Pts',(2.30916927320829,-19.4840001855115,10.8072512482867));
#84254=CARTESIAN_POINT('Ctrl Pts',(2.29231853163633,-19.4888172941262,10.8031765684167));
#84255=CARTESIAN_POINT('Ctrl Pts',(2.2759784968436,-19.4938026368773,10.8000457865001));
#84256=CARTESIAN_POINT('Ctrl Pts',(2.27375428601186,-19.4944812433483,10.7996196234509));
#84257=CARTESIAN_POINT('Ctrl Pts',(2.27153945952708,-19.4951629606774,10.7992109544957));
#84258=CARTESIAN_POINT('Ctrl Pts',(2.26933426098062,-19.4958477329477,10.7988193163431));
#84259=CARTESIAN_POINT('Ctrl Pts',(2.26467629109108,-19.4972941553671,10.7979920716827));
#84260=CARTESIAN_POINT('Ctrl Pts',(2.26006131757016,-19.4987542761252,10.7972407987156));
#84261=CARTESIAN_POINT('Ctrl Pts',(2.255491916587,-19.5002289809292,10.7965609749296));
#84262=CARTESIAN_POINT('Ctrl Pts',(2.23931624507815,-19.5054494333626,10.7941543999131));
#84263=CARTESIAN_POINT('Ctrl Pts',(2.22369167515068,-19.510863007211,10.7926392347204));
#84264=CARTESIAN_POINT('Ctrl Pts',(2.20872066031686,-19.5164597190796,10.7918341279312));
#84265=CARTESIAN_POINT('Ctrl Pts',(2.19296963644529,-19.522348026801,10.7909870740477));
#84266=CARTESIAN_POINT('Ctrl Pts',(2.17794021198136,-19.5284338048858,10.790926179143));
#84267=CARTESIAN_POINT('Ctrl Pts',(2.16371391624849,-19.5347195389631,10.791444877268));
#84268=CARTESIAN_POINT('Ctrl Pts',(2.14831679595182,-19.5415225891428,10.7920062642642));
#84269=CARTESIAN_POINT('Ctrl Pts',(2.13386025331722,-19.5485602758314,10.7932458031077));
#84270=CARTESIAN_POINT('Ctrl Pts',(2.12042184758101,-19.5558955782218,10.7949111398957));
#84271=CARTESIAN_POINT('Ctrl Pts',(2.10847797481028,-19.5624150955072,10.7963912686481));
#84272=CARTESIAN_POINT('Ctrl Pts',(2.09733850824266,-19.5691736498683,10.7982073251794));
#84273=CARTESIAN_POINT('Ctrl Pts',(2.08703817327717,-19.5762208095999,10.8001977919136));
#84274=CARTESIAN_POINT('Origin',(2.30065980503153,-19.4447369552491,11.1301922502066));
#84275=CARTESIAN_POINT('Origin',(2.18190353865,-18.7742356128,11.2911158416));
#84276=CARTESIAN_POINT('',(2.47879645562,-16.6742356128,10.8888042759));
#84277=CARTESIAN_POINT('Origin',(2.18190353865,-16.6742356128,11.2911158416));
#84278=CARTESIAN_POINT('',(2.47879645562,-18.0594863082,10.8888042759));
#84279=CARTESIAN_POINT('Ctrl Pts',(2.47879645562,-19.4447370035,10.8888042759));
#84280=CARTESIAN_POINT('Ctrl Pts',(2.48614926363,-19.4683842219,10.8942304132));
#84281=CARTESIAN_POINT('Ctrl Pts',(2.4919119687,-19.4920314402,10.901811256));
#84282=CARTESIAN_POINT('Ctrl Pts',(2.49597503074,-19.515326813,10.9114662563));
#84283=CARTESIAN_POINT('Ctrl Pts',(2.49827711961,-19.5379187068,10.9230496761));
#84284=CARTESIAN_POINT('Ctrl Pts',(2.49881045348,-19.5594863076,10.9363632729));
#84285=CARTESIAN_POINT('Ctrl Pts',(2.510543559,-19.4294897509,10.9122326109));
#84286=CARTESIAN_POINT('Ctrl Pts',(2.52509315654,-19.4549860554,10.9229697266));
#84287=CARTESIAN_POINT('Ctrl Pts',(2.53743184504,-19.4804823599,10.9367027854));
#84288=CARTESIAN_POINT('Ctrl Pts',(2.54730011106,-19.5054619039,10.9532408984));
#84289=CARTESIAN_POINT('Ctrl Pts',(2.55452473408,-19.52940842,10.9722767674));
#84290=CARTESIAN_POINT('Ctrl Pts',(2.55903583297,-19.5518626834,10.9934181309));
#84291=CARTESIAN_POINT('Ctrl Pts',(2.54358798483,-19.3961031493,10.9366183279));
#84292=CARTESIAN_POINT('Ctrl Pts',(2.56490210185,-19.4257202286,10.9523474783));
#84293=CARTESIAN_POINT('Ctrl Pts',(2.58262930917,-19.4553373078,10.972937153));
#84294=CARTESIAN_POINT('Ctrl Pts',(2.59620857289,-19.4840367355,10.997975939));
#84295=CARTESIAN_POINT('Ctrl Pts',(2.60527727222,-19.5109029172,11.0267904888));
#84296=CARTESIAN_POINT('Ctrl Pts',(2.60971873368,-19.5351693857,11.0585616091));
#84297=CARTESIAN_POINT('Ctrl Pts',(2.57980368735,-19.3527485635,10.9633443444));
#84298=CARTESIAN_POINT('Ctrl Pts',(2.60698188591,-19.3880359645,10.9834009889));
#84299=CARTESIAN_POINT('Ctrl Pts',(2.62854104782,-19.4233233655,11.011071838));
#84300=CARTESIAN_POINT('Ctrl Pts',(2.64323454282,-19.4570166595,11.0454386344));
#84301=CARTESIAN_POINT('Ctrl Pts',(2.65023339726,-19.4875204033,11.0850019677));
#84302=CARTESIAN_POINT('Ctrl Pts',(2.64928177187,-19.5134920611,11.1278449523));
#84303=CARTESIAN_POINT('Ctrl Pts',(2.66373575496,-19.2547159387,11.0252834944));
#84304=CARTESIAN_POINT('Ctrl Pts',(2.69872898986,-19.3050683152,11.0511073573));
#84305=CARTESIAN_POINT('Ctrl Pts',(2.72330881282,-19.3554206917,11.0910421533));
#84306=CARTESIAN_POINT('Ctrl Pts',(2.73408042005,-19.4013898853,11.1426264261));
#84307=CARTESIAN_POINT('Ctrl Pts',(2.72955068062,-19.4386199009,11.2009208948));
#84308=CARTESIAN_POINT('Ctrl Pts',(2.71098021085,-19.4644758001,11.2604631973));
#84309=CARTESIAN_POINT('Ctrl Pts',(2.78975290654,-19.1524485557,11.1182800744));
#84310=CARTESIAN_POINT('Ctrl Pts',(2.82090969201,-19.2230604651,11.1412727847));
#84311=CARTESIAN_POINT('Ctrl Pts',(2.83638207721,-19.2936723745,11.1855190018));
#84312=CARTESIAN_POINT('Ctrl Pts',(2.83135807356,-19.3541924937,11.2476786502));
#84313=CARTESIAN_POINT('Ctrl Pts',(2.80630726796,-19.3949915084,11.3177423125));
#84314=CARTESIAN_POINT('Ctrl Pts',(2.76681414133,-19.4133420624,11.3857731806));
#84315=CARTESIAN_POINT('Ctrl Pts',(2.86129530492,-19.1091646129,11.1710760494));
#84316=CARTESIAN_POINT('Ctrl Pts',(2.88687394597,-19.1898640218,11.1899522282));
#84317=CARTESIAN_POINT('Ctrl Pts',(2.89447935536,-19.2705634307,11.2331834474));
#84318=CARTESIAN_POINT('Ctrl Pts',(2.87932742318,-19.3377754042,11.2975635634));
#84319=CARTESIAN_POINT('Ctrl Pts',(2.84388765021,-19.3788647517,11.3707877234));
#84320=CARTESIAN_POINT('Ctrl Pts',(2.796245355,-19.3917000854,11.4409843867));
#84321=CARTESIAN_POINT('Ctrl Pts',(2.94208651244,-19.0824256558,11.2306973462));
#84322=CARTESIAN_POINT('Ctrl Pts',(2.95834742078,-19.1709113574,11.2426973703));
#84323=CARTESIAN_POINT('Ctrl Pts',(2.9547674495,-19.2593970589,11.2815832341));
#84324=CARTESIAN_POINT('Ctrl Pts',(2.92789987303,-19.3312626769,11.3452494815));
#84325=CARTESIAN_POINT('Ctrl Pts',(2.88323668464,-19.3712611943,11.4201106412));
#84326=CARTESIAN_POINT('Ctrl Pts',(2.83073115845,-19.3783306343,11.4925686116));
#84327=CARTESIAN_POINT('Ctrl Pts',(3.0257458739,-19.0756496396,11.2924352478));
#84328=CARTESIAN_POINT('Ctrl Pts',(3.03060872632,-19.1683851734,11.2960238755));
#84329=CARTESIAN_POINT('Ctrl Pts',(3.01410418365,-19.2611207071,11.3285668827));
#84330=CARTESIAN_POINT('Ctrl Pts',(2.97498276954,-19.334976222,11.3896852328));
#84331=CARTESIAN_POINT('Ctrl Pts',(2.92227176474,-19.372909531,11.465275844));
#84332=CARTESIAN_POINT('Ctrl Pts',(2.86720977988,-19.3749426262,11.5401119926));
#84333=CARTESIAN_POINT('',(3.0257458739,-19.0756502088,11.2924352478));
#84334=CARTESIAN_POINT('Ctrl Pts',(3.02574587389968,-19.0756502088,11.2924352478004));
#84335=CARTESIAN_POINT('Ctrl Pts',(3.00675351565961,-19.0771882002878,11.2784195019978));
#84336=CARTESIAN_POINT('Ctrl Pts',(2.98794556110458,-19.0799656124685,11.2645398401506));
#84337=CARTESIAN_POINT('Ctrl Pts',(2.96946444777136,-19.0838689703512,11.2509013765509));
#84338=CARTESIAN_POINT('Ctrl Pts',(2.95255124090799,-19.0874411739377,11.2384199771892));
#84339=CARTESIAN_POINT('Ctrl Pts',(2.93591148075212,-19.0919553471003,11.2261403726466));
#84340=CARTESIAN_POINT('Ctrl Pts',(2.91963473242905,-19.0972951829733,11.2141286590785));
#84341=CARTESIAN_POINT('Ctrl Pts',(2.90097606500497,-19.1034164437851,11.2003591662896));
#84342=CARTESIAN_POINT('Ctrl Pts',(2.88279745671413,-19.1106246716873,11.1869439416157));
#84343=CARTESIAN_POINT('Ctrl Pts',(2.86521289932878,-19.1187068763404,11.1739671072852));
#84344=CARTESIAN_POINT('Ctrl Pts',(2.85069831160009,-19.1253780632181,11.16325581122));
#84345=CARTESIAN_POINT('Ctrl Pts',(2.83658785784503,-19.1326436742646,11.1528427529497));
#84346=CARTESIAN_POINT('Ctrl Pts',(2.82292669530417,-19.140371437611,11.142761257057));
#84347=CARTESIAN_POINT('Ctrl Pts',(2.80596470462133,-19.1499663933469,11.1302438568071));
#84348=CARTESIAN_POINT('Ctrl Pts',(2.78969874364794,-19.1602717602212,11.1182401039592));
#84349=CARTESIAN_POINT('Ctrl Pts',(2.7741716633805,-19.1710306210649,11.1067816211666));
#84350=CARTESIAN_POINT('Ctrl Pts',(2.76433010714757,-19.1778499285053,11.0995188711321));
#84351=CARTESIAN_POINT('Ctrl Pts',(2.75478457692901,-19.1848513153056,11.0924745787183));
#84352=CARTESIAN_POINT('Ctrl Pts',(2.74553729325106,-19.1919708669864,11.0856503826122));
#84353=CARTESIAN_POINT('Ctrl Pts',(2.73213768965327,-19.2022873202974,11.075761908777));
#84354=CARTESIAN_POINT('Ctrl Pts',(2.7193444588255,-19.2128634993548,11.0663209183868));
#84355=CARTESIAN_POINT('Ctrl Pts',(2.70715916076948,-19.2235067787786,11.0573285627176));
#84356=CARTESIAN_POINT('Ctrl Pts',(2.69769192270529,-19.2317759618241,11.0503420473704));
#84357=CARTESIAN_POINT('Ctrl Pts',(2.68859091957648,-19.2400856488052,11.0436258015626));
#84358=CARTESIAN_POINT('Ctrl Pts',(2.67984102302334,-19.2483550306415,11.0371686610452));
#84359=CARTESIAN_POINT('Ctrl Pts',(2.66553704813159,-19.2618734796242,11.026612790439));
#84360=CARTESIAN_POINT('Ctrl Pts',(2.65214757506909,-19.2753062681188,11.0167317926194));
#84361=CARTESIAN_POINT('Ctrl Pts',(2.63954076934534,-19.2884074477262,11.0074283780573));
#84362=CARTESIAN_POINT('Ctrl Pts',(2.63452172045956,-19.2936233178166,11.0037244824381));
#84363=CARTESIAN_POINT('Ctrl Pts',(2.62962657043066,-19.2987872244217,11.0001120201687));
#84364=CARTESIAN_POINT('Ctrl Pts',(2.6248465335031,-19.3038857598675,10.9965845076172));
#84365=CARTESIAN_POINT('Ctrl Pts',(2.60806283236651,-19.3217877753653,10.9841986793659));
#84366=CARTESIAN_POINT('Ctrl Pts',(2.59269322531019,-19.3388823165721,10.972856406431));
#84367=CARTESIAN_POINT('Ctrl Pts',(2.57833633556526,-19.3547066387323,10.9622614863181));
#84368=CARTESIAN_POINT('Ctrl Pts',(2.56468487008995,-19.3697534344852,10.9521871464922));
#84369=CARTESIAN_POINT('Ctrl Pts',(2.55194665981057,-19.3836622157048,10.9427867595277));
#84370=CARTESIAN_POINT('Ctrl Pts',(2.53980373411162,-19.396024813606,10.9338256733092));
#84371=CARTESIAN_POINT('Ctrl Pts',(2.53017587314596,-19.4058268478701,10.926720623476));
#84372=CARTESIAN_POINT('Ctrl Pts',(2.52092740821589,-19.4146616173831,10.9198955559181));
#84373=CARTESIAN_POINT('Ctrl Pts',(2.51192137185923,-19.4222801308466,10.9132493927221));
#84374=CARTESIAN_POINT('Ctrl Pts',(2.50956800534002,-19.4242709238882,10.9115126844381));
#84375=CARTESIAN_POINT('Ctrl Pts',(2.50723135998009,-19.4261785010644,10.9097883158081));
#84376=CARTESIAN_POINT('Ctrl Pts',(2.50490937729373,-19.4279980029771,10.9080747677192));
#84377=CARTESIAN_POINT('Ctrl Pts',(2.49828731261426,-19.43318704225,10.9031878982596));
#84378=CARTESIAN_POINT('Ctrl Pts',(2.49177954925272,-19.4376614176956,10.8983853790159));
#84379=CARTESIAN_POINT('Ctrl Pts',(2.48534852651507,-19.4413044184337,10.8936394922355));
#84380=CARTESIAN_POINT('Ctrl Pts',(2.48315653562045,-19.44254612209,10.8920218738514));
#84381=CARTESIAN_POINT('Ctrl Pts',(2.48097305807628,-19.4436916418333,10.8904105380807));
#84382=CARTESIAN_POINT('Ctrl Pts',(2.47879645562,-19.4447370035,10.8888042759));
#84383=CARTESIAN_POINT('Origin',(2.84896336685575,-19.0776976706847,11.5322131892507));
#84384=CARTESIAN_POINT('Ctrl Pts',(3.02574587396,-19.0756502088,11.2924352478));
#84385=CARTESIAN_POINT('Ctrl Pts',(3.03060876213,-19.1683856419,11.2960239029));
#84386=CARTESIAN_POINT('Ctrl Pts',(3.0141042599,-19.261121075,11.3285669311));
#84387=CARTESIAN_POINT('Ctrl Pts',(2.97498288462,-19.3349765133,11.3896852899));
#84388=CARTESIAN_POINT('Ctrl Pts',(2.9222719047,-19.3729097939,11.465275899));
#84389=CARTESIAN_POINT('Ctrl Pts',(2.86720992778,-19.3749429031,11.5401120401));
#84390=CARTESIAN_POINT('Ctrl Pts',(3.03447355616,-19.0749433453,11.2988759949));
#84391=CARTESIAN_POINT('Ctrl Pts',(3.03813896473,-19.1681049521,11.3015809487));
#84392=CARTESIAN_POINT('Ctrl Pts',(3.02028592653,-19.2612665588,11.3334449681));
#84393=CARTESIAN_POINT('Ctrl Pts',(2.97989655367,-19.3353233942,11.3942703053));
#84394=CARTESIAN_POINT('Ctrl Pts',(2.92636073645,-19.3730546128,11.4699120931));
#84395=CARTESIAN_POINT('Ctrl Pts',(2.87104425856,-19.3745894729,11.5449824418));
#84396=CARTESIAN_POINT('Ctrl Pts',(3.04321296595,-19.0744719442,11.3053253965));
#84397=CARTESIAN_POINT('Ctrl Pts',(3.04566841653,-19.1680282232,11.3071374404));
#84398=CARTESIAN_POINT('Ctrl Pts',(3.02645347241,-19.2615845022,11.3383144504));
#84399=CARTESIAN_POINT('Ctrl Pts',(2.9847889853,-19.3358150142,11.3988454565));
#84400=CARTESIAN_POINT('Ctrl Pts',(2.93043564473,-19.3733247573,11.4745447401));
#84401=CARTESIAN_POINT('Ctrl Pts',(2.87488373803,-19.3743537743,11.5498593869));
#84402=CARTESIAN_POINT('Ctrl Pts',(3.05195820325,-19.0742362318,11.3117790986));
#84403=CARTESIAN_POINT('Ctrl Pts',(3.0531916857,-19.1681548312,11.3126893695));
#84404=CARTESIAN_POINT('Ctrl Pts',(3.03260202102,-19.2620734306,11.3431715971));
#84405=CARTESIAN_POINT('Ctrl Pts',(2.98965603461,-19.3364495577,11.4034071424));
#84406=CARTESIAN_POINT('Ctrl Pts',(2.93449336502,-19.3737189989,11.4791704265));
#84407=CARTESIAN_POINT('Ctrl Pts',(2.87872577363,-19.3742359202,11.5547395826));
#84408=CARTESIAN_POINT('Ctrl Pts',(3.06070337749,-19.0742362041,11.3182327542));
#84409=CARTESIAN_POINT('Ctrl Pts',(3.06070341502,-19.1684838804,11.3182327825));
#84410=CARTESIAN_POINT('Ctrl Pts',(3.0387268402,-19.2627315566,11.3480127241));
#84411=CARTESIAN_POINT('Ctrl Pts',(2.9944937393,-19.3372249046,11.4079518654));
#84412=CARTESIAN_POINT('Ctrl Pts',(2.93853076799,-19.3742358919,11.4837858067));
#84413=CARTESIAN_POINT('Ctrl Pts',(2.88256777785,-19.3742359083,11.5596197419));
#84414=CARTESIAN_POINT('',(3.06070337744086,-19.0742359088556,11.3182327542666));
#84415=CARTESIAN_POINT('Origin',(3.06701733419236,-19.6773931794005,11.3228922010275));
#84416=CARTESIAN_POINT('Origin',(2.88382729685578,-19.0763575401806,11.5579128499525));
#84417=CARTESIAN_POINT('Origin',(4.88509763285,-19.0742356128,13.0374220375));
#84418=CARTESIAN_POINT('',(5.27647385588,-19.0742356128,12.9533996668));
#84419=CARTESIAN_POINT('Origin',(2.3,-16.6742356128,10.7568582774));
#84420=CARTESIAN_POINT('',(7.49224433422,-16.6742356128,14.5885665792));
#84421=CARTESIAN_POINT('Origin',(0.,-18.1642356128,0.));
#84422=CARTESIAN_POINT('',(-0.213764216279,-20.8742356128,15.3985163201));
#84423=CARTESIAN_POINT('',(-0.213764216279,-16.6742356128,15.3985163201));
#84424=CARTESIAN_POINT('',(-0.213764216279,-18.7742356128,15.3985163201));
#84425=CARTESIAN_POINT('Origin',(0.,-16.6742356128,0.));
#84426=CARTESIAN_POINT('Origin',(0.,-20.8742356128,0.));
#84427=CARTESIAN_POINT('Origin',(-0.212376136953,-18.7742356128,15.2985259544));
#84428=CARTESIAN_POINT('',(-0.30759325472,-20.8742356128,15.3290824673));
#84429=CARTESIAN_POINT('Origin',(-0.212376136953,-20.8742356128,15.2985259544));
#84430=CARTESIAN_POINT('',(-0.30759325472,-16.6742356128,15.3290824673));
#84431=CARTESIAN_POINT('',(-0.30759325472,-18.7742356128,15.3290824673));
#84432=CARTESIAN_POINT('Origin',(-0.212376136952999,-16.6742356128,15.2985259544));
#84433=CARTESIAN_POINT('Origin',(-1.82391441117,-19.3742356128,10.6040757126));
#84434=CARTESIAN_POINT('',(-1.188848049,-20.8742356128,12.5830053333));
#84435=CARTESIAN_POINT('',(-0.748220651862,-20.8742356128,13.9560439003));
#84436=CARTESIAN_POINT('',(-1.188848049,-16.6742356128,12.5830053333));
#84437=CARTESIAN_POINT('',(-1.188848049,-18.7742356128,12.5830053333));
#84438=CARTESIAN_POINT('',(-0.30759325472,-16.6742356128,15.3290824673));
#84439=CARTESIAN_POINT('Origin',(-2.12507249391,-18.7742356128,11.3019496944));
#84440=CARTESIAN_POINT('',(-2.60115808275,-19.6742356128,11.4547322592));
#84441=CARTESIAN_POINT('',(-2.60115808275,-20.5742356128,11.4547322592));
#84442=CARTESIAN_POINT('',(-2.60115808275,-18.7742356128,11.4547322592));
#84443=CARTESIAN_POINT('Origin',(-2.12507249391,-19.6742356128,11.3019496944));
#84444=CARTESIAN_POINT('Origin',(-2.12507249391,-20.5742356128,11.3019496944));
#84445=CARTESIAN_POINT('Ctrl Pts',(-2.60115808268513,-20.5742356128,11.454732259376));
#84446=CARTESIAN_POINT('Ctrl Pts',(-2.68798680911532,-20.5742356128,11.1841653569836));
#84447=CARTESIAN_POINT('Ctrl Pts',(-2.49996449209242,-20.5742356128,10.9711083582602));
#84448=CARTESIAN_POINT('Ctrl Pts',(-2.31194217506952,-20.5742356128,10.7580513595367));
#84449=CARTESIAN_POINT('Ctrl Pts',(-2.03267803763261,-20.5742356128,10.8105605772543));
#84450=CARTESIAN_POINT('Ctrl Pts',(-2.60115808268513,-20.6984996815293,
11.454732259376));
#84451=CARTESIAN_POINT('Ctrl Pts',(-2.68798680911532,-20.6984996815293,
11.1841653569836));
#84452=CARTESIAN_POINT('Ctrl Pts',(-2.49996449209242,-20.6984996815293,
10.9711083582602));
#84453=CARTESIAN_POINT('Ctrl Pts',(-2.31194217506952,-20.6984996815293,
10.7580513595367));
#84454=CARTESIAN_POINT('Ctrl Pts',(-2.03267803763261,-20.6984996815293,
10.8105605772543));
#84455=CARTESIAN_POINT('Ctrl Pts',(-2.51749273834894,-20.7863676471769,
11.4278828730289));
#84456=CARTESIAN_POINT('Ctrl Pts',(-2.58906253767373,-20.7863676471769,
11.2048642972156));
#84457=CARTESIAN_POINT('Ctrl Pts',(-2.43408249764367,-20.7863676471769,
11.0292490685892));
#84458=CARTESIAN_POINT('Ctrl Pts',(-2.27910245761361,-20.7863676471769,
10.8536338399628));
#84459=CARTESIAN_POINT('Ctrl Pts',(-2.04891506345624,-20.7863676471769,
10.8969153014013));
#84460=CARTESIAN_POINT('Ctrl Pts',(-2.43382739401276,-20.8742356128246,
11.4010334866819));
#84461=CARTESIAN_POINT('Ctrl Pts',(-2.49013826623214,-20.8742356128246,
11.2255632374475));
#84462=CARTESIAN_POINT('Ctrl Pts',(-2.36820050319492,-20.8742356128246,
11.0873897789182));
#84463=CARTESIAN_POINT('Ctrl Pts',(-2.24626274015771,-20.8742356128246,
10.9492163203888));
#84464=CARTESIAN_POINT('Ctrl Pts',(-2.06515208927988,-20.8742356128246,
10.9832700255484));
#84465=CARTESIAN_POINT('Ctrl Pts',(-2.3155067293636,-20.8742356128,11.3630627203723));
#84466=CARTESIAN_POINT('Ctrl Pts',(-2.35023821992538,-20.8742356128,11.2548359594474));
#84467=CARTESIAN_POINT('Ctrl Pts',(-2.27502929313851,-20.8742356128,11.1696131599833));
#84468=CARTESIAN_POINT('Ctrl Pts',(-2.19982036635165,-20.8742356128,11.0843903605192));
#84469=CARTESIAN_POINT('Ctrl Pts',(-2.08811471141,-20.8742356128,11.1053940476));
#84470=CARTESIAN_POINT('',(-2.31550672945,-20.8742356128,11.3630627204));
#84471=CARTESIAN_POINT('Origin',(-2.31550672945,-20.5742356128,11.3630627204));
#84472=CARTESIAN_POINT('',(-2.08811471141,-20.8742356128,11.1053940476));
#84473=CARTESIAN_POINT('Origin',(-2.08811471141,-20.5742356128,11.1053940476));
#84474=CARTESIAN_POINT('Origin',(-2.12507249391,-20.8742356128,11.3019496944));
#84475=CARTESIAN_POINT('Origin',(0.,-20.8742356128,0.));
#84476=CARTESIAN_POINT('',(-1.59732923672,-20.8742356128,13.6009748472));
#84477=CARTESIAN_POINT('Origin',(7.1054273576E-15,-20.8742356128,4.4408920985E-16));
#84478=CARTESIAN_POINT('',(-1.08495132067,-20.8742356128,12.4528262106));
#84479=CARTESIAN_POINT('Origin',(0.,-20.8742356128,0.));
#84480=CARTESIAN_POINT('Origin',(-1.09363093124,-20.8742356128,12.5524488203));
#84481=CARTESIAN_POINT('Origin',(-1.59732923672,-20.5742356128,13.6009748472));
#84482=CARTESIAN_POINT('',(-1.94732913984,-20.5742356128,13.4921279379));
#84483=CARTESIAN_POINT('Origin',(-2.77608558884,-19.3742356128,10.9096408422));
#84484=CARTESIAN_POINT('',(-2.11321243752,-16.6742356128,12.9752191692));
#84485=CARTESIAN_POINT('',(-1.02442996075,-16.6742356128,16.3679730955));
#84486=CARTESIAN_POINT('',(-2.11321243436594,-19.0742355019,12.9752191789979));
#84487=CARTESIAN_POINT('',(-2.11321243752,-18.7742356128,12.9752191692));
#84488=CARTESIAN_POINT('',(-2.30669397219695,-19.6742353176957,12.3723115634183));
#84489=CARTESIAN_POINT('Origin',(-2.30675324894277,-19.0740005634869,12.37212685105));
#84490=CARTESIAN_POINT('',(-1.91660155908,-19.6742356128,13.5878781199));
#84491=CARTESIAN_POINT('Origin',(-2.39886379082,-18.7742356128,13.066888708));
#84492=CARTESIAN_POINT('',(-2.576999541,-16.6742356128,12.8255017686));
#84493=CARTESIAN_POINT('Origin',(-2.39886379082,-16.6742356128,13.066888708));
#84494=CARTESIAN_POINT('',(-2.57699954471655,-19.074235612975,12.8255017742882));
#84495=CARTESIAN_POINT('',(-2.576999541,-18.0242356128,12.8255017686));
#84496=CARTESIAN_POINT('Origin',(-2.39886379082,-19.07423555735,13.066888708));
#84497=CARTESIAN_POINT('Origin',(-1.40932124909,-16.6742356128,11.9637929743));
#84498=CARTESIAN_POINT('',(-2.576999541,-16.6742356128,12.8255017686));
#84499=CARTESIAN_POINT('',(-4.11574708991,-19.0742356128,13.9610476671));
#84500=CARTESIAN_POINT('Origin',(-1.09363093124,-18.7742356128,12.5524488203));
#84501=CARTESIAN_POINT('',(-1.08495132067,-16.6742356128,12.4528262106));
#84502=CARTESIAN_POINT('',(-1.08495132067,-18.7742356128,12.4528262106));
#84503=CARTESIAN_POINT('Origin',(-1.09363093124,-16.6742356128,12.5524488203));
#84504=CARTESIAN_POINT('Origin',(0.,-18.1642356128,0.));
#84505=CARTESIAN_POINT('Origin',(-3.01622616368355E-13,-16.6742356128,-1.06581410364015E-13));
#84506=CARTESIAN_POINT('Origin',(7.1054273576E-15,-20.5742356128,4.4408920985E-16));
#84507=CARTESIAN_POINT('Ctrl Pts',(-2.11321243145,-19.0742355019,12.9752191881));
#84508=CARTESIAN_POINT('Ctrl Pts',(-2.14797389499,-19.0742355464,12.8668990358));
#84509=CARTESIAN_POINT('Ctrl Pts',(-2.23407965787,-19.0742355909,12.7750559918));
#84510=CARTESIAN_POINT('Ctrl Pts',(-2.36191078436,-19.0742356216,12.7337901943));
#84511=CARTESIAN_POINT('Ctrl Pts',(-2.48546463599,-19.0742356274,12.7579519823));
#84512=CARTESIAN_POINT('Ctrl Pts',(-2.57699954053,-19.0742356132,12.82550178));
#84513=CARTESIAN_POINT('Ctrl Pts',(-2.11321242505,-19.1612543019,12.975219208));
#84514=CARTESIAN_POINT('Ctrl Pts',(-2.14797389154,-19.1438426701,12.8668990456));
#84515=CARTESIAN_POINT('Ctrl Pts',(-2.23407965879,-19.1264310382,12.7750559919));
#84516=CARTESIAN_POINT('Ctrl Pts',(-2.36191078991,-19.1144387816,12.7337901893));
#84517=CARTESIAN_POINT('Ctrl Pts',(-2.48546464338,-19.112181627,12.7579519792));
#84518=CARTESIAN_POINT('Ctrl Pts',(-2.57699954662,-19.1177450086,12.825501783));
#84519=CARTESIAN_POINT('Ctrl Pts',(-2.11829710106,-19.248306695,12.9593748545));
#84520=CARTESIAN_POINT('Ctrl Pts',(-2.15187949666,-19.2134621794,12.8547287833));
#84521=CARTESIAN_POINT('Ctrl Pts',(-2.23632644193,-19.1786176639,12.7664058619));
#84522=CARTESIAN_POINT('Ctrl Pts',(-2.3624655556,-19.1546253192,12.7270177415));
#84523=CARTESIAN_POINT('Ctrl Pts',(-2.48537378308,-19.1501233479,12.7505876284));
#84524=CARTESIAN_POINT('Ctrl Pts',(-2.57740280629,-19.1612710822,12.8160010902));
#84525=CARTESIAN_POINT('Ctrl Pts',(-2.1284939378,-19.3306965513,12.9276005023));
#84526=CARTESIAN_POINT('Ctrl Pts',(-2.15970428933,-19.2801076689,12.8303459527));
#84527=CARTESIAN_POINT('Ctrl Pts',(-2.24081540097,-19.2295187866,12.7491052593));
#84528=CARTESIAN_POINT('Ctrl Pts',(-2.36355540449,-19.1943772592,12.7134885287));
#84529=CARTESIAN_POINT('Ctrl Pts',(-2.48517594342,-19.1870911735,12.7358510743));
#84530=CARTESIAN_POINT('Ctrl Pts',(-2.5782116467,-19.2024661641,12.796948158));
#84531=CARTESIAN_POINT('Ctrl Pts',(-2.16109563614,-19.4975344726,12.8260103845));
#84532=CARTESIAN_POINT('Ctrl Pts',(-2.18524115037,-19.4177125414,12.7507705807));
#84533=CARTESIAN_POINT('Ctrl Pts',(-2.25630596622,-19.3378906101,12.6905878411));
#84534=CARTESIAN_POINT('Ctrl Pts',(-2.36852442786,-19.2809552961,12.6666894295));
#84535=CARTESIAN_POINT('Ctrl Pts',(-2.48552961718,-19.2657636574,12.6866327467));
#84536=CARTESIAN_POINT('Ctrl Pts',(-2.58079725879,-19.2858849393,12.7360320273));
#84537=CARTESIAN_POINT('Ctrl Pts',(-2.21060765367,-19.6106096232,12.6717260389));
#84538=CARTESIAN_POINT('Ctrl Pts',(-2.22542521735,-19.5162497602,12.6255530347));
#84539=CARTESIAN_POINT('Ctrl Pts',(-2.28292923485,-19.4218898972,12.5930787142));
#84540=CARTESIAN_POINT('Ctrl Pts',(-2.38019466467,-19.3518501373,12.5859609253));
#84541=CARTESIAN_POINT('Ctrl Pts',(-2.48889752329,-19.3268991358,12.6060157728));
#84542=CARTESIAN_POINT('Ctrl Pts',(-2.58472445083,-19.3424227485,12.6435184464));
#84543=CARTESIAN_POINT('Ctrl Pts',(-2.24157751669,-19.6529683202,12.5752208815));
#84544=CARTESIAN_POINT('Ctrl Pts',(-2.25115370883,-19.5552809276,12.5453805297));
#84545=CARTESIAN_POINT('Ctrl Pts',(-2.30089868661,-19.4575935349,12.5284309064));
#84546=CARTESIAN_POINT('Ctrl Pts',(-2.3892638599,-19.383367284,12.5313593346));
#84547=CARTESIAN_POINT('Ctrl Pts',(-2.49223570108,-19.3530489966,12.553066847));
#84548=CARTESIAN_POINT('Ctrl Pts',(-2.58718049198,-19.36360193,12.5856515981));
#84549=CARTESIAN_POINT('Ctrl Pts',(-2.27413005219,-19.6742347534,12.47378396));
#84550=CARTESIAN_POINT('Ctrl Pts',(-2.2787229772,-19.5767604829,12.4594719462));
#84551=CARTESIAN_POINT('Ctrl Pts',(-2.32096970846,-19.4792862125,12.4572435686));
#84552=CARTESIAN_POINT('Ctrl Pts',(-2.40043923714,-19.4036435793,12.4702692455));
#84553=CARTESIAN_POINT('Ctrl Pts',(-2.49695035202,-19.3691668211,12.4950419018));
#84554=CARTESIAN_POINT('Ctrl Pts',(-2.58976267699,-19.3742352023,12.5248266884));
#84555=CARTESIAN_POINT('Ctrl Pts',(-2.30669397214,-19.6742350234,12.3723115634));
#84556=CARTESIAN_POINT('Ctrl Pts',(-2.30669398607,-19.579987326,12.3723115185));
#84557=CARTESIAN_POINT('Ctrl Pts',(-2.34193483095,-19.4857396287,12.3836207521));
#84558=CARTESIAN_POINT('Ctrl Pts',(-2.41286534931,-19.4112462739,12.4063833145));
#84559=CARTESIAN_POINT('Ctrl Pts',(-2.50260539009,-19.374235302,12.4351821369));
#84560=CARTESIAN_POINT('Ctrl Pts',(-2.5923454193,-19.3742353183,12.4639809751));
#84561=CARTESIAN_POINT('',(-2.59234532544548,-19.3742354655498,12.4639811022925));
#84562=CARTESIAN_POINT('Origin',(-2.59234284839811,-19.0742335195363,12.4640390914794));
#84563=CARTESIAN_POINT('Origin',(-2.59032547075745,-19.6721137326376,12.4633329753833));
#84564=CARTESIAN_POINT('Origin',(-4.29388284009,-19.0742356128,13.7196607277));
#84565=CARTESIAN_POINT('',(-4.42080718383,-19.3742356128,13.8133267862));
#84566=CARTESIAN_POINT('Ctrl Pts',(-2.03267803765,-19.6742356128,10.8105605773));
#84567=CARTESIAN_POINT('Ctrl Pts',(-2.03267803765,-19.6742356128,10.8105605773));
#84568=CARTESIAN_POINT('Ctrl Pts',(-2.03267803765,-19.6742356128,10.8105605773));
#84569=CARTESIAN_POINT('Ctrl Pts',(-2.03267803765,-19.6742356128,10.8105605773));
#84570=CARTESIAN_POINT('Ctrl Pts',(-2.03267803765,-19.6742356128,10.8105605773));
#84571=CARTESIAN_POINT('Ctrl Pts',(-2.03267803765,-19.6742356128,10.8105605773));
#84572=CARTESIAN_POINT('Ctrl Pts',(-2.05894886759,-19.6259152622,10.8056234563));
#84573=CARTESIAN_POINT('Ctrl Pts',(-2.06734285289645,-19.6307029517914,
10.8040622488486));
#84574=CARTESIAN_POINT('Ctrl Pts',(-2.07573485238451,-19.6354906438259,
10.802501411656));
#84575=CARTESIAN_POINT('Ctrl Pts',(-2.08416049881215,-19.6403007330939,
10.8009343190103));
#84576=CARTESIAN_POINT('Ctrl Pts',(-2.09265549117115,-19.6451556121481,
10.7993543328483));
#84577=CARTESIAN_POINT('Ctrl Pts',(-2.10125198398,-19.6500754685,10.7977554742));
#84578=CARTESIAN_POINT('Ctrl Pts',(-2.0870381674,-19.5762206261,10.8001977615));
#84579=CARTESIAN_POINT('Ctrl Pts',(-2.1034870056,-19.586196795,10.7970191759));
#84580=CARTESIAN_POINT('Ctrl Pts',(-2.1202364023,-19.596172964,10.7953959482));
#84581=CARTESIAN_POINT('Ctrl Pts',(-2.13714159915,-19.6060613319,10.795356101));
#84582=CARTESIAN_POINT('Ctrl Pts',(-2.15405252281,-19.6157741162,10.796899988));
#84583=CARTESIAN_POINT('Ctrl Pts',(-2.17082159168,-19.6252281195,10.8000002758));
#84584=CARTESIAN_POINT('',(-2.17082156040968,-19.6252281736439,10.8000002868487));
#84585=CARTESIAN_POINT('Origin',(-2.14395737416692,-19.5762206558258,11.0947491984194));
#84586=CARTESIAN_POINT('Origin',(-2.12965350097472,-20.4077533044672,22.8291553975983));
#84587=CARTESIAN_POINT('Origin',(-2.12507249391,-19.6742356128,11.3019496944));
#84588=CARTESIAN_POINT('',(-2.86720989586223,-19.3749426183134,11.5401120066422));
#84589=CARTESIAN_POINT('',(-2.49881049555799,-19.5594863294135,10.9363632311538));
#84590=CARTESIAN_POINT('Ctrl Pts',(-2.86720983507867,-19.3749426241618,
11.5401119175781));
#84591=CARTESIAN_POINT('Ctrl Pts',(-2.85794042079669,-19.3758035323584,
11.5280309646887));
#84592=CARTESIAN_POINT('Ctrl Pts',(-2.84902123015658,-19.3774209880109,
11.5158588629276));
#84593=CARTESIAN_POINT('Ctrl Pts',(-2.84047942817318,-19.3796414951876,
11.5036349549176));
#84594=CARTESIAN_POINT('Ctrl Pts',(-2.83321900805626,-19.3815288972846,
11.4932447927721));
#84595=CARTESIAN_POINT('Ctrl Pts',(-2.82622945323719,-19.3838515544305,
11.4828167136796));
#84596=CARTESIAN_POINT('Ctrl Pts',(-2.8194993801726,-19.3865184502639,11.4723681225865));
#84597=CARTESIAN_POINT('Ctrl Pts',(-2.81420528569115,-19.3886163173121,
11.4641489208165));
#84598=CARTESIAN_POINT('Ctrl Pts',(-2.80919033263759,-19.3908762665008,
11.4560955502276));
#84599=CARTESIAN_POINT('Ctrl Pts',(-2.80431578664454,-19.393298788564,11.4480166929727));
#84600=CARTESIAN_POINT('Ctrl Pts',(-2.79896751651414,-19.3959567391525,
11.4391527062535));
#84601=CARTESIAN_POINT('Ctrl Pts',(-2.79378806281648,-19.398811001587,11.4302582445943));
#84602=CARTESIAN_POINT('Ctrl Pts',(-2.78861324655873,-19.4019174204448,
11.4210514196961));
#84603=CARTESIAN_POINT('Ctrl Pts',(-2.78545482629351,-19.4038134058835,
11.4154320854264));
#84604=CARTESIAN_POINT('Ctrl Pts',(-2.7822985437128,-19.4058043481332,11.4096958180335));
#84605=CARTESIAN_POINT('Ctrl Pts',(-2.77911013539142,-19.407909997777,11.4037733452569));
#84606=CARTESIAN_POINT('Ctrl Pts',(-2.77158501758046,-19.4128796440837,
11.3897954287283));
#84607=CARTESIAN_POINT('Ctrl Pts',(-2.76424601720805,-19.4182523799667,
11.3754630858337));
#84608=CARTESIAN_POINT('Ctrl Pts',(-2.7570614996732,-19.4238657810566,11.36086736767));
#84609=CARTESIAN_POINT('Ctrl Pts',(-2.74942930372377,-19.4298289618621,
11.3453621677025));
#84610=CARTESIAN_POINT('Ctrl Pts',(-2.74197085693992,-19.4360617673903,
11.3295591468001));
#84611=CARTESIAN_POINT('Ctrl Pts',(-2.73459878949584,-19.4423636392851,
11.3136025882499));
#84612=CARTESIAN_POINT('Ctrl Pts',(-2.72722672205175,-19.44866551118,11.2976460296998));
#84613=CARTESIAN_POINT('Ctrl Pts',(-2.71993933440834,-19.4550345102455,
11.2815360940162));
#84614=CARTESIAN_POINT('Ctrl Pts',(-2.71261970911949,-19.4612950594277,
11.2654542758801));
#84615=CARTESIAN_POINT('Ctrl Pts',(-2.71002476272399,-19.4635145431981,
11.2597529654498));
#84616=CARTESIAN_POINT('Ctrl Pts',(-2.70742557195454,-19.4657207814632,
11.2540555471212));
#84617=CARTESIAN_POINT('Ctrl Pts',(-2.70481758415677,-19.4679080407443,
11.2483697897688));
#84618=CARTESIAN_POINT('Ctrl Pts',(-2.69382295878758,-19.4771289797386,
11.2244000564427));
#84619=CARTESIAN_POINT('Ctrl Pts',(-2.68254235207586,-19.4861201933903,
11.2003269705257));
#84620=CARTESIAN_POINT('Ctrl Pts',(-2.67024406741993,-19.4948015724197,
11.1759168881403));
#84621=CARTESIAN_POINT('Ctrl Pts',(-2.66232922858485,-19.5003886699545,
11.1602072283432));
#84622=CARTESIAN_POINT('Ctrl Pts',(-2.65399319767008,-19.5058487044407,
11.1443575461923));
#84623=CARTESIAN_POINT('Ctrl Pts',(-2.64502082159231,-19.5111479090135,
11.128321463775));
#84624=CARTESIAN_POINT('Ctrl Pts',(-2.63719041285278,-19.5157726524973,
11.1143263883546));
#84625=CARTESIAN_POINT('Ctrl Pts',(-2.62887529120171,-19.5202752745558,
11.1001890144411));
#84626=CARTESIAN_POINT('Ctrl Pts',(-2.61991334581597,-19.5246145322958,
11.085897506031));
#84627=CARTESIAN_POINT('Ctrl Pts',(-2.60762140935298,-19.5305661285332,
11.0662957001981));
#84628=CARTESIAN_POINT('Ctrl Pts',(-2.59474731925378,-19.5358925855985,
11.0474288525336));
#84629=CARTESIAN_POINT('Ctrl Pts',(-2.58122541698925,-19.5405628662028,
11.0293309608975));
#84630=CARTESIAN_POINT('Ctrl Pts',(-2.56761875949697,-19.5452624201067,
11.0111196317512));
#84631=CARTESIAN_POINT('Ctrl Pts',(-2.55335737438676,-19.5492990339476,
10.9936859098735));
#84632=CARTESIAN_POINT('Ctrl Pts',(-2.53841802417724,-19.5526197567307,
10.9770558858659));
#84633=CARTESIAN_POINT('Ctrl Pts',(-2.52570452319816,-19.5554457171482,
10.962903608589));
#84634=CARTESIAN_POINT('Ctrl Pts',(-2.51250080576092,-19.5577533139566,
10.9493329054815));
#84635=CARTESIAN_POINT('Ctrl Pts',(-2.49881045387518,-19.5594863052749,
10.9363632719275));
#84636=CARTESIAN_POINT('Ctrl Pts',(-2.49881057490516,-19.5594863753635,
10.9363631535376));
#84637=CARTESIAN_POINT('Ctrl Pts',(-2.48189321230394,-19.5616279484725,
10.9203363430907));
#84638=CARTESIAN_POINT('Ctrl Pts',(-2.46385740336138,-19.5640380169532,
10.9055168337234));
#84639=CARTESIAN_POINT('Ctrl Pts',(-2.44489566614884,-19.5667483129689,
10.8920449861814));
#84640=CARTESIAN_POINT('Ctrl Pts',(-2.43732153123321,-19.5678309219859,
10.8866637497629));
#84641=CARTESIAN_POINT('Ctrl Pts',(-2.42960011206188,-19.5689617226717,
10.8814972313772));
#84642=CARTESIAN_POINT('Ctrl Pts',(-2.42174516216224,-19.5701438338236,
10.8765530967493));
#84643=CARTESIAN_POINT('Ctrl Pts',(-2.40085003502617,-19.5732883940211,
10.8634010941334));
#84644=CARTESIAN_POINT('Ctrl Pts',(-2.37900647676366,-19.576794631005,10.851824341331));
#84645=CARTESIAN_POINT('Ctrl Pts',(-2.35649261223513,-19.5807393452508,
10.8419423005584));
#84646=CARTESIAN_POINT('Ctrl Pts',(-2.34862227224651,-19.5821183285094,
10.8384877616646));
#84647=CARTESIAN_POINT('Ctrl Pts',(-2.34067012527774,-19.5835511190477,
10.8352399234243));
#84648=CARTESIAN_POINT('Ctrl Pts',(-2.33264814825159,-19.5850416728663,
10.8322025543555));
#84649=CARTESIAN_POINT('Ctrl Pts',(-2.31659588540332,-19.5880243243507,
10.8261246702505));
#84650=CARTESIAN_POINT('Ctrl Pts',(-2.30026230264194,-19.5912378419647,
10.8208866290135));
#84651=CARTESIAN_POINT('Ctrl Pts',(-2.28377162562935,-19.5947588383549,
10.8165105761754));
#84652=CARTESIAN_POINT('Ctrl Pts',(-2.27121598386632,-19.5974396482021,
10.8131787450001));
#84653=CARTESIAN_POINT('Ctrl Pts',(-2.25856722444482,-19.6002954429563,
10.8103468853162));
#84654=CARTESIAN_POINT('Ctrl Pts',(-2.24588993027475,-19.6033758386239,
10.8080180359072));
#84655=CARTESIAN_POINT('Ctrl Pts',(-2.24191676821981,-19.6043412584538,
10.8072881564882));
#84656=CARTESIAN_POINT('Ctrl Pts',(-2.23794098212931,-19.6053290264032,
10.8066076133275));
#84657=CARTESIAN_POINT('Ctrl Pts',(-2.23396517538284,-19.6063416556388,
10.8059762733988));
#84658=CARTESIAN_POINT('Ctrl Pts',(-2.22528476776626,-19.6085525363706,
10.8045978643677));
#84659=CARTESIAN_POINT('Ctrl Pts',(-2.21660055076944,-19.6108808098985,
10.8034535416467));
#84660=CARTESIAN_POINT('Ctrl Pts',(-2.20794528221928,-19.6133598336687,
10.8025389750823));
#84661=CARTESIAN_POINT('Ctrl Pts',(-2.19929001366913,-19.6158388574389,
10.8016244085179));
#84662=CARTESIAN_POINT('Ctrl Pts',(-2.19066341384667,-19.6184721846969,
10.8009406384501));
#84663=CARTESIAN_POINT('Ctrl Pts',(-2.18211944040195,-19.6213167700468,
10.8004807714098));
#84664=CARTESIAN_POINT('Ctrl Pts',(-2.17833689867943,-19.622576109491,10.8002771815604));
#84665=CARTESIAN_POINT('Ctrl Pts',(-2.17456948674399,-19.6238775578788,
10.800117324421));
#84666=CARTESIAN_POINT('Ctrl Pts',(-2.17082158489314,-19.6252282072342,
10.800000304529));
#84667=CARTESIAN_POINT('Origin',(-2.88680943605,-19.6742356128,11.5464017981));
#84668=CARTESIAN_POINT('Origin',(-2.20225291238,-19.6742356128,13.6795476588));
#84669=CARTESIAN_POINT('',(-2.8825676448599,-19.3742356866711,11.5596196699867));
#84670=CARTESIAN_POINT('Ctrl Pts',(-2.88256762736,-19.3742356128,11.5596196937));
#84671=CARTESIAN_POINT('Ctrl Pts',(-2.87949410326,-19.3742359194,11.555715524));
#84672=CARTESIAN_POINT('Ctrl Pts',(-2.87642049893,-19.3743066351,11.5518113974));
#84673=CARTESIAN_POINT('Ctrl Pts',(-2.87334791066,-19.3744480562,11.5479085637));
#84674=CARTESIAN_POINT('Ctrl Pts',(-2.87027737467,-19.3746601605,11.544008339));
#84675=CARTESIAN_POINT('Ctrl Pts',(-2.86720992947,-19.3749426154,11.5401120406));
#84676=CARTESIAN_POINT('',(-2.7374564764,-19.3742356128,12.011800398));
#84677=CARTESIAN_POINT('Origin',(0.,-19.3742356128,0.));
#84678=CARTESIAN_POINT('',(-4.88509763285,-19.3742356128,13.0374220375));
#84679=CARTESIAN_POINT('Ctrl Pts',(-2.47879655924,-19.4447372417,10.8888042378));
#84680=CARTESIAN_POINT('Ctrl Pts',(-2.4861493729,-19.4683844343,10.8942303744));
#84681=CARTESIAN_POINT('Ctrl Pts',(-2.49191208452,-19.4920316269,10.9018112135));
#84682=CARTESIAN_POINT('Ctrl Pts',(-2.49597515407,-19.5153269748,10.9114662072));
#84683=CARTESIAN_POINT('Ctrl Pts',(-2.49827725138,-19.5379188455,10.9230496178));
#84684=CARTESIAN_POINT('Ctrl Pts',(-2.49881059449,-19.5594864256,10.9363632033));
#84685=CARTESIAN_POINT('Ctrl Pts',(-2.44089425171,-19.4520187736,10.8608335));
#84686=CARTESIAN_POINT('Ctrl Pts',(-2.44963136368,-19.4748973849,10.8662112305));
#84687=CARTESIAN_POINT('Ctrl Pts',(-2.45702223689,-19.4977759963,10.8738380918));
#84688=CARTESIAN_POINT('Ctrl Pts',(-2.46293957656,-19.5203232432,10.8836363306));
#84689=CARTESIAN_POINT('Ctrl Pts',(-2.4672956606,-19.5422079505,10.8954618457));
#84690=CARTESIAN_POINT('Ctrl Pts',(-2.47004984489,-19.5631271909,10.9091164123));
#84691=CARTESIAN_POINT('Ctrl Pts',(-2.40004991429,-19.4606048121,10.8375867107));
#84692=CARTESIAN_POINT('Ctrl Pts',(-2.41019998813,-19.4825787168,10.8426296142));
#84693=CARTESIAN_POINT('Ctrl Pts',(-2.41925749864,-19.5045526216,10.8499715311));
#84694=CARTESIAN_POINT('Ctrl Pts',(-2.42707877395,-19.5262185084,10.8595420691));
#84695=CARTESIAN_POINT('Ctrl Pts',(-2.43355105359,-19.5472685228,10.8712051552));
#84696=CARTESIAN_POINT('Ctrl Pts',(-2.43860186298,-19.5674202148,10.8847702011));
#84697=CARTESIAN_POINT('Ctrl Pts',(-2.35714755108,-19.4705790255,10.8194836801));
#84698=CARTESIAN_POINT('Ctrl Pts',(-2.36865799258,-19.4915042786,10.8238986479));
#84699=CARTESIAN_POINT('Ctrl Pts',(-2.3793283911,-19.5124295317,10.8306149778));
#84700=CARTESIAN_POINT('Ctrl Pts',(-2.38900185162,-19.5330726947,10.839573774));
#84701=CARTESIAN_POINT('Ctrl Pts',(-2.3975442085,-19.5531518159,10.850652948));
#84702=CARTESIAN_POINT('Ctrl Pts',(-2.40485476239,-19.5724073147,10.863676829));
#84703=CARTESIAN_POINT('Ctrl Pts',(-2.27560738165,-19.4921831081,10.7955818101));
#84704=CARTESIAN_POINT('Ctrl Pts',(-2.2893900823,-19.510844473,10.7983487664));
#84705=CARTESIAN_POINT('Ctrl Pts',(-2.30277704132,-19.5295058379,10.8033357254));
#84706=CARTESIAN_POINT('Ctrl Pts',(-2.31559552336,-19.5479374484,10.8105100727));
#84707=CARTESIAN_POINT('Ctrl Pts',(-2.32768219961,-19.5659096429,10.8197835155));
#84708=CARTESIAN_POINT('Ctrl Pts',(-2.33889513807,-19.5832093643,10.8310183547));
#84709=CARTESIAN_POINT('Ctrl Pts',(-2.19384540622,-19.5207627351,10.7891484524));
#84710=CARTESIAN_POINT('Ctrl Pts',(-2.2092243494,-19.5364515236,10.7895844661));
#84711=CARTESIAN_POINT('Ctrl Pts',(-2.22456910998,-19.5521403122,10.7920171276));
#84712=CARTESIAN_POINT('Ctrl Pts',(-2.23970912867,-19.56765722,10.7964428));
#84713=CARTESIAN_POINT('Ctrl Pts',(-2.25447433499,-19.5828304221,10.8028133883));
#84714=CARTESIAN_POINT('Ctrl Pts',(-2.26870622615,-19.5974991706,10.8110393571));
#84715=CARTESIAN_POINT('Ctrl Pts',(-2.15676147687,-19.5361420848,10.7897230447));
#84716=CARTESIAN_POINT('Ctrl Pts',(-2.17269814184,-19.5502379741,10.7889802082));
#84717=CARTESIAN_POINT('Ctrl Pts',(-2.18874339027,-19.5643338633,10.7901046703));
#84718=CARTESIAN_POINT('Ctrl Pts',(-2.20473176783,-19.578285603,10.7931055871));
#84719=CARTESIAN_POINT('Ctrl Pts',(-2.22049530483,-19.591949083,10.7979533276));
#84720=CARTESIAN_POINT('Ctrl Pts',(-2.23587372456,-19.6051888511,10.8045811578));
#84721=CARTESIAN_POINT('Ctrl Pts',(-2.12065129512,-19.5532237866,10.7937022943));
#84722=CARTESIAN_POINT('Ctrl Pts',(-2.13693992507,-19.565556494,10.7917229743));
#84723=CARTESIAN_POINT('Ctrl Pts',(-2.15344959477,-19.5778892014,10.7914591884));
#84724=CARTESIAN_POINT('Ctrl Pts',(-2.1700239605,-19.5901054864,10.7929309325));
#84725=CARTESIAN_POINT('Ctrl Pts',(-2.18650229981,-19.6020889553,10.7961251723));
#84726=CARTESIAN_POINT('Ctrl Pts',(-2.20272856722,-19.6137296999,10.8009965235));
#84727=CARTESIAN_POINT('Ctrl Pts',(-2.08703817283,-19.5762208096,10.800197792));
#84728=CARTESIAN_POINT('Ctrl Pts',(-2.10348700925,-19.5861969598,10.7970192075));
#84729=CARTESIAN_POINT('Ctrl Pts',(-2.12023640403,-19.59617311,10.7953959802));
#84730=CARTESIAN_POINT('Ctrl Pts',(-2.13714159891,-19.6060614593,10.7953561328));
#84731=CARTESIAN_POINT('Ctrl Pts',(-2.1540525206,-19.6157742254,10.7969000191));
#84732=CARTESIAN_POINT('Ctrl Pts',(-2.17082158758,-19.625228211,10.8000003054));
#84733=CARTESIAN_POINT('',(-2.47879649228766,-19.4447371256487,10.8888042456754));
#84734=CARTESIAN_POINT('Origin',(-2.3006596926964,-19.4447370092007,11.1301921673071));
#84735=CARTESIAN_POINT('Ctrl Pts',(-2.47879653467762,-19.4447372464188,
10.8888042196737));
#84736=CARTESIAN_POINT('Ctrl Pts',(-2.46045463077369,-19.4482609676597,
10.8752684601721));
#84737=CARTESIAN_POINT('Ctrl Pts',(-2.44128408623476,-19.4521492663384,
10.8630639844833));
#84738=CARTESIAN_POINT('Ctrl Pts',(-2.42151329003282,-19.4564348686664,
10.8522709465103));
#84739=CARTESIAN_POINT('Ctrl Pts',(-2.40132346561323,-19.4608113013426,
10.8412491576352));
#84740=CARTESIAN_POINT('Ctrl Pts',(-2.38050875266403,-19.465602185527,10.8316993192422));
#84741=CARTESIAN_POINT('Ctrl Pts',(-2.35932627610263,-19.4708664875248,
10.8236593330656));
#84742=CARTESIAN_POINT('Ctrl Pts',(-2.33803965795491,-19.4761566709515,
10.8155798190788));
#84743=CARTESIAN_POINT('Ctrl Pts',(-2.31638283441941,-19.4819251433216,
10.8090249582489));
#84744=CARTESIAN_POINT('Ctrl Pts',(-2.29461341099357,-19.4882532179105,
10.803986219452));
#84745=CARTESIAN_POINT('Ctrl Pts',(-2.28619925943151,-19.4906990970524,
10.80203868455));
#84746=CARTESIAN_POINT('Ctrl Pts',(-2.27776815634791,-19.4932287863165,
10.8003171566218));
#84747=CARTESIAN_POINT('Ctrl Pts',(-2.2693342610873,-19.4958477330895,10.798819316362));
#84748=CARTESIAN_POINT('Ctrl Pts',(-2.25070834978327,-19.5016315694778,
10.7955113976644));
#84749=CARTESIAN_POINT('Ctrl Pts',(-2.23207171544287,-19.5078569454259,
10.7932947524955));
#84750=CARTESIAN_POINT('Ctrl Pts',(-2.213592013128,-19.5146534541264,10.7921199499763));
#84751=CARTESIAN_POINT('Ctrl Pts',(-2.20119473891072,-19.5192129530103,
10.7913318231584));
#84752=CARTESIAN_POINT('Ctrl Pts',(-2.18886677146711,-19.5240260825368,
10.791012665294));
#84753=CARTESIAN_POINT('Ctrl Pts',(-2.17665894379668,-19.52914744962,10.7911409237761));
#84754=CARTESIAN_POINT('Ctrl Pts',(-2.16571136803727,-19.5337401220962,
10.7912559417374));
#84755=CARTESIAN_POINT('Ctrl Pts',(-2.15486008673492,-19.5385797109364,
10.7917308495758));
#84756=CARTESIAN_POINT('Ctrl Pts',(-2.14414981251461,-19.5437418168646,
10.7925427409177));
#84757=CARTESIAN_POINT('Ctrl Pts',(-2.13433303459833,-19.5484732781172,
10.7932869008553));
#84758=CARTESIAN_POINT('Ctrl Pts',(-2.1246345745427,-19.5534752730665,10.7943141938894));
#84759=CARTESIAN_POINT('Ctrl Pts',(-2.11509897207031,-19.5588469738143,
10.7955997371279));
#84760=CARTESIAN_POINT('Ctrl Pts',(-2.10556336959791,-19.5642186745621,
10.7968852803664));
#84761=CARTESIAN_POINT('Ctrl Pts',(-2.09619036471992,-19.5699591730014,
10.7984291957784));
#84762=CARTESIAN_POINT('Ctrl Pts',(-2.08703817327717,-19.5762208095999,
10.8001977919136));
#84763=CARTESIAN_POINT('Origin',(-2.18190353865,-18.7742356128,11.2911158416));
#84764=CARTESIAN_POINT('',(-2.47879645562,-16.6742356128,10.8888042759));
#84765=CARTESIAN_POINT('',(-2.47879645562,-18.0594863082,10.8888042759));
#84766=CARTESIAN_POINT('Origin',(-2.18190353865,-16.6742356128,11.2911158416));
#84767=CARTESIAN_POINT('Ctrl Pts',(-2.47879645562,-19.4447370035,10.8888042759));
#84768=CARTESIAN_POINT('Ctrl Pts',(-2.48614926363,-19.4683842219,10.8942304132));
#84769=CARTESIAN_POINT('Ctrl Pts',(-2.4919119687,-19.4920314402,10.901811256));
#84770=CARTESIAN_POINT('Ctrl Pts',(-2.49597503074,-19.515326813,10.9114662563));
#84771=CARTESIAN_POINT('Ctrl Pts',(-2.49827711961,-19.5379187068,10.9230496761));
#84772=CARTESIAN_POINT('Ctrl Pts',(-2.49881045348,-19.5594863076,10.9363632729));
#84773=CARTESIAN_POINT('Ctrl Pts',(-2.510543559,-19.4294897509,10.9122326109));
#84774=CARTESIAN_POINT('Ctrl Pts',(-2.52509315654,-19.4549860554,10.9229697266));
#84775=CARTESIAN_POINT('Ctrl Pts',(-2.53743184504,-19.4804823599,10.9367027854));
#84776=CARTESIAN_POINT('Ctrl Pts',(-2.54730011106,-19.5054619039,10.9532408984));
#84777=CARTESIAN_POINT('Ctrl Pts',(-2.55452473408,-19.52940842,10.9722767674));
#84778=CARTESIAN_POINT('Ctrl Pts',(-2.55903583297,-19.5518626834,10.9934181309));
#84779=CARTESIAN_POINT('Ctrl Pts',(-2.54358798483,-19.3961031493,10.9366183279));
#84780=CARTESIAN_POINT('Ctrl Pts',(-2.56490210185,-19.4257202286,10.9523474783));
#84781=CARTESIAN_POINT('Ctrl Pts',(-2.58262930917,-19.4553373078,10.972937153));
#84782=CARTESIAN_POINT('Ctrl Pts',(-2.59620857289,-19.4840367355,10.997975939));
#84783=CARTESIAN_POINT('Ctrl Pts',(-2.60527727222,-19.5109029172,11.0267904888));
#84784=CARTESIAN_POINT('Ctrl Pts',(-2.60971873368,-19.5351693857,11.0585616091));
#84785=CARTESIAN_POINT('Ctrl Pts',(-2.57980368735,-19.3527485635,10.9633443444));
#84786=CARTESIAN_POINT('Ctrl Pts',(-2.60698188591,-19.3880359645,10.9834009889));
#84787=CARTESIAN_POINT('Ctrl Pts',(-2.62854104782,-19.4233233655,11.011071838));
#84788=CARTESIAN_POINT('Ctrl Pts',(-2.64323454282,-19.4570166595,11.0454386344));
#84789=CARTESIAN_POINT('Ctrl Pts',(-2.65023339726,-19.4875204033,11.0850019677));
#84790=CARTESIAN_POINT('Ctrl Pts',(-2.64928177187,-19.5134920611,11.1278449523));
#84791=CARTESIAN_POINT('Ctrl Pts',(-2.66373575496,-19.2547159387,11.0252834944));
#84792=CARTESIAN_POINT('Ctrl Pts',(-2.69872898986,-19.3050683152,11.0511073573));
#84793=CARTESIAN_POINT('Ctrl Pts',(-2.72330881282,-19.3554206917,11.0910421533));
#84794=CARTESIAN_POINT('Ctrl Pts',(-2.73408042005,-19.4013898853,11.1426264261));
#84795=CARTESIAN_POINT('Ctrl Pts',(-2.72955068062,-19.4386199009,11.2009208948));
#84796=CARTESIAN_POINT('Ctrl Pts',(-2.71098021085,-19.4644758001,11.2604631973));
#84797=CARTESIAN_POINT('Ctrl Pts',(-2.78975290654,-19.1524485557,11.1182800744));
#84798=CARTESIAN_POINT('Ctrl Pts',(-2.82090969201,-19.2230604651,11.1412727847));
#84799=CARTESIAN_POINT('Ctrl Pts',(-2.83638207721,-19.2936723745,11.1855190018));
#84800=CARTESIAN_POINT('Ctrl Pts',(-2.83135807356,-19.3541924937,11.2476786502));
#84801=CARTESIAN_POINT('Ctrl Pts',(-2.80630726796,-19.3949915084,11.3177423125));
#84802=CARTESIAN_POINT('Ctrl Pts',(-2.76681414133,-19.4133420624,11.3857731806));
#84803=CARTESIAN_POINT('Ctrl Pts',(-2.86129530492,-19.1091646129,11.1710760494));
#84804=CARTESIAN_POINT('Ctrl Pts',(-2.88687394597,-19.1898640218,11.1899522282));
#84805=CARTESIAN_POINT('Ctrl Pts',(-2.89447935536,-19.2705634307,11.2331834474));
#84806=CARTESIAN_POINT('Ctrl Pts',(-2.87932742318,-19.3377754042,11.2975635634));
#84807=CARTESIAN_POINT('Ctrl Pts',(-2.84388765021,-19.3788647517,11.3707877234));
#84808=CARTESIAN_POINT('Ctrl Pts',(-2.796245355,-19.3917000854,11.4409843867));
#84809=CARTESIAN_POINT('Ctrl Pts',(-2.94208651244,-19.0824256558,11.2306973462));
#84810=CARTESIAN_POINT('Ctrl Pts',(-2.95834742078,-19.1709113574,11.2426973703));
#84811=CARTESIAN_POINT('Ctrl Pts',(-2.9547674495,-19.2593970589,11.2815832341));
#84812=CARTESIAN_POINT('Ctrl Pts',(-2.92789987303,-19.3312626769,11.3452494815));
#84813=CARTESIAN_POINT('Ctrl Pts',(-2.88323668464,-19.3712611943,11.4201106412));
#84814=CARTESIAN_POINT('Ctrl Pts',(-2.83073115845,-19.3783306343,11.4925686116));
#84815=CARTESIAN_POINT('Ctrl Pts',(-3.0257458739,-19.0756496396,11.2924352478));
#84816=CARTESIAN_POINT('Ctrl Pts',(-3.03060872632,-19.1683851734,11.2960238755));
#84817=CARTESIAN_POINT('Ctrl Pts',(-3.01410418365,-19.2611207071,11.3285668827));
#84818=CARTESIAN_POINT('Ctrl Pts',(-2.97498276954,-19.334976222,11.3896852328));
#84819=CARTESIAN_POINT('Ctrl Pts',(-2.92227176474,-19.372909531,11.465275844));
#84820=CARTESIAN_POINT('Ctrl Pts',(-2.86720977988,-19.3749426262,11.5401119926));
#84821=CARTESIAN_POINT('',(-3.0257458739,-19.0756502088,11.2924352478));
#84822=CARTESIAN_POINT('Origin',(-2.84896336891823,-19.0776979407904,11.5322135659977));
#84823=CARTESIAN_POINT('Ctrl Pts',(-3.02574587389968,-19.0756502088,11.2924352478004));
#84824=CARTESIAN_POINT('Ctrl Pts',(-3.00675351565961,-19.0771882002878,
11.2784195019978));
#84825=CARTESIAN_POINT('Ctrl Pts',(-2.98794556110458,-19.0799656124685,
11.2645398401506));
#84826=CARTESIAN_POINT('Ctrl Pts',(-2.96946444777136,-19.0838689703512,
11.2509013765509));
#84827=CARTESIAN_POINT('Ctrl Pts',(-2.95255124090799,-19.0874411739377,
11.2384199771892));
#84828=CARTESIAN_POINT('Ctrl Pts',(-2.93591148075212,-19.0919553471003,
11.2261403726466));
#84829=CARTESIAN_POINT('Ctrl Pts',(-2.91963473242905,-19.0972951829733,
11.2141286590785));
#84830=CARTESIAN_POINT('Ctrl Pts',(-2.90097606500497,-19.1034164437851,
11.2003591662896));
#84831=CARTESIAN_POINT('Ctrl Pts',(-2.88279745671413,-19.1106246716873,
11.1869439416157));
#84832=CARTESIAN_POINT('Ctrl Pts',(-2.86521289932878,-19.1187068763404,
11.1739671072852));
#84833=CARTESIAN_POINT('Ctrl Pts',(-2.85069831160009,-19.1253780632181,
11.16325581122));
#84834=CARTESIAN_POINT('Ctrl Pts',(-2.83658785784503,-19.1326436742646,
11.1528427529497));
#84835=CARTESIAN_POINT('Ctrl Pts',(-2.82292669530417,-19.140371437611,11.142761257057));
#84836=CARTESIAN_POINT('Ctrl Pts',(-2.80596470462133,-19.1499663933469,
11.1302438568071));
#84837=CARTESIAN_POINT('Ctrl Pts',(-2.78969874364794,-19.1602717602212,
11.1182401039592));
#84838=CARTESIAN_POINT('Ctrl Pts',(-2.7741716633805,-19.1710306210649,11.1067816211666));
#84839=CARTESIAN_POINT('Ctrl Pts',(-2.76433010714757,-19.1778499285053,
11.0995188711321));
#84840=CARTESIAN_POINT('Ctrl Pts',(-2.75478457692901,-19.1848513153056,
11.0924745787183));
#84841=CARTESIAN_POINT('Ctrl Pts',(-2.74553729325106,-19.1919708669864,
11.0856503826122));
#84842=CARTESIAN_POINT('Ctrl Pts',(-2.73213768965327,-19.2022873202974,
11.075761908777));
#84843=CARTESIAN_POINT('Ctrl Pts',(-2.7193444588255,-19.2128634993548,11.0663209183868));
#84844=CARTESIAN_POINT('Ctrl Pts',(-2.70715916076948,-19.2235067787786,
11.0573285627176));
#84845=CARTESIAN_POINT('Ctrl Pts',(-2.69769192270529,-19.2317759618241,
11.0503420473704));
#84846=CARTESIAN_POINT('Ctrl Pts',(-2.68859091957648,-19.2400856488052,
11.0436258015626));
#84847=CARTESIAN_POINT('Ctrl Pts',(-2.67984102302334,-19.2483550306415,
11.0371686610452));
#84848=CARTESIAN_POINT('Ctrl Pts',(-2.66553704813159,-19.2618734796242,
11.026612790439));
#84849=CARTESIAN_POINT('Ctrl Pts',(-2.65214757506909,-19.2753062681188,
11.0167317926194));
#84850=CARTESIAN_POINT('Ctrl Pts',(-2.63954076934534,-19.2884074477262,
11.0074283780573));
#84851=CARTESIAN_POINT('Ctrl Pts',(-2.63452172045956,-19.2936233178166,
11.0037244824381));
#84852=CARTESIAN_POINT('Ctrl Pts',(-2.62962657043066,-19.2987872244217,
11.0001120201687));
#84853=CARTESIAN_POINT('Ctrl Pts',(-2.6248465335031,-19.3038857598675,10.9965845076172));
#84854=CARTESIAN_POINT('Ctrl Pts',(-2.60806283236651,-19.3217877753653,
10.9841986793659));
#84855=CARTESIAN_POINT('Ctrl Pts',(-2.59269322531019,-19.3388823165721,
10.972856406431));
#84856=CARTESIAN_POINT('Ctrl Pts',(-2.57833633556526,-19.3547066387323,
10.9622614863181));
#84857=CARTESIAN_POINT('Ctrl Pts',(-2.56468487008995,-19.3697534344852,
10.9521871464922));
#84858=CARTESIAN_POINT('Ctrl Pts',(-2.55194665981057,-19.3836622157048,
10.9427867595277));
#84859=CARTESIAN_POINT('Ctrl Pts',(-2.53980373411162,-19.396024813606,10.9338256733092));
#84860=CARTESIAN_POINT('Ctrl Pts',(-2.53017587314596,-19.4058268478701,
10.926720623476));
#84861=CARTESIAN_POINT('Ctrl Pts',(-2.52092740821589,-19.4146616173831,
10.9198955559181));
#84862=CARTESIAN_POINT('Ctrl Pts',(-2.51192137185923,-19.4222801308466,
10.9132493927221));
#84863=CARTESIAN_POINT('Ctrl Pts',(-2.50956800534002,-19.4242709238882,
10.9115126844381));
#84864=CARTESIAN_POINT('Ctrl Pts',(-2.50723135998009,-19.4261785010644,
10.9097883158081));
#84865=CARTESIAN_POINT('Ctrl Pts',(-2.50490937729373,-19.4279980029771,
10.9080747677192));
#84866=CARTESIAN_POINT('Ctrl Pts',(-2.49828731261426,-19.43318704225,10.9031878982596));
#84867=CARTESIAN_POINT('Ctrl Pts',(-2.49177954925272,-19.4376614176956,
10.8983853790159));
#84868=CARTESIAN_POINT('Ctrl Pts',(-2.48534852651507,-19.4413044184337,
10.8936394922355));
#84869=CARTESIAN_POINT('Ctrl Pts',(-2.48315653562045,-19.44254612209,10.8920218738514));
#84870=CARTESIAN_POINT('Ctrl Pts',(-2.48097305807628,-19.4436916418333,
10.8904105380807));
#84871=CARTESIAN_POINT('Ctrl Pts',(-2.47879645562,-19.4447370035,10.8888042759));
#84872=CARTESIAN_POINT('Ctrl Pts',(-3.02574587396,-19.0756502088,11.2924352478));
#84873=CARTESIAN_POINT('Ctrl Pts',(-3.03060876213,-19.1683856419,11.2960239029));
#84874=CARTESIAN_POINT('Ctrl Pts',(-3.0141042599,-19.261121075,11.3285669311));
#84875=CARTESIAN_POINT('Ctrl Pts',(-2.97498288462,-19.3349765133,11.3896852899));
#84876=CARTESIAN_POINT('Ctrl Pts',(-2.9222719047,-19.3729097939,11.465275899));
#84877=CARTESIAN_POINT('Ctrl Pts',(-2.86720992778,-19.3749429031,11.5401120401));
#84878=CARTESIAN_POINT('Ctrl Pts',(-3.03447355616,-19.0749433453,11.2988759949));
#84879=CARTESIAN_POINT('Ctrl Pts',(-3.03813896473,-19.1681049521,11.3015809487));
#84880=CARTESIAN_POINT('Ctrl Pts',(-3.02028592653,-19.2612665588,11.3334449681));
#84881=CARTESIAN_POINT('Ctrl Pts',(-2.97989655367,-19.3353233942,11.3942703053));
#84882=CARTESIAN_POINT('Ctrl Pts',(-2.92636073645,-19.3730546128,11.4699120931));
#84883=CARTESIAN_POINT('Ctrl Pts',(-2.87104425856,-19.3745894729,11.5449824418));
#84884=CARTESIAN_POINT('Ctrl Pts',(-3.04321296595,-19.0744719442,11.3053253965));
#84885=CARTESIAN_POINT('Ctrl Pts',(-3.04566841653,-19.1680282232,11.3071374404));
#84886=CARTESIAN_POINT('Ctrl Pts',(-3.02645347241,-19.2615845022,11.3383144504));
#84887=CARTESIAN_POINT('Ctrl Pts',(-2.9847889853,-19.3358150142,11.3988454565));
#84888=CARTESIAN_POINT('Ctrl Pts',(-2.93043564473,-19.3733247573,11.4745447401));
#84889=CARTESIAN_POINT('Ctrl Pts',(-2.87488373803,-19.3743537743,11.5498593869));
#84890=CARTESIAN_POINT('Ctrl Pts',(-3.05195820325,-19.0742362318,11.3117790986));
#84891=CARTESIAN_POINT('Ctrl Pts',(-3.0531916857,-19.1681548312,11.3126893695));
#84892=CARTESIAN_POINT('Ctrl Pts',(-3.03260202102,-19.2620734306,11.3431715971));
#84893=CARTESIAN_POINT('Ctrl Pts',(-2.98965603461,-19.3364495577,11.4034071424));
#84894=CARTESIAN_POINT('Ctrl Pts',(-2.93449336502,-19.3737189989,11.4791704265));
#84895=CARTESIAN_POINT('Ctrl Pts',(-2.87872577363,-19.3742359202,11.5547395826));
#84896=CARTESIAN_POINT('Ctrl Pts',(-3.06070337749,-19.0742362041,11.3182327542));
#84897=CARTESIAN_POINT('Ctrl Pts',(-3.06070341502,-19.1684838804,11.3182327825));
#84898=CARTESIAN_POINT('Ctrl Pts',(-3.0387268402,-19.2627315566,11.3480127241));
#84899=CARTESIAN_POINT('Ctrl Pts',(-2.9944937393,-19.3372249046,11.4079518654));
#84900=CARTESIAN_POINT('Ctrl Pts',(-2.93853076799,-19.3742358919,11.4837858067));
#84901=CARTESIAN_POINT('Ctrl Pts',(-2.88256777785,-19.3742359083,11.5596197419));
#84902=CARTESIAN_POINT('',(-3.06070337744081,-19.0742359088556,11.3182327542666));
#84903=CARTESIAN_POINT('Origin',(-2.88382717324306,-19.0763574922431,11.5579128187659));
#84904=CARTESIAN_POINT('Origin',(-3.06701733419236,-19.6773931794005,11.3228922010275));
#84905=CARTESIAN_POINT('Origin',(-4.88509763285,-19.0742356128,13.0374220375));
#84906=CARTESIAN_POINT('',(-5.27647385588,-19.0742356128,12.9533996668));
#84907=CARTESIAN_POINT('Origin',(-2.3,-16.6742356128,10.7568582774));
#84908=CARTESIAN_POINT('',(-7.49224433422,-16.6742356128,14.5885665792));
#84909=CARTESIAN_POINT('Origin',(-14.0872311983,-16.6742356128,1.01503102594));
#84910=CARTESIAN_POINT('',(-14.9221240862,-16.6742356128,1.52650344091));
#84911=CARTESIAN_POINT('',(-14.9221240862,-16.6742356128,1.52650344091));
#84912=CARTESIAN_POINT('',(-14.9221240862,-19.3742356128,1.52650344091));
#84913=CARTESIAN_POINT('',(-14.9221240862,-18.0242356128,1.52650344091));
#84914=CARTESIAN_POINT('',(-15.57788482,-19.3742356128,1.92823584397));
#84915=CARTESIAN_POINT('Origin',(-13.4419608479,-16.6742356128,-0.619725245787));
#84916=CARTESIAN_POINT('',(-14.8362431871,-19.3742356128,-1.4738910501));
#84917=CARTESIAN_POINT('',(-15.5349443705,-19.3742356128,-1.90192964856));
#84918=CARTESIAN_POINT('',(-14.8362431871,-16.6742356128,-1.4738910501));
#84919=CARTESIAN_POINT('',(-14.8362431871,-18.0242356128,-1.4738910501));
#84920=CARTESIAN_POINT('',(-14.8362431871,-16.6742356128,-1.4738910501));
#84921=CARTESIAN_POINT('Origin',(0.,-18.0242356128,0.));
#84922=CARTESIAN_POINT('',(-14.976285439,-19.3742356128,-0.843133708384));
#84923=CARTESIAN_POINT('Origin',(0.,-19.3742356128,0.));
#84924=CARTESIAN_POINT('',(-14.976285439,-16.6742356128,-0.843133708384));
#84925=CARTESIAN_POINT('Origin',(3.5527136788005E-13,-16.6742356128,5.24580379135386E-14));
#84926=CARTESIAN_POINT('',(-14.976285439,-18.0242356128,-0.843133708384));
#84927=CARTESIAN_POINT('Origin',(-12.9794473804,-18.0242356128,-0.730715880599));
#84928=CARTESIAN_POINT('Origin',(-12.9794473804,-16.6742356128,-0.730715880599));
#84929=CARTESIAN_POINT('Origin',(-12.9794473804,-19.3742356128,-0.730715880599));
#84930=CARTESIAN_POINT('Origin',(0.,-18.0242356128,0.));
#84931=CARTESIAN_POINT('',(-13.4786568951,-19.3742356128,-0.758820337546));
#84932=CARTESIAN_POINT('',(-13.4786568951,-16.6742356128,-0.758820337546));
#84933=CARTESIAN_POINT('',(-13.4786568951,-18.0242356128,-0.758820337546));
#84934=CARTESIAN_POINT('',(-13.3555478213,-16.6742356128,1.96960462883));
#84935=CARTESIAN_POINT('Origin',(-1.04360964314765E-13,-16.6742356128,-1.24761312392252E-13));
#84936=CARTESIAN_POINT('',(-13.3555478213,-19.3742356128,1.96960462883));
#84937=CARTESIAN_POINT('',(-13.3555478213,-18.0242356128,1.96960462883));
#84938=CARTESIAN_POINT('Origin',(0.,-19.3742356128,0.));
#84939=CARTESIAN_POINT('Origin',(-12.9794473804,-18.0242356128,-0.730715880599));
#84940=CARTESIAN_POINT('',(-13.1249762208,-16.6742356128,-1.20906863394));
#84941=CARTESIAN_POINT('',(-13.1249762208,-19.3742356128,-1.20906863394));
#84942=CARTESIAN_POINT('',(-13.1249762208,-18.0242356128,-1.20906863394));
#84943=CARTESIAN_POINT('Origin',(-12.9794473804,-16.6742356128,-0.730715880598998));
#84944=CARTESIAN_POINT('Origin',(-12.9794473804,-19.3742356128,-0.730715880599));
#84945=CARTESIAN_POINT('Origin',(-13.2705050612,-18.0242356128,-1.68742138727));
#84946=CARTESIAN_POINT('',(-13.0093116937,-19.3742356128,-2.11377572911));
#84947=CARTESIAN_POINT('Origin',(-13.2705050612,-19.3742356128,-1.68742138727));
#84948=CARTESIAN_POINT('',(-13.0093116937,-16.6742356128,-2.11377572911));
#84949=CARTESIAN_POINT('',(-13.0093116937,-18.0242356128,-2.11377572911));
#84950=CARTESIAN_POINT('Origin',(-13.2705050612,-16.6742356128,-1.68742138727));
#84951=CARTESIAN_POINT('Origin',(-12.6583807456,-16.6742356128,-1.8987882713));
#84952=CARTESIAN_POINT('',(-14.4691278654,-19.3742356128,-3.00808889615));
#84953=CARTESIAN_POINT('',(-15.9289440371,-16.6742356128,-3.90240206319));
#84954=CARTESIAN_POINT('Origin',(-13.8501977406,-18.0242356128,2.04255294841));
#84955=CARTESIAN_POINT('',(-13.5890043731,-19.3742356128,2.46890729025));
#84956=CARTESIAN_POINT('Origin',(-13.8501977406,-19.3742356128,2.04255294841));
#84957=CARTESIAN_POINT('',(-13.5890043731,-16.6742356128,2.46890729025));
#84958=CARTESIAN_POINT('Origin',(-13.8501977406,-16.6742356128,2.04255294841));
#84959=CARTESIAN_POINT('',(-13.5890043731,-18.0242356128,2.46890729025));
#84960=CARTESIAN_POINT('Origin',(0.,-19.3742356128,0.));
#84961=CARTESIAN_POINT('',(-14.7589742051,-19.3742356128,3.18565467672));
#84962=CARTESIAN_POINT('Origin',(-13.303651096,-16.6742356128,2.29409405145));
#84963=CARTESIAN_POINT('',(-13.5890043731,-16.6742356128,2.46890729025));
#84964=CARTESIAN_POINT('Origin',(5.,-39.2742356128,0.));
#84965=CARTESIAN_POINT('',(5.,-35.2742356128,-16.5096094653));
#84966=CARTESIAN_POINT('',(5.,-38.7742356128,0.1339280819));
#84967=CARTESIAN_POINT('Origin',(4.,-35.2742356128,-16.5096094653));
#84968=CARTESIAN_POINT('',(4.,-34.2742356128,-16.4193528851));
#84969=CARTESIAN_POINT('Origin',(5.,-34.2742356128,0.));
#84970=CARTESIAN_POINT('',(-4.,-34.2742356128,-16.5096094653));
#84971=CARTESIAN_POINT('Origin',(-4.,-35.2742356128,-16.5096094653));
#84972=CARTESIAN_POINT('',(-5.,-35.2742356128,-16.1426761277));
#84973=CARTESIAN_POINT('Origin',(-5.,-39.2742356128,0.));
#84974=CARTESIAN_POINT('',(-5.,-38.7742356128,0.1339280819));
#84975=CARTESIAN_POINT('Origin',(4.,-39.2742356128,0.));
#84976=CARTESIAN_POINT('',(4.,-35.2742356128,16.6523581408));
#84977=CARTESIAN_POINT('',(4.,-38.7742356128,0.213056290446));
#84978=CARTESIAN_POINT('Origin',(3.,-35.2742356128,16.6523581408));
#84979=CARTESIAN_POINT('',(3.,-34.2742356128,16.631351665));
#84980=CARTESIAN_POINT('Origin',(5.,-34.2742356128,0.));
#84981=CARTESIAN_POINT('',(-3.,-34.2742356128,16.6523581408));
#84982=CARTESIAN_POINT('Origin',(-3.,-35.2742356128,16.6523581408));
#84983=CARTESIAN_POINT('',(-4.,-35.2742356128,16.4206921659));
#84984=CARTESIAN_POINT('Origin',(-4.,-39.2742356128,0.));
#84985=CARTESIAN_POINT('',(-4.,-38.7742356128,0.213056290446));
#84986=CARTESIAN_POINT('Origin',(-5.5,-38.7742356128,0.1339280819));
#84987=CARTESIAN_POINT('',(-5.5,-39.2742356128,-15.9790598121));
#84988=CARTESIAN_POINT('Origin',(-4.5,-38.7742356128,0.213056290446));
#84989=CARTESIAN_POINT('',(-4.5,-39.2742356128,16.2892879764));
#84990=CARTESIAN_POINT('Origin',(0.,-39.2742356128,17.4));
#84991=CARTESIAN_POINT('Origin',(5.5,-38.7742356128,0.1339280819));
#84992=CARTESIAN_POINT('',(5.5,-39.2742356128,-15.9790598121));
#84993=CARTESIAN_POINT('Origin',(4.5,-38.7742356128,0.213056290446));
#84994=CARTESIAN_POINT('',(4.5,-39.2742356128,16.2892879764));
#84995=CARTESIAN_POINT('Origin',(0.,-39.2742356128,17.4));
#84996=CARTESIAN_POINT('Origin',(0.,-21.7742356128,0.));
#84997=CARTESIAN_POINT('',(-4.38674367823,-16.6742356128,-8.0298804413));
#84998=CARTESIAN_POINT('Origin',(-2.22044604925031E-15,-16.6742356128,-2.22044604925031E-15));
#84999=CARTESIAN_POINT('',(-4.38674367822846,-21.7742356128,-8.02988044129691));
#85000=CARTESIAN_POINT('Origin',(0.,-16.6742356128,17.4));
#85001=CARTESIAN_POINT('Origin',(0.,-16.6742356128,17.4));
#85002=CARTESIAN_POINT('Origin',(0.,-16.6742356128,17.4));
#85003=CARTESIAN_POINT('Origin',(0.,-16.6742356128,17.4));
#85004=CARTESIAN_POINT('Origin',(0.,-16.6742356128,17.4));
#85005=CARTESIAN_POINT('Origin',(0.,-16.6742356128,17.4));
#85006=CARTESIAN_POINT('Origin',(0.,-14.6742356128,17.4));
#85007=CARTESIAN_POINT('',(3.90056490239326,-14.6742356128,10.5597900654496));
#85008=CARTESIAN_POINT('',(7.1947640041133,-14.6742356128,8.65788332730725));
#85009=CARTESIAN_POINT('Origin',(0.,-14.6742356128,0.));
#85010=CARTESIAN_POINT('',(-3.90056490239319,-14.6742356128,10.5597900654496));
#85011=CARTESIAN_POINT('',(3.75578649684289E-14,-14.6742356128,10.5597900654496));
#85012=CARTESIAN_POINT('',(-7.19476400411325,-14.6742356128,8.65788332730729));
#85013=CARTESIAN_POINT('Origin',(0.,-14.6742356128,0.));
#85014=CARTESIAN_POINT('',(-11.0953289065065,-14.6742356128,1.9019067381423));
#85015=CARTESIAN_POINT('',(-9.14504645530986,-14.6742356128,5.27989503272479));
#85016=CARTESIAN_POINT('',(-11.0953289065065,-14.6742356128,-1.90190673814234));
#85017=CARTESIAN_POINT('Origin',(0.,-14.6742356128,0.));
#85018=CARTESIAN_POINT('',(-7.1947640041134,-14.6742356128,-8.65788332730717));
#85019=CARTESIAN_POINT('',(-9.14504645530993,-14.6742356128,-5.27989503272475));
#85020=CARTESIAN_POINT('',(-3.90056490239334,-14.6742356128,-10.5597900654495));
#85021=CARTESIAN_POINT('Origin',(0.,-14.6742356128,0.));
#85022=CARTESIAN_POINT('',(3.90056490239312,-14.6742356128,-10.5597900654496));
#85023=CARTESIAN_POINT('',(-1.11171280306549E-13,-14.6742356128,-10.5597900654496));
#85024=CARTESIAN_POINT('',(7.19476400411319,-14.6742356128,-8.65788332730735));
#85025=CARTESIAN_POINT('Origin',(0.,-14.6742356128,0.));
#85026=CARTESIAN_POINT('',(11.0953289065065,-14.6742356128,-1.90190673814237));
#85027=CARTESIAN_POINT('',(9.14504645530982,-14.6742356128,-5.27989503272486));
#85028=CARTESIAN_POINT('',(11.0953289065065,-14.6742356128,1.90190673814221));
#85029=CARTESIAN_POINT('Origin',(0.,-14.6742356128,0.));
#85030=CARTESIAN_POINT('',(9.14504645530989,-14.6742356128,5.27989503272473));
#85031=CARTESIAN_POINT('Origin',(3.75578649684289E-14,26.5953441711815,
10.5597900654496));
#85032=CARTESIAN_POINT('',(3.90056490239326,26.5953441711815,10.5597900654496));
#85033=CARTESIAN_POINT('',(-3.90056490239319,26.5953441711815,10.5597900654496));
#85034=CARTESIAN_POINT('Origin',(0.,26.5953441711815,0.));
#85035=CARTESIAN_POINT('',(7.1947640041133,26.5953441711815,8.65788332730725));
#85036=CARTESIAN_POINT('Origin',(9.14504645530989,26.5953441711815,5.27989503272473));
#85037=CARTESIAN_POINT('',(11.0953289065065,26.5953441711815,1.90190673814221));
#85038=CARTESIAN_POINT('Origin',(0.,26.5953441711815,0.));
#85039=CARTESIAN_POINT('',(11.0953289065065,-6.63753909988913,-1.90190673814237));
#85040=CARTESIAN_POINT('',(11.0953289065065,26.5953441711815,-1.90190673814237));
#85041=CARTESIAN_POINT('Origin',(0.,-6.63753909988913,0.));
#85042=CARTESIAN_POINT('Origin',(9.14504645530982,26.5953441711815,-5.27989503272486));
#85043=CARTESIAN_POINT('',(7.19476400411318,-6.63753909988913,-8.65788332730734));
#85044=CARTESIAN_POINT('',(7.19476400411319,26.5953441711815,-8.65788332730735));
#85045=CARTESIAN_POINT('Ctrl Pts',(7.19476400411318,-6.63753909988913,-8.65788332730735));
#85046=CARTESIAN_POINT('Ctrl Pts',(7.20793342429826,-6.25115677756999,-8.63507322244056));
#85047=CARTESIAN_POINT('Ctrl Pts',(7.22957597298824,-5.92703963684599,-8.59758722850423));
#85048=CARTESIAN_POINT('Ctrl Pts',(7.33264605094296,-5.4824893351699,-8.41906461674658));
#85049=CARTESIAN_POINT('Ctrl Pts',(7.38587885165349,-5.33005160890808,-8.32686270128674));
#85050=CARTESIAN_POINT('Ctrl Pts',(7.55351534711876,-5.02205392516981,-8.03650777393812));
#85051=CARTESIAN_POINT('Ctrl Pts',(7.68241549558792,-4.85741613145686,-7.81324616768638));
#85052=CARTESIAN_POINT('Ctrl Pts',(8.07805804686918,-4.55925658398797,-7.12797316723107));
#85053=CARTESIAN_POINT('Ctrl Pts',(8.2987360820476,-4.46102644577706,-6.74574759818758));
#85054=CARTESIAN_POINT('Ctrl Pts',(8.61875324812248,-4.36808225563921,-6.19146160725169));
#85055=CARTESIAN_POINT('Ctrl Pts',(8.73033406055812,-4.34507072735135,-5.99819797096336));
#85056=CARTESIAN_POINT('Ctrl Pts',(8.89953062521147,-4.32271936364378,-5.70514092451763));
#85057=CARTESIAN_POINT('Ctrl Pts',(8.95774725247859,-4.31728665962078,-5.60430676824569));
#85058=CARTESIAN_POINT('Ctrl Pts',(9.05873727376944,-4.31167125033784,-5.42938692031248));
#85059=CARTESIAN_POINT('Ctrl Pts',(9.10160080381223,-4.31047752426155,-5.35514510848663));
#85060=CARTESIAN_POINT('Ctrl Pts',(9.18843216468531,-4.31045476730958,-5.20474877976411));
#85061=CARTESIAN_POINT('Ctrl Pts',(9.23245827883154,-4.31169063776257,-5.1284933132029));
#85062=CARTESIAN_POINT('Ctrl Pts',(9.33992086438215,-4.3177710909309,-4.94236265511655));
#85063=CARTESIAN_POINT('Ctrl Pts',(9.40346807156964,-4.32398244074384,-4.83229566358879));
#85064=CARTESIAN_POINT('Ctrl Pts',(9.5916439749527,-4.35037319724934,-4.50636543816916));
#85065=CARTESIAN_POINT('Ctrl Pts',(9.71718683007716,-4.37846636964572,-4.28891883456635));
#85066=CARTESIAN_POINT('Ctrl Pts',(10.0959505184882,-4.5002770190838,-3.63288088217621));
#85067=CARTESIAN_POINT('Ctrl Pts',(10.3416323810413,-4.63190537710699,-3.20734741373611));
#85068=CARTESIAN_POINT('Ctrl Pts',(10.7018033055628,-4.96923903784649,-2.58351307305582));
#85069=CARTESIAN_POINT('Ctrl Pts',(10.8039037926238,-5.13032755416942,-2.4066698419886));
#85070=CARTESIAN_POINT('Ctrl Pts',(10.9344613444125,-5.41302767928334,-2.18053752897883));
#85071=CARTESIAN_POINT('Ctrl Pts',(10.9804393462862,-5.56176401030052,-2.10090129370317));
#85072=CARTESIAN_POINT('Ctrl Pts',(11.0647640875135,-5.9935176192942,-1.95484655756232));
#85073=CARTESIAN_POINT('Ctrl Pts',(11.0834813101589,-6.28993823923298,-1.92242737696393));
#85074=CARTESIAN_POINT('Ctrl Pts',(11.0953289065065,-6.63753909988913,-1.90190673814236));
#85075=CARTESIAN_POINT('Origin',(0.,26.5953441711815,0.));
#85076=CARTESIAN_POINT('',(3.90056490239312,-6.63753909988913,-10.5597900654496));
#85077=CARTESIAN_POINT('',(3.90056490239312,26.5953441711815,-10.5597900654496));
#85078=CARTESIAN_POINT('Origin',(0.,-6.63753909988913,0.));
#85079=CARTESIAN_POINT('Origin',(-1.11171280306549E-13,26.5953441711815,
-10.5597900654496));
#85080=CARTESIAN_POINT('',(-3.90056490239334,-6.63753909988913,-10.5597900654495));
#85081=CARTESIAN_POINT('',(-3.90056490239334,26.5953441711815,-10.5597900654495));
#85082=CARTESIAN_POINT('Ctrl Pts',(-3.90056490239333,-6.63753909988912,
-10.5597900654495));
#85083=CARTESIAN_POINT('Ctrl Pts',(-3.88650640714021,-6.43130549325069,
-10.5597900654495));
#85084=CARTESIAN_POINT('Ctrl Pts',(-3.86750921833438,-6.24077478304535,
-10.5597900654495));
#85085=CARTESIAN_POINT('Ctrl Pts',(-3.79603527122593,-5.88328867547882,
-10.5597900654495));
#85086=CARTESIAN_POINT('Ctrl Pts',(-3.74111739908583,-5.70969285765481,
-10.5597900656594));
#85087=CARTESIAN_POINT('Ctrl Pts',(-3.56226471943126,-5.38996752638052,
-10.5597900656594));
#85088=CARTESIAN_POINT('Ctrl Pts',(-3.4385859282338,-5.23989257637364,-10.5597900654495));
#85089=CARTESIAN_POINT('Ctrl Pts',(-2.92900810424285,-4.84096372109965,
-10.5597900654495));
#85090=CARTESIAN_POINT('Ctrl Pts',(-2.50413756504146,-4.6858650511529,-10.5597900654495));
#85091=CARTESIAN_POINT('Ctrl Pts',(-1.80048019244854,-4.48301709563195,
-10.5597900654495));
#85092=CARTESIAN_POINT('Ctrl Pts',(-1.40703076126886,-4.41160065323693,
-10.5597900654495));
#85093=CARTESIAN_POINT('Ctrl Pts',(-0.841933717031831,-4.34702984071184,
-10.5597900654496));
#85094=CARTESIAN_POINT('Ctrl Pts',(-0.658043722812697,-4.33203279124675,
-10.5597900654496));
#85095=CARTESIAN_POINT('Ctrl Pts',(-0.382154538654522,-4.31786065829338,
-10.5597900654496));
#85096=CARTESIAN_POINT('Ctrl Pts',(-0.289586349002193,-4.31451406956158,
-10.5597900654496));
#85097=CARTESIAN_POINT('Ctrl Pts',(-0.131799833370343,-4.31116993398485,
-10.5597900654496));
#85098=CARTESIAN_POINT('Ctrl Pts',(-0.0664976322663677,-4.31047485185275,
-10.5597900654496));
#85099=CARTESIAN_POINT('Ctrl Pts',(0.0639173571934239,-4.31045776213066,
-10.5597900654496));
#85100=CARTESIAN_POINT('Ctrl Pts',(0.129079361026242,-4.31113280201933,
-10.5597900654496));
#85101=CARTESIAN_POINT('Ctrl Pts',(0.28605704414335,-4.31441138123185,-10.5597900654496));
#85102=CARTESIAN_POINT('Ctrl Pts',(0.377955322537869,-4.31769531886316,
-10.5597900654496));
#85103=CARTESIAN_POINT('Ctrl Pts',(0.651486594053966,-4.33160004901355,
-10.5597900654496));
#85104=CARTESIAN_POINT('Ctrl Pts',(0.833670646936078,-4.34630752826428,
-10.5597900654496));
#85105=CARTESIAN_POINT('Ctrl Pts',(1.39309035936172,-4.40956151168582,-10.5597900654496));
#85106=CARTESIAN_POINT('Ctrl Pts',(1.78195277809562,-4.47937544741232,-10.5597900654496));
#85107=CARTESIAN_POINT('Ctrl Pts',(2.48599710360056,-4.67915031046531,-10.5597900654496));
#85108=CARTESIAN_POINT('Ctrl Pts',(2.91820462596513,-4.83459622286637,-10.5597900654496));
#85109=CARTESIAN_POINT('Ctrl Pts',(3.43432853419123,-5.23545667439774,-10.5597900654496));
#85110=CARTESIAN_POINT('Ctrl Pts',(3.55892444433031,-5.38544981580505,-10.5597900657021));
#85111=CARTESIAN_POINT('Ctrl Pts',(3.73882514967999,-5.7041522322255,-10.5597900657021));
#85112=CARTESIAN_POINT('Ctrl Pts',(3.79423029833326,-5.87690202689049,-10.5597900654496));
#85113=CARTESIAN_POINT('Ctrl Pts',(3.86701620951233,-6.23579968922608,-10.5597900654496));
#85114=CARTESIAN_POINT('Ctrl Pts',(3.88632393679749,-6.42862871197637,-10.5597900654496));
#85115=CARTESIAN_POINT('Ctrl Pts',(3.90056490239312,-6.63753909988913,-10.5597900654496));
#85116=CARTESIAN_POINT('Origin',(0.,26.5953441711815,0.));
#85117=CARTESIAN_POINT('',(-7.1947640041134,-6.63753909988913,-8.65788332730716));
#85118=CARTESIAN_POINT('',(-7.1947640041134,26.5953441711815,-8.65788332730717));
#85119=CARTESIAN_POINT('Origin',(0.,-6.63753909988913,0.));
#85120=CARTESIAN_POINT('Origin',(-9.14504645530993,26.5953441711815,-5.27989503272475));
#85121=CARTESIAN_POINT('',(-11.0953289065065,-6.63753909988913,-1.90190673814234));
#85122=CARTESIAN_POINT('',(-11.0953289065065,26.5953441711815,-1.90190673814234));
#85123=CARTESIAN_POINT('Ctrl Pts',(-11.0953289065065,-6.63753909988913,
-1.90190673814234));
#85124=CARTESIAN_POINT('Ctrl Pts',(-11.0835931462191,-6.29321943734551,
-1.92223367122555));
#85125=CARTESIAN_POINT('Ctrl Pts',(-11.0651161129459,-5.99918609364617,
-1.95423683162789));
#85126=CARTESIAN_POINT('Ctrl Pts',(-10.9824464115036,-5.56957898521099,
-2.09742495477247));
#85127=CARTESIAN_POINT('Ctrl Pts',(-10.9371509020334,-5.4206851321178,-2.17587907852964));
#85128=CARTESIAN_POINT('Ctrl Pts',(-10.8075382554253,-5.13626438454722,
-2.4003747677582));
#85129=CARTESIAN_POINT('Ctrl Pts',(-10.706766468623,-4.9763500796868,-2.57491662246939));
#85130=CARTESIAN_POINT('Ctrl Pts',(-10.3498218261682,-4.63662053620469,
-3.1931628786906));
#85131=CARTESIAN_POINT('Ctrl Pts',(-10.1022245203587,-4.50300238908727,
-3.62201399216979));
#85132=CARTESIAN_POINT('Ctrl Pts',(-9.72143984871383,-4.37950172223962,
-4.28155239020215));
#85133=CARTESIAN_POINT('Ctrl Pts',(-9.59502849226356,-4.35099240625125,
-4.50050328222773));
#85134=CARTESIAN_POINT('Ctrl Pts',(-9.40565012662499,-4.32421736597011,
-4.8285162333681));
#85135=CARTESIAN_POINT('Ctrl Pts',(-9.34174413003707,-4.31791520443562,
-4.93920466636659));
#85136=CARTESIAN_POINT('Ctrl Pts',(-9.23384225124107,-4.31174147077324,
-5.12609620267341));
#85137=CARTESIAN_POINT('Ctrl Pts',(-9.18973415909178,-4.31047784978136,
-5.202493659301));
#85138=CARTESIAN_POINT('Ctrl Pts',(-9.1028760836399,-4.31045508582798,-5.35293625903132));
#85139=CARTESIAN_POINT('Ctrl Pts',(-9.06006776325605,-4.3116233104859,-5.42708244492283));
#85140=CARTESIAN_POINT('Ctrl Pts',(-8.95941636902032,-4.31715957848673,
-5.60141577359174));
#85141=CARTESIAN_POINT('Ctrl Pts',(-8.90148409311079,-4.32252007109627,
-5.70175741886518));
#85142=CARTESIAN_POINT('Ctrl Pts',(-8.7332509121229,-4.3445763195675,-5.99314583585513));
#85143=CARTESIAN_POINT('Ctrl Pts',(-8.62236299560954,-4.36727979901891,
-6.18520934120172));
#85144=CARTESIAN_POINT('Ctrl Pts',(-8.30433573130979,-4.45894533929483,
-6.73604872116104));
#85145=CARTESIAN_POINT('Ctrl Pts',(-8.08539249003307,-4.55566580971441,
-7.11526953902613));
#85146=CARTESIAN_POINT('Ctrl Pts',(-7.68947767855954,-4.85020226805379,
-7.80101410796735));
#85147=CARTESIAN_POINT('Ctrl Pts',(-7.55829760823967,-5.01478805334227,
-8.02822465470182));
#85148=CARTESIAN_POINT('Ctrl Pts',(-7.38777942464433,-5.32531557816731,
-8.32357081230331));
#85149=CARTESIAN_POINT('Ctrl Pts',(-7.33403218269018,-5.47793756447234,
-8.4166637661346));
#85150=CARTESIAN_POINT('Ctrl Pts',(-7.22979823884874,-5.92365652676773,
-8.59720225274125));
#85151=CARTESIAN_POINT('Ctrl Pts',(-7.20800124955019,-6.249166828286,-8.63495574565837));
#85152=CARTESIAN_POINT('Ctrl Pts',(-7.1947640041134,-6.63753909988913,-8.65788332730716));
#85153=CARTESIAN_POINT('Origin',(0.,26.5953441711815,0.));
#85154=CARTESIAN_POINT('',(-11.0953289065065,26.5953441711815,1.9019067381423));
#85155=CARTESIAN_POINT('Origin',(0.,-6.63753909988913,0.));
#85156=CARTESIAN_POINT('Origin',(-9.14504645530986,26.5953441711815,5.27989503272479));
#85157=CARTESIAN_POINT('',(-7.19476400411325,26.5953441711815,8.65788332730729));
#85158=CARTESIAN_POINT('Origin',(0.,26.5953441711815,0.));
#85159=CARTESIAN_POINT('Ctrl Pts',(11.2571565141535,-6.63753909988913,1.37860406925589E-15));
#85160=CARTESIAN_POINT('Ctrl Pts',(11.2571565141535,-6.63753909988913,-22.5143130283071));
#85161=CARTESIAN_POINT('Ctrl Pts',(-11.2571565141535,-6.63753909988913,
-22.5143130283071));
#85162=CARTESIAN_POINT('Ctrl Pts',(-11.2571565141535,-6.63753909988913,
-2.75720813851178E-15));
#85163=CARTESIAN_POINT('Ctrl Pts',(11.2316061906402,-5.55581078583997,1.37547505706511E-15));
#85164=CARTESIAN_POINT('Ctrl Pts',(11.2316061906402,-5.55581078583997,-22.4632123812804));
#85165=CARTESIAN_POINT('Ctrl Pts',(-11.2316061906402,-5.55581078583997,
-22.4632123812804));
#85166=CARTESIAN_POINT('Ctrl Pts',(-11.2316061906402,-5.55581078583997,
-2.75095011413023E-15));
#85167=CARTESIAN_POINT('Ctrl Pts',(11.1603664914423,-4.97414426866896,1.36675071010562E-15));
#85168=CARTESIAN_POINT('Ctrl Pts',(11.1603664914423,-4.97414426866896,-22.3207329828847));
#85169=CARTESIAN_POINT('Ctrl Pts',(-11.1603664914423,-4.97414426866896,
-22.3207329828847));
#85170=CARTESIAN_POINT('Ctrl Pts',(-11.1603664914423,-4.97414426866896,
-2.73350142021125E-15));
#85171=CARTESIAN_POINT('Ctrl Pts',(10.527435261753,-4.27423561284,1.28923898965368E-15));
#85172=CARTESIAN_POINT('Ctrl Pts',(10.527435261753,-4.27423561284,-21.054870523506));
#85173=CARTESIAN_POINT('Ctrl Pts',(-10.527435261753,-4.27423561284,-21.054870523506));
#85174=CARTESIAN_POINT('Ctrl Pts',(-10.527435261753,-4.27423561284,-2.57847797930735E-15));
#85175=CARTESIAN_POINT('Ctrl Pts',(10.5228448600506,-4.26915945016302,1.28867682757851E-15));
#85176=CARTESIAN_POINT('Ctrl Pts',(10.5228448600506,-4.26915945016302,-21.0456897201011));
#85177=CARTESIAN_POINT('Ctrl Pts',(-10.5228448600506,-4.26915945016302,
-21.0456897201012));
#85178=CARTESIAN_POINT('Ctrl Pts',(-10.5228448600506,-4.26915945016302,
-2.57735365515702E-15));
#85179=CARTESIAN_POINT('Ctrl Pts',(10.5182544583482,-4.26408328748604,1.28811466550335E-15));
#85180=CARTESIAN_POINT('Ctrl Pts',(10.5182544583482,-4.26408328748604,-21.0365089166963));
#85181=CARTESIAN_POINT('Ctrl Pts',(-10.5182544583482,-4.26408328748604,
-21.0365089166963));
#85182=CARTESIAN_POINT('Ctrl Pts',(-10.5182544583482,-4.26408328748604,
-2.57622933100669E-15));
#85183=CARTESIAN_POINT('Ctrl Pts',(10.5136640566458,-4.25900712480906,1.28755250342818E-15));
#85184=CARTESIAN_POINT('Ctrl Pts',(10.5136640566458,-4.25900712480906,-21.0273281132915));
#85185=CARTESIAN_POINT('Ctrl Pts',(-10.5136640566458,-4.25900712480906,
-21.0273281132915));
#85186=CARTESIAN_POINT('Ctrl Pts',(-10.5136640566458,-4.25900712480906,
-2.57510500685636E-15));
#98286=UNCERTAINTY_MEASURE_WITH_UNIT(LENGTH_MEASURE(0.01),#98303,
'DISTANCE_ACCURACY_VALUE',
'Maximum model space distance between geometric entities at asserted c
onnectivities');
#98290=UNCERTAINTY_MEASURE_WITH_UNIT(LENGTH_MEASURE(0.01),#98303,
'DISTANCE_ACCURACY_VALUE',
'Maximum model space distance between geometric entities at asserted c
onnectivities');
#98298=(
GEOMETRIC_REPRESENTATION_CONTEXT(3)
GLOBAL_UNCERTAINTY_ASSIGNED_CONTEXT((#98286))
GLOBAL_UNIT_ASSIGNED_CONTEXT((#98303,#98305,#98306))
REPRESENTATION_CONTEXT('','3D')
);
#98302=(
GEOMETRIC_REPRESENTATION_CONTEXT(3)
GLOBAL_UNCERTAINTY_ASSIGNED_CONTEXT((#98290))
GLOBAL_UNIT_ASSIGNED_CONTEXT((#98303,#98305,#98306))
REPRESENTATION_CONTEXT('','3D')
);
#98303=(
LENGTH_UNIT()
NAMED_UNIT(*)
SI_UNIT(.MILLI.,.METRE.)
);
#98305=(
NAMED_UNIT(*)
PLANE_ANGLE_UNIT()
SI_UNIT($,.RADIAN.)
);
#98306=(
NAMED_UNIT(*)
SI_UNIT($,.STERADIAN.)
SOLID_ANGLE_UNIT()
);
#98314=SHAPE_DEFINITION_REPRESENTATION(#98325,#98346);
#98325=PRODUCT_DEFINITION_SHAPE('',$,#98358);
#98346=SHAPE_REPRESENTATION('',(#36369),#98298);
#98350=PRODUCT_DEFINITION_CONTEXT('part definition',#98385,'design');
#98358=PRODUCT_DEFINITION('Main Cartridge Housing',
'Main Cartridge Housing',#98369,#98350);
#98369=PRODUCT_DEFINITION_FORMATION('',$,#98394);
#98385=APPLICATION_CONTEXT(
'Core Data for Automotive Mechanical Design Process');
#98386=PRODUCT_CONTEXT('part definition',#98385,'mechanical');
#98394=PRODUCT('Main Cartridge Housing','Main Cartridge Housing',$,(#98386));
#98399=PRESENTATION_STYLE_ASSIGNMENT((#98401));
#98401=SURFACE_STYLE_USAGE(.BOTH.,#98403);
#98403=SURFACE_SIDE_STYLE('',(#98405));
#98405=SURFACE_STYLE_FILL_AREA(#98407);
#98407=FILL_AREA_STYLE('Opaque(202,209,238)',(#98409));
#98409=FILL_AREA_STYLE_COLOUR('Opaque(202,209,238)',#98411);
#98411=COLOUR_RGB('Opaque(202,209,238)', 0.31764706, 0.68627451, 0.89019608);
ENDSEC;
END-ISO-10303-21;
